ISO-10303-21;
HEADER;
FILE_DESCRIPTION (('STEP AP214'),
    '1' );
FILE_NAME ('hex bolt gradeab_din_DIN EN 24014 - M8 x 70 x 22-S.step',
    '2026-10-09T14:04:53',
    ( '' ),
    ( '' ),
    'SwSTEP 2.0',
    'SolidWorks 2021',
    '' );
FILE_SCHEMA (( 'AUTOMOTIVE_DESIGN' ));
ENDSEC;

DATA;
#64=DIRECTION ( 'NONE',  ( -1.000000000000000000, -1.224606353822377258E-16, -0.000000000000000000 ) ) ;
#80=CARTESIAN_POINT ( 'NONE',  ( 60.14984002819952025, -1.232595164407830946E-29, 4.000000000000007105 ) ) ;
#83=FACE_OUTER_BOUND ( 'NONE', #95892, .T. ) ;
#105=ORIENTED_EDGE ( 'NONE', *, *, #85457, .F. ) ;
#151=ORIENTED_EDGE ( 'NONE', *, *, #28634, .T. ) ;
#175=DIRECTION ( 'NONE',  ( -1.000000000000000000, -1.224606353822377258E-16, -0.000000000000000000 ) ) ;
#197=ORIENTED_EDGE ( 'NONE', *, *, #28937, .F. ) ;
#204=ORIENTED_EDGE ( 'NONE', *, *, #17500, .T. ) ;
#221=MECHANICAL_DESIGN_GEOMETRIC_PRESENTATION_REPRESENTATION('',(#3741),#8876);
#240=VECTOR ( 'NONE', #96144, 1000.000000000000114 ) ;
#311=CIRCLE ( 'NONE', #55388, 4.000000000000007105 ) ;
#319=ORIENTED_EDGE ( 'NONE', *, *, #87246, .F. ) ;
#331=DIRECTION ( 'NONE',  ( -1.000000000000000000, -1.224606353822377258E-16, -0.000000000000000000 ) ) ;
#339=DIRECTION ( 'NONE',  ( -1.000000000000000000, -1.224606353822377258E-16, -0.000000000000000000 ) ) ;
#345=ORIENTED_EDGE ( 'NONE', *, *, #51668, .F. ) ;
#358=DIRECTION ( 'NONE',  ( 0.000000000000000000, 1.000000000000000000, 0.000000000000000000 ) ) ;
#413=CARTESIAN_POINT ( 'NONE',  ( 67.96666666666666856, -3.309500000000000774, 4.475777889183797681E-16 ) ) ;
#454=ADVANCED_FACE ( 'NONE', ( #62064 ), #49615, .T. ) ;
#460=CONICAL_SURFACE ( 'NONE', #53864, 3.309500000000007880, 0.9599310885968770357 ) ;
#474=DIRECTION ( 'NONE',  ( 1.000000000000000000, 0.000000000000000000, 0.000000000000000000 ) ) ;
#505=ADVANCED_FACE ( 'NONE', ( #4864 ), #70658, .T. ) ;
#572=CARTESIAN_POINT ( 'NONE',  ( 73.59428447264397732, 6.856755485862130937E-15, 0.000000000000000000 ) ) ;
#631=CARTESIAN_POINT ( 'NONE',  ( 0.000000000000000000, 0.000000000000000000, 0.000000000000000000 ) ) ;
#633=CARTESIAN_POINT ( 'NONE',  ( 75.30000000000001137, 4.052968581778165278E-16, -3.309499999999999886 ) ) ;
#655=DIRECTION ( 'NONE',  ( 0.000000000000000000, 0.000000000000000000, 1.000000000000000000 ) ) ;
#740=DIRECTION ( 'NONE',  ( 1.000000000000000000, 1.224606353822377258E-16, 0.000000000000000000 ) ) ;
#794=AXIS2_PLACEMENT_3D ( 'NONE', #54164, #55232, #13714 ) ;
#820=DIRECTION ( 'NONE',  ( 1.000000000000000000, 0.000000000000000000, 0.000000000000000000 ) ) ;
#848=DIRECTION ( 'NONE',  ( 0.000000000000000000, 1.000000000000000000, 0.000000000000000000 ) ) ;
#851=EDGE_LOOP ( 'NONE', ( #68969, #20502, #6587, #6206, #66955 ) ) ;
#874=CARTESIAN_POINT ( 'NONE',  ( 55.74444444444444713, 6.915964383211875250E-15, 0.000000000000000000 ) ) ;
#888=FACE_OUTER_BOUND ( 'NONE', #42515, .T. ) ;
#904=ORIENTED_EDGE ( 'NONE', *, *, #62879, .F. ) ;
#954=ORIENTED_EDGE ( 'NONE', *, *, #59257, .T. ) ;
#989=ORIENTED_EDGE ( 'NONE', *, *, #17999, .T. ) ;
#1029=VECTOR ( 'NONE', #105452, 1000.000000000000000 ) ;
#1032=AXIS2_PLACEMENT_3D ( 'NONE', #27039, #92244, #21458 ) ;
#1043=CONICAL_SURFACE ( 'NONE', #28691, 4.000000000000007105, 0.9599310885968835860 ) ;
#1061=DIRECTION ( 'NONE',  ( -0.5735764363510497121, 0.8191520442889892450, 1.003171929053521665E-16 ) ) ;
#1069=ORIENTED_EDGE ( 'NONE', *, *, #67018, .F. ) ;
#1105=VERTEX_POINT ( 'NONE', #16006 ) ;
#1136=EDGE_CURVE ( 'NONE', #26511, #53379, #48882, .T. ) ;
#1151=AXIS2_PLACEMENT_3D ( 'NONE', #56465, #98526, #74774 ) ;
#1206=DIRECTION ( 'NONE',  ( 0.000000000000000000, -1.000000000000000000, 0.000000000000000000 ) ) ;
#1212=CARTESIAN_POINT ( 'NONE',  ( 4.699999999999999289, 7.505553499465139389, 0.000000000000000000 ) ) ;
#1242=ORIENTED_EDGE ( 'NONE', *, *, #17766, .F. ) ;
#1246=DIRECTION ( 'NONE',  ( 0.000000000000000000, 0.000000000000000000, 1.000000000000000000 ) ) ;
#1269=AXIS2_PLACEMENT_3D ( 'NONE', #64012, #96889, #7855 ) ;
#1274=DIRECTION ( 'NONE',  ( -1.000000000000000000, -1.224606353822377258E-16, -0.000000000000000000 ) ) ;
#1292=FACE_OUTER_BOUND ( 'NONE', #5334, .T. ) ;
#1320=CARTESIAN_POINT ( 'NONE',  ( 0.01372220897661855475, 5.948365447239585713, 2.697128823393877273 ) ) ;
#1333=ORIENTED_EDGE ( 'NONE', *, *, #88212, .F. ) ;
#1349=DIRECTION ( 'NONE',  ( 0.000000000000000000, -1.000000000000000000, 0.000000000000000000 ) ) ;
#1388=ORIENTED_EDGE ( 'NONE', *, *, #43399, .F. ) ;
#1431=CARTESIAN_POINT ( 'NONE',  ( 56.48317336153285595, 6.856755485862130937E-15, 0.000000000000000000 ) ) ;
#1525=AXIS2_PLACEMENT_3D ( 'NONE', #82681, #15823, #655 ) ;
#1581=VERTEX_POINT ( 'NONE', #17361 ) ;
#1605=CIRCLE ( 'NONE', #75690, 3.309499999999999886 ) ;
#1609=DIRECTION ( 'NONE',  ( -1.000000000000000000, -1.224606353822377258E-16, -0.000000000000000000 ) ) ;
#1626=CARTESIAN_POINT ( 'NONE',  ( 61.85555555555556140, 6.915964383211875250E-15, 0.000000000000000000 ) ) ;
#1649=CARTESIAN_POINT ( 'NONE',  ( 4.699999999999999289, 3.752776749732569694, 6.499999999999997335 ) ) ;
#1708=CIRCLE ( 'NONE', #68888, 4.000000000000007105 ) ;
#1732=ORIENTED_EDGE ( 'NONE', *, *, #22739, .T. ) ;
#1745=CARTESIAN_POINT ( 'NONE',  ( 56.96666666666666856, -3.309500000000000774, 0.000000000000000000 ) ) ;
#1752=ADVANCED_FACE ( 'NONE', ( #101972 ), #90896, .T. ) ;
#1759=CARTESIAN_POINT ( 'NONE',  ( 67.96666666666666856, 6.915964383211875250E-15, 0.000000000000000000 ) ) ;
#1809=AXIS2_PLACEMENT_3D ( 'NONE', #3719, #4238, #38229 ) ;
#1872=CARTESIAN_POINT ( 'NONE',  ( 58.92761780597729881, -1.232595164407830946E-29, 4.000000000000007105 ) ) ;
#1908=DIRECTION ( 'NONE',  ( 1.000000000000000000, 1.224606353822377258E-16, 0.000000000000000000 ) ) ;
#1973=EDGE_CURVE ( 'NONE', #102083, #106204, #75445, .T. ) ;
#1976=DIRECTION ( 'NONE',  ( -1.000000000000000000, -1.224606353822377258E-16, -0.000000000000000000 ) ) ;
#1978=DIRECTION ( 'NONE',  ( -1.000000000000000000, -1.224606353822377258E-16, -0.000000000000000000 ) ) ;
#1992=DIRECTION ( 'NONE',  ( 0.000000000000000000, 0.000000000000000000, -1.000000000000000000 ) ) ;
#2030=FACE_OUTER_BOUND ( 'NONE', #68537, .T. ) ;
#2084=DIRECTION ( 'NONE',  ( -1.000000000000000000, -1.224606353822377258E-16, -0.000000000000000000 ) ) ;
#2085=CARTESIAN_POINT ( 'NONE',  ( 67.22793774957824553, 6.975173280561618775E-15, 0.000000000000000000 ) ) ;
#2188=ORIENTED_EDGE ( 'NONE', *, *, #63395, .F. ) ;
#2194=ORIENTED_EDGE ( 'NONE', *, *, #43555, .T. ) ;
#2253=AXIS2_PLACEMENT_3D ( 'NONE', #13145, #29904, #55199 ) ;
#2255=LINE ( 'NONE', #28190, #26239 ) ;
#2288=DIRECTION ( 'NONE',  ( 0.000000000000000000, 0.000000000000000000, 1.000000000000000000 ) ) ;
#2327=DIRECTION ( 'NONE',  ( -1.000000000000000000, -1.224606353822377258E-16, -0.000000000000000000 ) ) ;
#2329=CARTESIAN_POINT ( 'NONE',  ( 4.699999999999999289, 0.000000000000000000, 0.000000000000000000 ) ) ;
#2333=CARTESIAN_POINT ( 'NONE',  ( 55.00571552735602410, 4.000000000000014211, 0.000000000000000000 ) ) ;
#2334=AXIS2_PLACEMENT_3D ( 'NONE', #102678, #94054, #61717 ) ;
#2395=EDGE_CURVE ( 'NONE', #21935, #99732, #40999, .T. ) ;
#2411=CARTESIAN_POINT ( 'NONE',  ( 0.000000000000000000, 0.000000000000000000, 0.000000000000000000 ) ) ;
#2438=EDGE_CURVE ( 'NONE', #23524, #39236, #72034, .T. ) ;
#2495=EDGE_CURVE ( 'NONE', #39308, #32062, #96125, .T. ) ;
#2515=VERTEX_POINT ( 'NONE', #76379 ) ;
#2521=EDGE_CURVE ( 'NONE', #59573, #6296, #77259, .T. ) ;
#2584=FACE_OUTER_BOUND ( 'NONE', #20421, .T. ) ;
#2602=EDGE_LOOP ( 'NONE', ( #104914, #105323, #91552, #92595, #60643, #23938 ) ) ;
#2667=CONICAL_SURFACE ( 'NONE', #66429, 4.000000000000007105, 0.9599310885968835860 ) ;
#2681=VERTEX_POINT ( 'NONE', #79573 ) ;
#2714=ORIENTED_EDGE ( 'NONE', *, *, #61379, .T. ) ;
#2729=CARTESIAN_POINT ( 'NONE',  ( 70.41111111111112564, 3.309500000000014541, 0.000000000000000000 ) ) ;
#2784=PRODUCT_DEFINITION_SHAPE ( 'NONE', 'NONE',  #50892 ) ;
#2792=AXIS2_PLACEMENT_3D ( 'NONE', #70403, #18686, #51544 ) ;
#2870=DIRECTION ( 'NONE',  ( 0.000000000000000000, -1.000000000000000000, 0.000000000000000000 ) ) ;
#2884=CONICAL_SURFACE ( 'NONE', #63193, 3.309500000000007880, 0.9599310885968770357 ) ;
#2907=ORIENTED_EDGE ( 'NONE', *, *, #36895, .T. ) ;
#2917=VERTEX_POINT ( 'NONE', #55155 ) ;
#2933=CARTESIAN_POINT ( 'NONE',  ( 57.45015997180046696, 6.975173280561618775E-15, 0.000000000000000000 ) ) ;
#3008=CARTESIAN_POINT ( 'NONE',  ( 0.000000000000000000, 0.000000000000000000, 0.000000000000000000 ) ) ;
#3063=DIRECTION ( 'NONE',  ( 0.000000000000000000, -1.000000000000000000, 0.000000000000000000 ) ) ;
#3070=CONICAL_SURFACE ( 'NONE', #51231, 4.000000000000007105, 0.9599310885968835860 ) ;
#3071=CIRCLE ( 'NONE', #8219, 4.000000000000007105 ) ;
#3167=VERTEX_POINT ( 'NONE', #83167 ) ;
#3174=ORIENTED_EDGE ( 'NONE', *, *, #9014, .F. ) ;
#3189=ADVANCED_FACE ( 'NONE', ( #83 ), #68378, .T. ) ;
#3198=DIRECTION ( 'NONE',  ( -1.000000000000000000, -0.000000000000000000, -0.000000000000000000 ) ) ;
#3203=DIRECTION ( 'NONE',  ( -1.000000000000000000, -0.000000000000000000, -0.000000000000000000 ) ) ;
#3228=LINE ( 'NONE', #85759, #94927 ) ;
#3232=ORIENTED_EDGE ( 'NONE', *, *, #82323, .F. ) ;
#3248=CARTESIAN_POINT ( 'NONE',  ( 65.03872891708842019, 6.856755485862130937E-15, 0.000000000000000000 ) ) ;
#3259=EDGE_LOOP ( 'NONE', ( #50709, #49256, #100260, #36531, #1388, #54276 ) ) ;
#3266=EDGE_CURVE ( 'NONE', #82529, #31918, #34401, .T. ) ;
#3269=VECTOR ( 'NONE', #29765, 1000.000000000000000 ) ;
#3278=ORIENTED_EDGE ( 'NONE', *, *, #32936, .F. ) ;
#3398=EDGE_CURVE ( 'NONE', #101318, #85895, #51098, .T. ) ;
#3405=ORIENTED_EDGE ( 'NONE', *, *, #89956, .T. ) ;
#3535=ORIENTED_EDGE ( 'NONE', *, *, #3927, .F. ) ;
#3562=AXIS2_PLACEMENT_3D ( 'NONE', #68522, #52850, #51778 ) ;
#3582=VECTOR ( 'NONE', #88790, 1000.000000000000000 ) ;
#3599=AXIS2_PLACEMENT_3D ( 'NONE', #64956, #65494, #98381 ) ;
#3606=CARTESIAN_POINT ( 'NONE',  ( 55.74444444444444713, 6.915964383211875250E-15, 0.000000000000000000 ) ) ;
#3615=CIRCLE ( 'NONE', #69053, 4.000000000000007105 ) ;
#3644=CIRCLE ( 'NONE', #32915, 4.000000000000007105 ) ;
#3673=FILL_AREA_STYLE_COLOUR ( '', #64028 ) ;
#3704=EDGE_CURVE ( 'NONE', #75804, #82092, #99810, .T. ) ;
#3719=CARTESIAN_POINT ( 'NONE',  ( 60.63333333333333286, 6.915964383211875250E-15, 0.000000000000000000 ) ) ;
#3741=STYLED_ITEM ( 'NONE', ( #69471 ), #19502 ) ;
#3838=FACE_OUTER_BOUND ( 'NONE', #53178, .T. ) ;
#3840=VECTOR ( 'NONE', #104714, 1000.000000000000000 ) ;
#3878=AXIS2_PLACEMENT_3D ( 'NONE', #4173, #23030, #79637 ) ;
#3882=VERTEX_POINT ( 'NONE', #36725 ) ;
#3884=CARTESIAN_POINT ( 'NONE',  ( 74.56127108291157413, 6.975173280561618775E-15, 0.000000000000000000 ) ) ;
#3890=CARTESIAN_POINT ( 'NONE',  ( 64.78349330513380266, 6.975173280561618775E-15, 0.000000000000000000 ) ) ;
#3898=AXIS2_PLACEMENT_3D ( 'NONE', #21541, #54376, #80797 ) ;
#3927=EDGE_CURVE ( 'NONE', #21000, #104615, #20305, .T. ) ;
#3944=DIRECTION ( 'NONE',  ( 0.000000000000000000, -1.000000000000000000, 0.000000000000000000 ) ) ;
#3950=DIRECTION ( 'NONE',  ( -1.000000000000000000, -1.224606353822377258E-16, -0.000000000000000000 ) ) ;
#3986=DIRECTION ( 'NONE',  ( 0.000000000000000000, 0.000000000000000000, -1.000000000000000000 ) ) ;
#4022=VERTEX_POINT ( 'NONE', #21588 ) ;
#4041=CIRCLE ( 'NONE', #14334, 4.000000000000000000 ) ;
#4110=CARTESIAN_POINT ( 'NONE',  ( 64.78349330513380266, 6.975173280561618775E-15, 0.000000000000000000 ) ) ;
#4113=ORIENTED_EDGE ( 'NONE', *, *, #28865, .T. ) ;
#4139=( GEOMETRIC_REPRESENTATION_CONTEXT ( 3 ) GLOBAL_UNCERTAINTY_ASSIGNED_CONTEXT ( ( #57512 ) ) GLOBAL_UNIT_ASSIGNED_CONTEXT ( ( #104150, #65820, #24854 ) ) REPRESENTATION_CONTEXT ( 'NONE', 'WORKASPACE' ) );
#4149=ADVANCED_FACE ( 'NONE', ( #86842 ), #13374, .T. ) ;
#4173=CARTESIAN_POINT ( 'NONE',  ( 55.00571552735602410, 6.975173280561618775E-15, 0.000000000000000000 ) ) ;
#4182=EDGE_LOOP ( 'NONE', ( #77702, #62178, #72671, #28091, #74221 ) ) ;
#4200=CARTESIAN_POINT ( 'NONE',  ( 0.000000000000000000, 0.000000000000000000, 0.000000000000000000 ) ) ;
#4238=DIRECTION ( 'NONE',  ( -1.000000000000000000, -1.224606353822377258E-16, -0.000000000000000000 ) ) ;
#4281=EDGE_CURVE ( 'NONE', #68880, #20574, #54712, .T. ) ;
#4287=EDGE_CURVE ( 'NONE', #39378, #59650, #82283, .T. ) ;
#4289=DIRECTION ( 'NONE',  ( 0.5735764363510442720, -0.8191520442889930198, 1.003171929053526349E-16 ) ) ;
#4307=LINE ( 'NONE', #62554, #66069 ) ;
#4314=CIRCLE ( 'NONE', #14605, 3.309500000000007880 ) ;
#4336=CARTESIAN_POINT ( 'NONE',  ( 71.63333333333333997, -3.309500000000000774, 4.475777889183797681E-16 ) ) ;
#4361=ORIENTED_EDGE ( 'NONE', *, *, #75414, .T. ) ;
#4408=CARTESIAN_POINT ( 'NONE',  ( 0.000000000000000000, 4.898587196589412829E-16, -4.000000000000000000 ) ) ;
#4419=LINE ( 'NONE', #37357, #37548 ) ;
#4460=CIRCLE ( 'NONE', #45815, 4.000000000000007105 ) ;
#4469=ORIENTED_EDGE ( 'NONE', *, *, #21854, .T. ) ;
#4497=CARTESIAN_POINT ( 'NONE',  ( 63.56127108291158123, -4.000000000000000000, 4.898587196589421703E-16 ) ) ;
#4505=DIRECTION ( 'NONE',  ( 0.000000000000000000, 0.000000000000000000, -1.000000000000000000 ) ) ;
#4517=VERTEX_POINT ( 'NONE', #13318 ) ;
#4561=DIRECTION ( 'NONE',  ( 0.000000000000000000, -1.000000000000000000, 0.000000000000000000 ) ) ;
#4646=ORIENTED_EDGE ( 'NONE', *, *, #10088, .T. ) ;
#4670=CARTESIAN_POINT ( 'NONE',  ( 62.33904886068935980, 6.975173280561618775E-15, 0.000000000000000000 ) ) ;
#4732=ORIENTED_EDGE ( 'NONE', *, *, #20921, .F. ) ;
#4769=DIRECTION ( 'NONE',  ( -0.5735764363510494901, -0.8191520442889894671, 0.000000000000000000 ) ) ;
#4777=AXIS2_PLACEMENT_3D ( 'NONE', #39604, #100465, #100999 ) ;
#4785=CIRCLE ( 'NONE', #46135, 4.000000000000007105 ) ;
#4793=CARTESIAN_POINT ( 'NONE',  ( 0.5805565836007581249, -3.752776749732553263, 6.499999999999999112 ) ) ;
#4831=CARTESIAN_POINT ( 'NONE',  ( 58.67238219402268840, -1.232595164407830946E-29, 4.000000000000007105 ) ) ;
#4834=VECTOR ( 'NONE', #91626, 999.9999999999998863 ) ;
#4850=ORIENTED_EDGE ( 'NONE', *, *, #74021, .F. ) ;
#4863=CARTESIAN_POINT ( 'NONE',  ( 74.07777777777778283, 3.309500000000014541, 0.000000000000000000 ) ) ;
#4864=FACE_OUTER_BOUND ( 'NONE', #3259, .T. ) ;
#4870=ORIENTED_EDGE ( 'NONE', *, *, #31867, .F. ) ;
#4894=ORIENTED_EDGE ( 'NONE', *, *, #9741, .F. ) ;
#4976=PLANE ( 'NONE',  #12990 ) ;
#4983=EDGE_CURVE ( 'NONE', #38550, #69704, #25365, .T. ) ;
#5029=LINE ( 'NONE', #13093, #12433 ) ;
#5047=FACE_OUTER_BOUND ( 'NONE', #32184, .T. ) ;
#5066=EDGE_CURVE ( 'NONE', #66517, #45176, #31029, .T. ) ;
#5067=ORIENTED_EDGE ( 'NONE', *, *, #39618, .F. ) ;
#5094=ORIENTED_EDGE ( 'NONE', *, *, #63924, .F. ) ;
#5141=DIRECTION ( 'NONE',  ( 0.000000000000000000, 0.000000000000000000, 1.000000000000000000 ) ) ;
#5165=DIRECTION ( 'NONE',  ( 0.000000000000000000, 0.000000000000000000, -1.000000000000000000 ) ) ;
#5334=EDGE_LOOP ( 'NONE', ( #87031, #100414, #14652, #73546, #45242 ) ) ;
#5346=VECTOR ( 'NONE', #17120, 1000.000000000000000 ) ;
#5373=CIRCLE ( 'NONE', #84603, 4.000000000000007105 ) ;
#5381=DIRECTION ( 'NONE',  ( 0.000000000000000000, -1.000000000000000000, 0.000000000000000000 ) ) ;
#5391=LINE ( 'NONE', #88436, #15143 ) ;
#5494=CARTESIAN_POINT ( 'NONE',  ( 5.299999999999999822, 5.388445916248354013E-16, 4.400000000000000355 ) ) ;
#5547=DIRECTION ( 'NONE',  ( -1.000000000000000000, -0.000000000000000000, -0.000000000000000000 ) ) ;
#5556=CONICAL_SURFACE ( 'NONE', #29768, 3.309500000000007880, 0.9599310885968770357 ) ;
#5571=LINE ( 'NONE', #104261, #62919 ) ;
#5611=EDGE_CURVE ( 'NONE', #14056, #31918, #6228, .T. ) ;
#5622=EDGE_CURVE ( 'NONE', #25775, #1581, #36818, .T. ) ;
#5638=AXIS2_PLACEMENT_3D ( 'NONE', #95639, #48122, #97734 ) ;
#5647=FACE_OUTER_BOUND ( 'NONE', #86646, .T. ) ;
#5674=EDGE_CURVE ( 'NONE', #87774, #95890, #46979, .T. ) ;
#5710=ORIENTED_EDGE ( 'NONE', *, *, #15452, .F. ) ;
#5742=CARTESIAN_POINT ( 'NONE',  ( 63.81650669486618455, 4.898587196589294500E-16, -4.000000000000007105 ) ) ;
#5781=EDGE_CURVE ( 'NONE', #43471, #37118, #92772, .T. ) ;
#5839=CARTESIAN_POINT ( 'NONE',  ( -6.595563215953496614E-15, -5.469921996229793137, 3.525817189091417170 ) ) ;
#5847=LINE ( 'NONE', #21034, #90037 ) ;
#5880=EDGE_LOOP ( 'NONE', ( #96406, #97052, #13928, #8893, #38450 ) ) ;
#5888=VERTEX_POINT ( 'NONE', #96483 ) ;
#6004=DIRECTION ( 'NONE',  ( 0.000000000000000000, -1.000000000000000000, 0.000000000000000000 ) ) ;
#6005=ORIENTED_EDGE ( 'NONE', *, *, #23686, .T. ) ;
#6087=DIRECTION ( 'NONE',  ( -1.000000000000000000, -1.224606353822377258E-16, -0.000000000000000000 ) ) ;
#6099=ORIENTED_EDGE ( 'NONE', *, *, #19298, .T. ) ;
#6159=CARTESIAN_POINT ( 'NONE',  ( 72.37206225042174879, 4.898587196589294500E-16, -4.000000000000007105 ) ) ;
#6206=ORIENTED_EDGE ( 'NONE', *, *, #12314, .F. ) ;
#6217=ORIENTED_EDGE ( 'NONE', *, *, #53256, .T. ) ;
#6228=CIRCLE ( 'NONE', #57880, 6.499999999999999112 ) ;
#6296=VERTEX_POINT ( 'NONE', #68359 ) ;
#6317=AXIS2_PLACEMENT_3D ( 'NONE', #90288, #48743, #58457 ) ;
#6334=FACE_OUTER_BOUND ( 'NONE', #71553, .T. ) ;
#6359=CONICAL_SURFACE ( 'NONE', #11520, 3.309500000000007880, 0.9599310885968770357 ) ;
#6388=DIRECTION ( 'NONE',  ( -1.000000000000000000, -0.000000000000000000, -0.000000000000000000 ) ) ;
#6430=DIRECTION ( 'NONE',  ( 0.000000000000000000, -1.000000000000000000, 0.000000000000000000 ) ) ;
#6434=VERTEX_POINT ( 'NONE', #24596 ) ;
#6447=DIRECTION ( 'NONE',  ( 0.000000000000000000, -1.000000000000000000, 0.000000000000000000 ) ) ;
#6458=ORIENTED_EDGE ( 'NONE', *, *, #53109, .F. ) ;
#6480=AXIS2_PLACEMENT_3D ( 'NONE', #92796, #57752, #83631 ) ;
#6495=VERTEX_POINT ( 'NONE', #99504 ) ;
#6528=AXIS2_PLACEMENT_3D ( 'NONE', #61092, #68662, #84826 ) ;
#6574=DIRECTION ( 'NONE',  ( -1.000000000000000000, -0.000000000000000000, -0.000000000000000000 ) ) ;
#6587=ORIENTED_EDGE ( 'NONE', *, *, #84567, .T. ) ;
#6604=AXIS2_PLACEMENT_3D ( 'NONE', #51342, #76684, #35199 ) ;
#6619=ORIENTED_EDGE ( 'NONE', *, *, #12314, .T. ) ;
#6650=DIRECTION ( 'NONE',  ( -1.000000000000000000, -1.224606353822377258E-16, -0.000000000000000000 ) ) ;
#6665=DIRECTION ( 'NONE',  ( 0.000000000000000000, 0.000000000000000000, 1.000000000000000000 ) ) ;
#6676=CYLINDRICAL_SURFACE ( 'NONE', #4777, 4.000000000000000000 ) ;
#6680=EDGE_CURVE ( 'NONE', #30745, #43471, #70609, .T. ) ;
#6705=CARTESIAN_POINT ( 'NONE',  ( 63.81650669486618455, 6.856755485862130937E-15, 0.000000000000000000 ) ) ;
#6728=CARTESIAN_POINT ( 'NONE',  ( 59.89460441624491693, 6.975173280561618775E-15, 0.000000000000000000 ) ) ;
#6746=EDGE_CURVE ( 'NONE', #71455, #6434, #43942, .T. ) ;
#6791=CARTESIAN_POINT ( 'NONE',  ( 0.5805565836007582359, 3.752776749732553263, -6.499999999999999112 ) ) ;
#6816=FACE_OUTER_BOUND ( 'NONE', #98880, .T. ) ;
#6818=CARTESIAN_POINT ( 'NONE',  ( 68.45015997180047407, -1.232595164407830946E-29, 4.000000000000007105 ) ) ;
#6819=VECTOR ( 'NONE', #76831, 1000.000000000000000 ) ;
#6862=ORIENTED_EDGE ( 'NONE', *, *, #101224, .F. ) ;
#6871=ORIENTED_EDGE ( 'NONE', *, *, #16330, .T. ) ;
#6877=ADVANCED_FACE ( 'NONE', ( #97262 ), #2884, .T. ) ;
#6930=CARTESIAN_POINT ( 'NONE',  ( 0.000000000000000000, 0.000000000000000000, 4.000000000000000000 ) ) ;
#6953=CIRCLE ( 'NONE', #32859, 4.000000000000007105 ) ;
#6963=DIRECTION ( 'NONE',  ( -1.000000000000000000, -0.000000000000000000, -0.000000000000000000 ) ) ;
#7156=ORIENTED_EDGE ( 'NONE', *, *, #51668, .T. ) ;
#7191=CARTESIAN_POINT ( 'NONE',  ( 60.63333333333333286, 6.915964383211875250E-15, 0.000000000000000000 ) ) ;
#7195=ORIENTED_EDGE ( 'NONE', *, *, #55288, .T. ) ;
#7221=CARTESIAN_POINT ( 'NONE',  ( 55.26095113931063452, 4.000000000000015099, 4.898587196589422689E-16 ) ) ;
#7279=ORIENTED_EDGE ( 'NONE', *, *, #44473, .F. ) ;
#7294=EDGE_LOOP ( 'NONE', ( #85658, #92876, #22062, #11630, #39143, #60502 ) ) ;
#7306=VERTEX_POINT ( 'NONE', #27957 ) ;
#7346=CARTESIAN_POINT ( 'NONE',  ( 61.11682663846713837, 6.975173280561618775E-15, 0.000000000000000000 ) ) ;
#7404=VERTEX_POINT ( 'NONE', #72598 ) ;
#7416=ORIENTED_EDGE ( 'NONE', *, *, #19218, .F. ) ;
#7430=ORIENTED_EDGE ( 'NONE', *, *, #100420, .F. ) ;
#7432=FACE_OUTER_BOUND ( 'NONE', #89099, .T. ) ;
#7450=PLANE ( 'NONE',  #51352 ) ;
#7466=DIRECTION ( 'NONE',  ( 0.000000000000000000, -1.000000000000000000, 0.000000000000000000 ) ) ;
#7504=CARTESIAN_POINT ( 'NONE',  ( 67.22793774957824553, 6.975173280561618775E-15, 0.000000000000000000 ) ) ;
#7511=CIRCLE ( 'NONE', #52330, 6.499999999999999112 ) ;
#7581=CIRCLE ( 'NONE', #55847, 4.000000000000007105 ) ;
#7686=VECTOR ( 'NONE', #91595, 1000.000000000000000 ) ;
#7738=VERTEX_POINT ( 'NONE', #97804 ) ;
#7753=VECTOR ( 'NONE', #73946, 1000.000000000000227 ) ;
#7759=CIRCLE ( 'NONE', #99073, 4.000000000000007105 ) ;
#7762=CONICAL_SURFACE ( 'NONE', #87028, 4.000000000000007105, 0.9599310885968835860 ) ;
#7806=ADVANCED_FACE ( 'NONE', ( #16909 ), #57333, .F. ) ;
#7810=EDGE_CURVE ( 'NONE', #99732, #99463, #100094, .T. ) ;
#7811=ORIENTED_EDGE ( 'NONE', *, *, #69806, .T. ) ;
#7827=VECTOR ( 'NONE', #51569, 1000.000000000000000 ) ;
#7843=CARTESIAN_POINT ( 'NONE',  ( 0.01372220897661434458, 5.309964801958107827, -3.802871176606132497 ) ) ;
#7846=EDGE_CURVE ( 'NONE', #56292, #38550, #3644, .T. ) ;
#7855=DIRECTION ( 'NONE',  ( 0.000000000000000000, -1.000000000000000000, 0.000000000000000000 ) ) ;
#7867=ORIENTED_EDGE ( 'NONE', *, *, #59257, .F. ) ;
#7886=ORIENTED_EDGE ( 'NONE', *, *, #6746, .T. ) ;
#7916=CARTESIAN_POINT ( 'NONE',  ( 0.2573354458087825369, 6.889406814520509847, -1.067197363239225760 ) ) ;
#7965=VECTOR ( 'NONE', #82912, 1000.000000000000227 ) ;
#7975=AXIS2_PLACEMENT_3D ( 'NONE', #99931, #16359, #67054 ) ;
#7995=AXIS2_PLACEMENT_3D ( 'NONE', #89206, #8802, #48192 ) ;
#8010=CARTESIAN_POINT ( 'NONE',  ( 56.22793774957824553, -4.000000000000000000, 4.898587196589421703E-16 ) ) ;
#8016=ORIENTED_EDGE ( 'NONE', *, *, #54369, .F. ) ;
#8058=AXIS2_PLACEMENT_3D ( 'NONE', #86590, #52587, #44520 ) ;
#8059=CARTESIAN_POINT ( 'NONE',  ( 63.07777777777777573, 6.915964383211875250E-15, 0.000000000000000000 ) ) ;
#8060=ADVANCED_FACE ( 'NONE', ( #73384 ), #106281, .T. ) ;
#8077=VECTOR ( 'NONE', #10387, 1000.000000000000114 ) ;
#8155=CARTESIAN_POINT ( 'NONE',  ( 69.67238219402268840, -4.000000000000000888, 4.898587196589422689E-16 ) ) ;
#8173=VECTOR ( 'NONE', #88452, 1000.000000000000114 ) ;
#8174=DIRECTION ( 'NONE',  ( 0.000000000000000000, -1.000000000000000000, 0.000000000000000000 ) ) ;
#8219=AXIS2_PLACEMENT_3D ( 'NONE', #99821, #91745, #51258 ) ;
#8222=EDGE_CURVE ( 'NONE', #66339, #31268, #41425, .T. ) ;
#8224=VERTEX_POINT ( 'NONE', #28088 ) ;
#8247=ADVANCED_FACE ( 'NONE', ( #35646 ), #19476, .T. ) ;
#8251=ORIENTED_EDGE ( 'NONE', *, *, #84159, .F. ) ;
#8320=CARTESIAN_POINT ( 'NONE',  ( 0.000000000000000000, 7.960204194457794491E-16, -6.499999999999999112 ) ) ;
#8337=ORIENTED_EDGE ( 'NONE', *, *, #73986, .F. ) ;
#8358=VERTEX_POINT ( 'NONE', #86834 ) ;
#8362=LINE ( 'NONE', #26196, #92688 ) ;
#8372=CARTESIAN_POINT ( 'NONE',  ( -1.902012483059531411E-15, 5.788408252967903955, 2.974182810908594377 ) ) ;
#8402=CARTESIAN_POINT ( 'NONE',  ( 4.699999999999999289, 3.752776749732553263, -6.499999999999999112 ) ) ;
#8426=ORIENTED_EDGE ( 'NONE', *, *, #71393, .F. ) ;
#8443=CIRCLE ( 'NONE', #96326, 4.000000000000007105 ) ;
#8468=VERTEX_POINT ( 'NONE', #65726 ) ;
#8483=CIRCLE ( 'NONE', #70479, 4.000000000000007105 ) ;
#8506=DIRECTION ( 'NONE',  ( 0.000000000000000000, -1.000000000000000000, 0.000000000000000000 ) ) ;
#8564=FACE_OUTER_BOUND ( 'NONE', #18414, .T. ) ;
#8571=ORIENTED_EDGE ( 'NONE', *, *, #89960, .F. ) ;
#8594=EDGE_CURVE ( 'NONE', #58641, #103962, #70382, .T. ) ;
#8605=DIRECTION ( 'NONE',  ( 0.000000000000000000, 0.000000000000000000, -1.000000000000000000 ) ) ;
#8665=DIRECTION ( 'NONE',  ( 0.000000000000000000, 0.000000000000000000, -1.000000000000000000 ) ) ;
#8681=ORIENTED_EDGE ( 'NONE', *, *, #94898, .F. ) ;
#8702=CARTESIAN_POINT ( 'NONE',  ( 55.00571552735602410, -4.000000000000000888, 4.898587196589422689E-16 ) ) ;
#8714=CARTESIAN_POINT ( 'NONE',  ( 55.00571552735602410, 4.898587196589294500E-16, -4.000000000000007105 ) ) ;
#8747=CARTESIAN_POINT ( 'NONE',  ( 59.41111111111111143, 6.915964383211875250E-15, 0.000000000000000000 ) ) ;
#8764=FACE_OUTER_BOUND ( 'NONE', #41937, .T. ) ;
#8772=CARTESIAN_POINT ( 'NONE',  ( 72.11682663846713126, -4.000000000000000888, 4.898587196589422689E-16 ) ) ;
#8787=DIRECTION ( 'NONE',  ( 0.000000000000000000, -1.000000000000000000, 0.000000000000000000 ) ) ;
#8802=DIRECTION ( 'NONE',  ( 1.000000000000000000, 1.224606353822377258E-16, 0.000000000000000000 ) ) ;
#8864=ADVANCED_FACE ( 'NONE', ( #53814 ), #59850, .T. ) ;
#8873=DIRECTION ( 'NONE',  ( 1.000000000000000000, 1.224606353822377258E-16, 0.000000000000000000 ) ) ;
#8876=( GEOMETRIC_REPRESENTATION_CONTEXT ( 3 ) GLOBAL_UNCERTAINTY_ASSIGNED_CONTEXT ( ( #33296 ) ) GLOBAL_UNIT_ASSIGNED_CONTEXT ( ( #73148, #64561, #30621 ) ) REPRESENTATION_CONTEXT ( 'NONE', 'WORKASPACE' ) );
#8885=ORIENTED_EDGE ( 'NONE', *, *, #22997, .T. ) ;
#8893=ORIENTED_EDGE ( 'NONE', *, *, #72319, .F. ) ;
#9005=CARTESIAN_POINT ( 'NONE',  ( 72.37206225042174879, 6.856755485862130937E-15, 0.000000000000000000 ) ) ;
#9014=EDGE_CURVE ( 'NONE', #98734, #7404, #4785, .T. ) ;
#9016=VERTEX_POINT ( 'NONE', #32217 ) ;
#9081=CARTESIAN_POINT ( 'NONE',  ( 69.92761780597730592, 6.856755485862130937E-15, 0.000000000000000000 ) ) ;
#9082=ORIENTED_EDGE ( 'NONE', *, *, #44161, .T. ) ;
#9096=EDGE_LOOP ( 'NONE', ( #88332, #60119 ) ) ;
#9108=AXIS2_PLACEMENT_3D ( 'NONE', #27955, #52168, #85623 ) ;
#9137=CARTESIAN_POINT ( 'NONE',  ( 63.07777777777777573, -3.309500000000000774, 4.475777889183797681E-16 ) ) ;
#9256=CARTESIAN_POINT ( 'NONE',  ( 0.000000000000000000, 1.502314598737160017E-15, -6.500000000000000000 ) ) ;
#9275=ADVANCED_FACE ( 'NONE', ( #82749 ), #2667, .T. ) ;
#9298=AXIS2_PLACEMENT_3D ( 'NONE', #38170, #79644, #39734 ) ;
#9334=CARTESIAN_POINT ( 'NONE',  ( 69.67238219402268840, 4.000000000000013323, 0.000000000000000000 ) ) ;
#9375=ORIENTED_EDGE ( 'NONE', *, *, #93605, .F. ) ;
#9381=DIRECTION ( 'NONE',  ( 0.000000000000000000, 1.000000000000000000, 0.000000000000000000 ) ) ;
#9395=EDGE_CURVE ( 'NONE', #70791, #9016, #95696, .T. ) ;
#9398=CARTESIAN_POINT ( 'NONE',  ( 55.00571552735602410, 6.975173280561618775E-15, 0.000000000000000000 ) ) ;
#9424=ORIENTED_EDGE ( 'NONE', *, *, #52022, .T. ) ;
#9479=ORIENTED_EDGE ( 'NONE', *, *, #76890, .T. ) ;
#9494=FACE_OUTER_BOUND ( 'NONE', #71118, .T. ) ;
#9513=CARTESIAN_POINT ( 'NONE',  ( 65.03872891708842019, 6.856755485862130937E-15, 0.000000000000000000 ) ) ;
#9530=CARTESIAN_POINT ( 'NONE',  ( 62.33904886068935980, 6.975173280561618775E-15, 0.000000000000000000 ) ) ;
#9533=AXIS2_PLACEMENT_3D ( 'NONE', #49299, #104363, #47186 ) ;
#9539=ORIENTED_EDGE ( 'NONE', *, *, #29584, .F. ) ;
#9550=CARTESIAN_POINT ( 'NONE',  ( 5.700000000000000178, 0.000000000000000000, 0.000000000000000000 ) ) ;
#9551=DIRECTION ( 'NONE',  ( -1.000000000000000000, -0.000000000000000000, -0.000000000000000000 ) ) ;
#9555=DIRECTION ( 'NONE',  ( 0.000000000000000000, -1.000000000000000000, 0.000000000000000000 ) ) ;
#9578=AXIS2_PLACEMENT_3D ( 'NONE', #52720, #10659, #18261 ) ;
#9579=ORIENTED_EDGE ( 'NONE', *, *, #70245, .T. ) ;
#9588=LINE ( 'NONE', #18806, #32429 ) ;
#9589=ORIENTED_EDGE ( 'NONE', *, *, #75414, .F. ) ;
#9590=CARTESIAN_POINT ( 'NONE',  ( 0.000000000000000000, 0.000000000000000000, 0.000000000000000000 ) ) ;
#9602=AXIS2_PLACEMENT_3D ( 'NONE', #7191, #56259, #8787 ) ;
#9620=CYLINDRICAL_SURFACE ( 'NONE', #34456, 4.000000000000000000 ) ;
#9694=DIRECTION ( 'NONE',  ( 0.000000000000000000, -1.000000000000000000, 0.000000000000000000 ) ) ;
#9735=LINE ( 'NONE', #90143, #7753 ) ;
#9741=EDGE_CURVE ( 'NONE', #102808, #52615, #80130, .T. ) ;
#9754=DIRECTION ( 'NONE',  ( -1.000000000000000000, -1.224606353822377258E-16, -0.000000000000000000 ) ) ;
#9757=LINE ( 'NONE', #82602, #21852 ) ;
#9864=DIRECTION ( 'NONE',  ( 1.000000000000000000, 0.000000000000000000, -0.000000000000000000 ) ) ;
#9868=DIRECTION ( 'NONE',  ( 0.000000000000000000, 1.000000000000000000, 0.000000000000000000 ) ) ;
#9910=EDGE_LOOP ( 'NONE', ( #79667, #99820, #3535, #46627, #21099 ) ) ;
#9917=CIRCLE ( 'NONE', #78740, 4.000000000000007105 ) ;
#9983=CIRCLE ( 'NONE', #96158, 4.000000000000007105 ) ;
#10011=CARTESIAN_POINT ( 'NONE',  ( 65.52222222222222570, 3.309500000000014541, 0.000000000000000000 ) ) ;
#10024=CONICAL_SURFACE ( 'NONE', #104717, 3.309500000000007880, 0.9599310885968770357 ) ;
#10052=CARTESIAN_POINT ( 'NONE',  ( 62.33904886068935980, 6.975173280561618775E-15, 0.000000000000000000 ) ) ;
#10057=ORIENTED_EDGE ( 'NONE', *, *, #82323, .T. ) ;
#10073=CONICAL_SURFACE ( 'NONE', #77453, 3.309500000000007880, 0.9599310885968770357 ) ;
#10088=EDGE_CURVE ( 'NONE', #101318, #75872, #45118, .T. ) ;
#10098=LINE ( 'NONE', #100171, #39846 ) ;
#10102=ADVANCED_FACE ( 'NONE', ( #71482, #78515 ), #37042, .T. ) ;
#10201=DIRECTION ( 'NONE',  ( -1.000000000000000000, -0.000000000000000000, -0.000000000000000000 ) ) ;
#10212=CARTESIAN_POINT ( 'NONE',  ( 58.92761780597729881, 4.000000000000015099, 4.898587196589422689E-16 ) ) ;
#10218=DIRECTION ( 'NONE',  ( 0.000000000000000000, -1.000000000000000000, 0.000000000000000000 ) ) ;
#10318=LINE ( 'NONE', #60503, #79737 ) ;
#10356=LINE ( 'NONE', #633, #41174 ) ;
#10357=DIRECTION ( 'NONE',  ( -0.5735764363510494901, -0.8191520442889894671, 0.000000000000000000 ) ) ;
#10387=DIRECTION ( 'NONE',  ( 0.000000000000000000, -0.5000000000000004441, 0.8660254037844383745 ) ) ;
#10454=CARTESIAN_POINT ( 'NONE',  ( 62.59428447264396311, 6.856755485862130937E-15, 0.000000000000000000 ) ) ;
#10460=ORIENTED_EDGE ( 'NONE', *, *, #87246, .T. ) ;
#10511=ORIENTED_EDGE ( 'NONE', *, *, #78576, .F. ) ;
#10521=DIRECTION ( 'NONE',  ( -1.000000000000000000, -1.224606353822377258E-16, -0.000000000000000000 ) ) ;
#10532=ADVANCED_FACE ( 'NONE', ( #5047 ), #69370, .T. ) ;
#10533=CIRCLE ( 'NONE', #77769, 4.000000000000007105 ) ;
#10560=EDGE_CURVE ( 'NONE', #1581, #35102, #77981, .T. ) ;
#10590=ORIENTED_EDGE ( 'NONE', *, *, #19298, .F. ) ;
#10602=CARTESIAN_POINT ( 'NONE',  ( 4.699999999999999289, -5.629165124598853431, -3.249999999999994671 ) ) ;
#10630=EDGE_CURVE ( 'NONE', #66517, #43629, #76277, .T. ) ;
#10659=DIRECTION ( 'NONE',  ( -1.000000000000000000, -1.224606353822377258E-16, -0.000000000000000000 ) ) ;
#10671=CARTESIAN_POINT ( 'NONE',  ( 4.699999999999999289, 3.752776749732553263, -6.499999999999999112 ) ) ;
#10728=AXIS2_PLACEMENT_3D ( 'NONE', #14983, #57033, #47878 ) ;
#10749=ADVANCED_FACE ( 'NONE', ( #40059 ), #23532, .T. ) ;
#10788=ORIENTED_EDGE ( 'NONE', *, *, #22711, .F. ) ;
#10795=EDGE_LOOP ( 'NONE', ( #45224, #52671, #34948, #41171, #93834 ) ) ;
#10808=ORIENTED_EDGE ( 'NONE', *, *, #11698, .F. ) ;
#10830=CARTESIAN_POINT ( 'NONE',  ( 68.45015997180047407, 6.975173280561618775E-15, 0.000000000000000000 ) ) ;
#10870=FACE_OUTER_BOUND ( 'NONE', #51454, .T. ) ;
#10891=ORIENTED_EDGE ( 'NONE', *, *, #96365, .T. ) ;
#10897=ORIENTED_EDGE ( 'NONE', *, *, #39854, .F. ) ;
#10900=DIRECTION ( 'NONE',  ( -0.5735764363510494901, -0.8191520442889894671, 0.000000000000000000 ) ) ;
#10908=CARTESIAN_POINT ( 'NONE',  ( 0.000000000000000000, 0.000000000000000000, 0.000000000000000000 ) ) ;
#10912=CIRCLE ( 'NONE', #97089, 4.000000000000007105 ) ;
#10951=FACE_OUTER_BOUND ( 'NONE', #70335, .T. ) ;
#10983=ORIENTED_EDGE ( 'NONE', *, *, #17302, .T. ) ;
#10984=AXIS2_PLACEMENT_3D ( 'NONE', #40024, #6574, #23326 ) ;
#10995=DIRECTION ( 'NONE',  ( -1.000000000000000000, -0.000000000000000000, -0.000000000000000000 ) ) ;
#11100=ORIENTED_EDGE ( 'NONE', *, *, #38488, .F. ) ;
#11136=DIRECTION ( 'NONE',  ( -1.000000000000000000, -1.224606353822377258E-16, -0.000000000000000000 ) ) ;
#11176=CARTESIAN_POINT ( 'NONE',  ( 0.000000000000000000, 0.000000000000000000, 0.000000000000000000 ) ) ;
#11251=AXIS2_PLACEMENT_3D ( 'NONE', #21693, #45422, #102582 ) ;
#11289=CONICAL_SURFACE ( 'NONE', #85388, 4.000000000000007105, 0.9599310885968835860 ) ;
#11322=AXIS2_PLACEMENT_3D ( 'NONE', #47909, #30716, #72721 ) ;
#11344=ORIENTED_EDGE ( 'NONE', *, *, #22997, .F. ) ;
#11391=CARTESIAN_POINT ( 'NONE',  ( 69.92761780597730592, -1.232595164407830946E-29, 4.000000000000007105 ) ) ;
#11406=ORIENTED_EDGE ( 'NONE', *, *, #52022, .F. ) ;
#11453=ORIENTED_EDGE ( 'NONE', *, *, #69806, .F. ) ;
#11469=EDGE_LOOP ( 'NONE', ( #13968, #31699 ) ) ;
#11483=VECTOR ( 'NONE', #82476, 1000.000000000000000 ) ;
#11520=AXIS2_PLACEMENT_3D ( 'NONE', #52718, #77001, #26378 ) ;
#11525=CARTESIAN_POINT ( 'NONE',  ( 0.000000000000000000, 4.898587196589412829E-16, -4.000000000000000000 ) ) ;
#11526=ORIENTED_EDGE ( 'NONE', *, *, #76027, .T. ) ;
#11546=DIRECTION ( 'NONE',  ( -1.000000000000000000, -1.224606353822377258E-16, -0.000000000000000000 ) ) ;
#11630=ORIENTED_EDGE ( 'NONE', *, *, #68656, .T. ) ;
#11645=CIRCLE ( 'NONE', #6480, 3.309500000000007880 ) ;
#11654=DIRECTION ( 'NONE',  ( 0.000000000000000000, -1.000000000000000000, 0.000000000000000000 ) ) ;
#11698=EDGE_CURVE ( 'NONE', #82092, #14056, #76073, .T. ) ;
#11703=CARTESIAN_POINT ( 'NONE',  ( 53.78349330513380266, 6.975173280561618775E-15, 0.000000000000000000 ) ) ;
#11715=CARTESIAN_POINT ( 'NONE',  ( 56.96666666666666856, 6.915964383211875250E-15, 0.000000000000000000 ) ) ;
#11728=ORIENTED_EDGE ( 'NONE', *, *, #31588, .F. ) ;
#11751=VERTEX_POINT ( 'NONE', #81268 ) ;
#11757=DIRECTION ( 'NONE',  ( 0.000000000000000000, 0.000000000000000000, 1.000000000000000000 ) ) ;
#11805=DIRECTION ( 'NONE',  ( 0.000000000000000000, 0.000000000000000000, 1.000000000000000000 ) ) ;
#11812=ORIENTED_EDGE ( 'NONE', *, *, #74021, .T. ) ;
#11836=ADVANCED_FACE ( 'NONE', ( #34899 ), #28587, .T. ) ;
#11851=VECTOR ( 'NONE', #43286, 1000.000000000000000 ) ;
#11866=ORIENTED_EDGE ( 'NONE', *, *, #17702, .F. ) ;
#11871=EDGE_CURVE ( 'NONE', #82654, #102372, #101721, .T. ) ;
#11899=CARTESIAN_POINT ( 'NONE',  ( 69.18888888888888289, 6.915964383211875250E-15, 0.000000000000000000 ) ) ;
#11904=DIRECTION ( 'NONE',  ( 0.5735764363510442720, -0.8191520442889930198, 1.003171929053526349E-16 ) ) ;
#11977=VERTEX_POINT ( 'NONE', #20336 ) ;
#11985=AXIS2_PLACEMENT_3D ( 'NONE', #52795, #104527, #45256 ) ;
#12021=DIRECTION ( 'NONE',  ( 0.000000000000000000, -1.000000000000000000, 0.000000000000000000 ) ) ;
#12071=CARTESIAN_POINT ( 'NONE',  ( 5.299999999999999822, 0.000000000000000000, 6.499999999999999112 ) ) ;
#12095=DIRECTION ( 'NONE',  ( -1.000000000000000000, -0.000000000000000000, -0.000000000000000000 ) ) ;
#12107=CIRCLE ( 'NONE', #86208, 4.000000000000007105 ) ;
#12126=ORIENTED_EDGE ( 'NONE', *, *, #87411, .T. ) ;
#12177=DIRECTION ( 'NONE',  ( 0.000000000000000000, -1.000000000000000000, 0.000000000000000000 ) ) ;
#12181=CIRCLE ( 'NONE', #26024, 4.000000000000007105 ) ;
#12186=ORIENTED_EDGE ( 'NONE', *, *, #53378, .F. ) ;
#12201=CARTESIAN_POINT ( 'NONE',  ( 58.67238219402268840, 6.975173280561618775E-15, 0.000000000000000000 ) ) ;
#12202=EDGE_CURVE ( 'NONE', #106205, #54493, #81146, .T. ) ;
#12217=TOROIDAL_SURFACE ( 'NONE', #55243, 4.400000000000000355, 0.4000000000000000222 ) ;
#12250=VECTOR ( 'NONE', #80506, 1000.000000000000000 ) ;
#12258=AXIS2_PLACEMENT_3D ( 'NONE', #9081, #42519, #43589 ) ;
#12306=DIRECTION ( 'NONE',  ( 0.000000000000000000, 1.000000000000000000, 0.000000000000000000 ) ) ;
#12314=EDGE_CURVE ( 'NONE', #102890, #19599, #74017, .T. ) ;
#12323=AXIS2_PLACEMENT_3D ( 'NONE', #32975, #49110, #8665 ) ;
#12341=CARTESIAN_POINT ( 'NONE',  ( 0.000000000000000000, 0.000000000000000000, 0.000000000000000000 ) ) ;
#12371=DIRECTION ( 'NONE',  ( -1.000000000000000000, -1.224606353822377258E-16, -0.000000000000000000 ) ) ;
#12412=VERTEX_POINT ( 'NONE', #84884 ) ;
#12433=VECTOR ( 'NONE', #5547, 1000.000000000000000 ) ;
#12464=ORIENTED_EDGE ( 'NONE', *, *, #89531, .F. ) ;
#12469=DIRECTION ( 'NONE',  ( 1.000000000000000000, 1.224606353822377258E-16, 0.000000000000000000 ) ) ;
#12481=DIRECTION ( 'NONE',  ( -1.000000000000000000, -1.224606353822377258E-16, -0.000000000000000000 ) ) ;
#12529=ORIENTED_EDGE ( 'NONE', *, *, #29997, .F. ) ;
#12542=CIRCLE ( 'NONE', #43527, 4.000000000000007105 ) ;
#12555=ORIENTED_EDGE ( 'NONE', *, *, #73428, .F. ) ;
#12566=DIRECTION ( 'NONE',  ( 0.000000000000000000, 0.000000000000000000, 1.000000000000000000 ) ) ;
#12572=CARTESIAN_POINT ( 'NONE',  ( 5.299999999999999822, 0.000000000000000000, -4.400000000000000355 ) ) ;
#12584=ORIENTED_EDGE ( 'NONE', *, *, #93605, .T. ) ;
#12596=ORIENTED_EDGE ( 'NONE', *, *, #74241, .T. ) ;
#12611=CARTESIAN_POINT ( 'NONE',  ( 56.22793774957824553, 4.000000000000013323, 0.000000000000000000 ) ) ;
#12623=DIRECTION ( 'NONE',  ( -1.000000000000000000, -0.000000000000000000, -0.000000000000000000 ) ) ;
#12672=EDGE_LOOP ( 'NONE', ( #71150, #67387, #68825, #73278, #79971 ) ) ;
#12701=VERTEX_POINT ( 'NONE', #79961 ) ;
#12704=CIRCLE ( 'NONE', #90240, 4.000000000000007105 ) ;
#12708=AXIS2_PLACEMENT_3D ( 'NONE', #104333, #70397, #103296 ) ;
#12715=ORIENTED_EDGE ( 'NONE', *, *, #104878, .T. ) ;
#12723=DIRECTION ( 'NONE',  ( 0.000000000000000000, -1.000000000000000000, 0.000000000000000000 ) ) ;
#12728=DIRECTION ( 'NONE',  ( -1.000000000000000000, -1.224606353822377258E-16, -0.000000000000000000 ) ) ;
#12786=ORIENTED_EDGE ( 'NONE', *, *, #69541, .F. ) ;
#12790=FACE_OUTER_BOUND ( 'NONE', #104299, .T. ) ;
#12796=ORIENTED_EDGE ( 'NONE', *, *, #30006, .F. ) ;
#12846=CARTESIAN_POINT ( 'NONE',  ( 0.5805565836007618996, 3.752776749732569250, 6.499999999999997335 ) ) ;
#12850=CARTESIAN_POINT ( 'NONE',  ( 72.85555555555556850, 6.915964383211875250E-15, 0.000000000000000000 ) ) ;
#12901=ORIENTED_EDGE ( 'NONE', *, *, #16673, .T. ) ;
#12902=VECTOR ( 'NONE', #28418, 1000.000000000000000 ) ;
#12916=DIRECTION ( 'NONE',  ( -1.000000000000000000, -1.224606353822377258E-16, -0.000000000000000000 ) ) ;
#12977=ORIENTED_EDGE ( 'NONE', *, *, #2495, .F. ) ;
#12990=AXIS2_PLACEMENT_3D ( 'NONE', #21197, #96108, #21714 ) ;
#13010=CARTESIAN_POINT ( 'NONE',  ( 0.000000000000000000, 0.000000000000000000, 0.000000000000000000 ) ) ;
#13041=DIRECTION ( 'NONE',  ( -1.000000000000000000, -0.000000000000000000, -0.000000000000000000 ) ) ;
#13056=CIRCLE ( 'NONE', #23425, 4.000000000000007105 ) ;
#13077=DIRECTION ( 'NONE',  ( -1.000000000000000000, -0.000000000000000000, -0.000000000000000000 ) ) ;
#13093=CARTESIAN_POINT ( 'NONE',  ( 5.299999999999999822, 3.752776749732553263, -6.499999999999999112 ) ) ;
#13119=EDGE_CURVE ( 'NONE', #102083, #60384, #64996, .T. ) ;
#13139=CIRCLE ( 'NONE', #44114, 4.000000000000007105 ) ;
#13145=CARTESIAN_POINT ( 'NONE',  ( 66.00571552735603120, 6.975173280561618775E-15, 0.000000000000000000 ) ) ;
#13172=CIRCLE ( 'NONE', #27009, 4.000000000000007105 ) ;
#13184=ORIENTED_EDGE ( 'NONE', *, *, #52493, .F. ) ;
#13207=DIRECTION ( 'NONE',  ( 0.000000000000000000, -1.000000000000000000, 0.000000000000000000 ) ) ;
#13210=FACE_OUTER_BOUND ( 'NONE', #53447, .T. ) ;
#13221=ADVANCED_FACE ( 'NONE', ( #1292 ), #43896, .T. ) ;
#13223=CIRCLE ( 'NONE', #82127, 4.000000000000007105 ) ;
#13225=AXIS2_PLACEMENT_3D ( 'NONE', #11703, #103907, #104434 ) ;
#13233=CARTESIAN_POINT ( 'NONE',  ( 0.000000000000000000, 0.000000000000000000, 0.000000000000000000 ) ) ;
#13264=DIRECTION ( 'NONE',  ( -1.000000000000000000, -1.224606353822377258E-16, -0.000000000000000000 ) ) ;
#13268=CARTESIAN_POINT ( 'NONE',  ( -4.878909776184771925E-16, 0.6351314446025499993, 6.500000000000000888 ) ) ;
#13303=ADVANCED_FACE ( 'NONE', ( #17670 ), #65679, .T. ) ;
#13318=CARTESIAN_POINT ( 'NONE',  ( 60.63333333333333286, 3.309500000000014541, 0.000000000000000000 ) ) ;
#13366=CYLINDRICAL_SURFACE ( 'NONE', #73530, 4.000000000000000000 ) ;
#13367=EDGE_LOOP ( 'NONE', ( #71869, #96792, #90411, #27182, #2188 ) ) ;
#13372=CARTESIAN_POINT ( 'NONE',  ( 0.000000000000000000, 5.629165124598848990, 3.250000000000002220 ) ) ;
#13374=CONICAL_SURFACE ( 'NONE', #63383, 3.309500000000007880, 0.9599310885968770357 ) ;
#13386=DIRECTION ( 'NONE',  ( 0.000000000000000000, -1.000000000000000000, 0.000000000000000000 ) ) ;
#13422=EDGE_LOOP ( 'NONE', ( #14121, #29377, #16243, #102370, #15690 ) ) ;
#13473=AXIS2_PLACEMENT_3D ( 'NONE', #2085, #18313, #44708 ) ;
#13515=VERTEX_POINT ( 'NONE', #38135 ) ;
#13529=DIRECTION ( 'NONE',  ( 0.000000000000000000, 0.000000000000000000, 1.000000000000000000 ) ) ;
#13601=DIRECTION ( 'NONE',  ( -1.000000000000000000, -1.224606353822377258E-16, -0.000000000000000000 ) ) ;
#13602=ADVANCED_FACE ( 'NONE', ( #21166 ), #16403, .T. ) ;
#13607=DIRECTION ( 'NONE',  ( 0.000000000000000000, -1.000000000000000000, 0.000000000000000000 ) ) ;
#13617=ORIENTED_EDGE ( 'NONE', *, *, #26494, .T. ) ;
#13712=DIRECTION ( 'NONE',  ( 0.000000000000000000, 1.000000000000000000, 0.000000000000000000 ) ) ;
#13714=DIRECTION ( 'NONE',  ( -0.000000000000000000, 0.000000000000000000, -1.000000000000000000 ) ) ;
#13769=ADVANCED_FACE ( 'NONE', ( #22740 ), #72832, .T. ) ;
#13851=DIRECTION ( 'NONE',  ( 0.000000000000000000, 0.000000000000000000, -1.000000000000000000 ) ) ;
#13910=ADVANCED_FACE ( 'NONE', ( #53091 ), #87101, .T. ) ;
#13924=CARTESIAN_POINT ( 'NONE',  ( 0.01372220897661389702, -5.309964801958108715, 3.802871176606130721 ) ) ;
#13928=ORIENTED_EDGE ( 'NONE', *, *, #74003, .T. ) ;
#13968=ORIENTED_EDGE ( 'NONE', *, *, #28158, .T. ) ;
#14013=DIRECTION ( 'NONE',  ( -1.000000000000000000, -1.224606353822377258E-16, -0.000000000000000000 ) ) ;
#14018=ORIENTED_EDGE ( 'NONE', *, *, #92223, .T. ) ;
#14056=VERTEX_POINT ( 'NONE', #39575 ) ;
#14067=ORIENTED_EDGE ( 'NONE', *, *, #34964, .F. ) ;
#14078=AXIS2_PLACEMENT_3D ( 'NONE', #631, #33598, #83187 ) ;
#14087=ORIENTED_EDGE ( 'NONE', *, *, #101283, .F. ) ;
#14116=ADVANCED_FACE ( 'NONE', ( #24475 ), #42346, .T. ) ;
#14121=ORIENTED_EDGE ( 'NONE', *, *, #66029, .F. ) ;
#14135=DIRECTION ( 'NONE',  ( -1.000000000000000000, -1.224606353822377258E-16, -0.000000000000000000 ) ) ;
#14137=CARTESIAN_POINT ( 'NONE',  ( 61.85555555555556140, 6.915964383211875250E-15, 0.000000000000000000 ) ) ;
#14170=EDGE_LOOP ( 'NONE', ( #319, #104568, #49693, #45411 ) ) ;
#14207=DIRECTION ( 'NONE',  ( 0.000000000000000000, 0.000000000000000000, -1.000000000000000000 ) ) ;
#14211=PRODUCT_CONTEXT ( 'NONE', #76878, 'mechanical' ) ;
#14263=EDGE_CURVE ( 'NONE', #58641, #63624, #101511, .T. ) ;
#14276=ORIENTED_EDGE ( 'NONE', *, *, #14263, .F. ) ;
#14328=DIRECTION ( 'NONE',  ( 0.5735764363510440500, 0.8191520442889932418, 0.000000000000000000 ) ) ;
#14334=AXIS2_PLACEMENT_3D ( 'NONE', #9550, #85060, #1992 ) ;
#14336=VERTEX_POINT ( 'NONE', #8772 ) ;
#14377=EDGE_LOOP ( 'NONE', ( #5710, #28242, #95556, #102634, #101034, #93924 ) ) ;
#14426=ADVANCED_FACE ( 'NONE', ( #98848 ), #88862, .T. ) ;
#14429=ORIENTED_EDGE ( 'NONE', *, *, #43854, .T. ) ;
#14441=EDGE_CURVE ( 'NONE', #90738, #4517, #99146, .T. ) ;
#14498=ORIENTED_EDGE ( 'NONE', *, *, #68757, .F. ) ;
#14506=CARTESIAN_POINT ( 'NONE',  ( 53.29999999999999716, 3.309500000000014541, 4.052968581778174646E-16 ) ) ;
#14510=FACE_OUTER_BOUND ( 'NONE', #16731, .T. ) ;
#14605=AXIS2_PLACEMENT_3D ( 'NONE', #40301, #14949, #88336 ) ;
#14652=ORIENTED_EDGE ( 'NONE', *, *, #22711, .T. ) ;
#14730=DIRECTION ( 'NONE',  ( 0.000000000000000000, 1.000000000000000000, 0.000000000000000000 ) ) ;
#14742=ADVANCED_FACE ( 'NONE', ( #74443 ), #1043, .T. ) ;
#14807=DIRECTION ( 'NONE',  ( 0.000000000000000000, -0.8660254037844375974, 0.5000000000000019984 ) ) ;
#14809=DIRECTION ( 'NONE',  ( 0.000000000000000000, -1.000000000000000000, 0.000000000000000000 ) ) ;
#14823=EDGE_CURVE ( 'NONE', #2515, #54844, #69989, .T. ) ;
#14839=CARTESIAN_POINT ( 'NONE',  ( 69.67238219402268840, -4.000000000000000000, 4.898587196589421703E-16 ) ) ;
#14907=DIRECTION ( 'NONE',  ( 0.000000000000000000, -1.000000000000000000, 0.000000000000000000 ) ) ;
#14910=CARTESIAN_POINT ( 'NONE',  ( 0.000000000000000000, 0.000000000000000000, 4.000000000000000000 ) ) ;
#14949=DIRECTION ( 'NONE',  ( -1.000000000000000000, -1.224606353822377258E-16, -0.000000000000000000 ) ) ;
#14963=CARTESIAN_POINT ( 'NONE',  ( 74.07777777777778283, -3.309500000000000774, 4.475777889183797681E-16 ) ) ;
#14981=ORIENTED_EDGE ( 'NONE', *, *, #26774, .T. ) ;
#14983=CARTESIAN_POINT ( 'NONE',  ( 0.000000000000000000, 0.000000000000000000, 0.000000000000000000 ) ) ;
#15059=AXIS2_PLACEMENT_3D ( 'NONE', #92522, #75269, #17596 ) ;
#15143=VECTOR ( 'NONE', #71174, 1000.000000000000000 ) ;
#15151=CIRCLE ( 'NONE', #66825, 4.000000000000007105 ) ;
#15165=PLANE ( 'NONE',  #26608 ) ;
#15170=LINE ( 'NONE', #64790, #22986 ) ;
#15224=EDGE_LOOP ( 'NONE', ( #53625, #7811, #2194, #44009, #35035 ) ) ;
#15233=CONICAL_SURFACE ( 'NONE', #99616, 4.000000000000007105, 0.9599310885968835860 ) ;
#15240=CYLINDRICAL_SURFACE ( 'NONE', #73095, 4.000000000000000000 ) ;
#15253=CARTESIAN_POINT ( 'NONE',  ( 70.89460441624491693, 4.000000000000014211, 0.000000000000000000 ) ) ;
#15267=ADVANCED_FACE ( 'NONE', ( #49253 ), #68311, .T. ) ;
#15274=EDGE_LOOP ( 'NONE', ( #37589, #73123, #97533, #57658, #43358, #93947 ) ) ;
#15289=ORIENTED_EDGE ( 'NONE', *, *, #16638, .F. ) ;
#15295=VERTEX_POINT ( 'NONE', #23976 ) ;
#15312=CARTESIAN_POINT ( 'NONE',  ( 62.33904886068935980, -4.000000000000000888, 4.898587196589422689E-16 ) ) ;
#15316=CIRCLE ( 'NONE', #75606, 4.000000000000007105 ) ;
#15400=DIRECTION ( 'NONE',  ( -0.5735764363510494901, -0.8191520442889894671, 0.000000000000000000 ) ) ;
#15401=CONICAL_SURFACE ( 'NONE', #24063, 4.000000000000007105, 0.9599310885968835860 ) ;
#15421=ADVANCED_FACE ( 'NONE', ( #19611 ), #35695, .T. ) ;
#15448=LINE ( 'NONE', #14910, #47196 ) ;
#15452=EDGE_CURVE ( 'NONE', #75804, #54950, #20141, .T. ) ;
#15472=ADVANCED_FACE ( 'NONE', ( #26110 ), #76993, .T. ) ;
#15497=CIRCLE ( 'NONE', #87809, 4.000000000000000000 ) ;
#15500=CIRCLE ( 'NONE', #94760, 4.000000000000007105 ) ;
#15544=DIRECTION ( 'NONE',  ( -1.000000000000000000, -1.224606353822377258E-16, -0.000000000000000000 ) ) ;
#15577=LINE ( 'NONE', #8010, #56003 ) ;
#15667=ORIENTED_EDGE ( 'NONE', *, *, #44202, .T. ) ;
#15675=AXIS2_PLACEMENT_3D ( 'NONE', #75334, #1976, #34923 ) ;
#15690=ORIENTED_EDGE ( 'NONE', *, *, #47700, .T. ) ;
#15699=CARTESIAN_POINT ( 'NONE',  ( 53.78349330513380266, 6.975173280561618775E-15, 0.000000000000000000 ) ) ;
#15711=ORIENTED_EDGE ( 'NONE', *, *, #105237, .T. ) ;
#15737=DIRECTION ( 'NONE',  ( -1.000000000000000000, -0.000000000000000000, -0.000000000000000000 ) ) ;
#15777=ORIENTED_EDGE ( 'NONE', *, *, #92646, .T. ) ;
#15823=DIRECTION ( 'NONE',  ( -1.000000000000000000, -0.000000000000000000, -0.000000000000000000 ) ) ;
#15831=DIRECTION ( 'NONE',  ( -1.000000000000000000, -1.224606353822377258E-16, -0.000000000000000000 ) ) ;
#15932=ORIENTED_EDGE ( 'NONE', *, *, #86616, .T. ) ;
#15939=AXIS2_PLACEMENT_3D ( 'NONE', #6705, #39632, #72503 ) ;
#15989=AXIS2_PLACEMENT_3D ( 'NONE', #36915, #61166, #85434 ) ;
#16006=CARTESIAN_POINT ( 'NONE',  ( 62.59428447264396311, -1.232595164407830946E-29, 4.000000000000007105 ) ) ;
#16014=CYLINDRICAL_SURFACE ( 'NONE', #61147, 4.000000000000000000 ) ;
#16017=CARTESIAN_POINT ( 'NONE',  ( 0.4033376246892499406, 7.198601258566903027, -0.5316568767328684331 ) ) ;
#16086=CIRCLE ( 'NONE', #90156, 4.000000000000000000 ) ;
#16125=DIRECTION ( 'NONE',  ( 1.000000000000000000, 1.224606353822377258E-16, 0.000000000000000000 ) ) ;
#16148=DIRECTION ( 'NONE',  ( -1.000000000000000000, -1.224606353822377258E-16, -0.000000000000000000 ) ) ;
#16153=FACE_OUTER_BOUND ( 'NONE', #72604, .T. ) ;
#16185=CARTESIAN_POINT ( 'NONE',  ( 5.700000000000000178, 0.000000000000000000, 4.000000000000000000 ) ) ;
#16199=AXIS2_PLACEMENT_3D ( 'NONE', #74281, #72691, #358 ) ;
#16228=VECTOR ( 'NONE', #47793, 1000.000000000000000 ) ;
#16243=ORIENTED_EDGE ( 'NONE', *, *, #35361, .T. ) ;
#16306=CARTESIAN_POINT ( 'NONE',  ( 4.699999999999999289, 3.752776749732553263, -6.499999999999999112 ) ) ;
#16314=CIRCLE ( 'NONE', #76590, 6.499999999999999112 ) ;
#16330=EDGE_CURVE ( 'NONE', #3167, #12701, #87970, .T. ) ;
#16359=DIRECTION ( 'NONE',  ( 1.000000000000000000, 0.000000000000000000, 0.000000000000000000 ) ) ;
#16388=CARTESIAN_POINT ( 'NONE',  ( 55.00571552735602410, 6.975173280561618775E-15, 0.000000000000000000 ) ) ;
#16403=CONICAL_SURFACE ( 'NONE', #21595, 4.000000000000007105, 0.9599310885968835860 ) ;
#16430=AXIS2_PLACEMENT_3D ( 'NONE', #3890, #44349, #37351 ) ;
#16443=ORIENTED_EDGE ( 'NONE', *, *, #7846, .F. ) ;
#16470=CARTESIAN_POINT ( 'NONE',  ( 0.1061556211655350773, 6.421950209808282573, 1.876855952934449734 ) ) ;
#16486=CARTESIAN_POINT ( 'NONE',  ( 0.000000000000000000, 0.000000000000000000, 4.000000000000000000 ) ) ;
#16606=DIRECTION ( 'NONE',  ( -1.000000000000000000, -1.224606353822377258E-16, -0.000000000000000000 ) ) ;
#16630=CARTESIAN_POINT ( 'NONE',  ( 5.299999999999999822, 3.752776749732569694, 6.499999999999997335 ) ) ;
#16638=EDGE_CURVE ( 'NONE', #47158, #20792, #85194, .T. ) ;
#16673=EDGE_CURVE ( 'NONE', #99028, #69704, #36141, .T. ) ;
#16729=CIRCLE ( 'NONE', #18521, 4.000000000000007105 ) ;
#16731=EDGE_LOOP ( 'NONE', ( #75305, #20553, #18929, #61120, #51446, #91306 ) ) ;
#16756=VERTEX_POINT ( 'NONE', #10212 ) ;
#16761=CARTESIAN_POINT ( 'NONE',  ( 64.29999999999999716, 6.915964383211875250E-15, 0.000000000000000000 ) ) ;
#16768=FACE_OUTER_BOUND ( 'NONE', #57091, .T. ) ;
#16788=DIRECTION ( 'NONE',  ( -1.000000000000000000, -1.224606353822377258E-16, -0.000000000000000000 ) ) ;
#16808=EDGE_CURVE ( 'NONE', #50186, #59786, #45878, .T. ) ;
#16849=DIRECTION ( 'NONE',  ( 0.000000000000000000, 1.000000000000000000, 0.000000000000000000 ) ) ;
#16882=CIRCLE ( 'NONE', #104705, 4.000000000000007105 ) ;
#16900=DIRECTION ( 'NONE',  ( 0.000000000000000000, -1.000000000000000000, 0.000000000000000000 ) ) ;
#16909=FACE_OUTER_BOUND ( 'NONE', #14377, .T. ) ;
#16945=ORIENTED_EDGE ( 'NONE', *, *, #67860, .T. ) ;
#16965=ORIENTED_EDGE ( 'NONE', *, *, #60292, .F. ) ;
#17044=ORIENTED_EDGE ( 'NONE', *, *, #50019, .T. ) ;
#17058=CYLINDRICAL_SURFACE ( 'NONE', #32422, 4.000000000000000000 ) ;
#17111=ORIENTED_EDGE ( 'NONE', *, *, #55288, .F. ) ;
#17114=VERTEX_POINT ( 'NONE', #91563 ) ;
#17120=DIRECTION ( 'NONE',  ( -1.000000000000000000, -0.000000000000000000, -0.000000000000000000 ) ) ;
#17178=CARTESIAN_POINT ( 'NONE',  ( 53.29999999999999716, 6.915964383211875250E-15, 0.000000000000000000 ) ) ;
#17198=ORIENTED_EDGE ( 'NONE', *, *, #96075, .F. ) ;
#17234=EDGE_CURVE ( 'NONE', #50622, #51147, #4041, .T. ) ;
#17241=ORIENTED_EDGE ( 'NONE', *, *, #79990, .T. ) ;
#17245=AXIS2_PLACEMENT_3D ( 'NONE', #102709, #61744, #21292 ) ;
#17281=CIRCLE ( 'NONE', #77550, 4.000000000000007105 ) ;
#17282=FACE_OUTER_BOUND ( 'NONE', #47614, .T. ) ;
#17302=EDGE_CURVE ( 'NONE', #17325, #82529, #96117, .T. ) ;
#17325=VERTEX_POINT ( 'NONE', #61865 ) ;
#17334=CARTESIAN_POINT ( 'NONE',  ( 0.000000000000000000, -5.629165124598853431, -3.249999999999994227 ) ) ;
#17361=CARTESIAN_POINT ( 'NONE',  ( 73.33904886068935980, 4.898587196589294500E-16, -4.000000000000007105 ) ) ;
#17376=AXIS2_PLACEMENT_3D ( 'NONE', #84247, #27112, #34671 ) ;
#17378=ORIENTED_EDGE ( 'NONE', *, *, #90686, .F. ) ;
#17416=EDGE_CURVE ( 'NONE', #39236, #2917, #103877, .T. ) ;
#17438=EDGE_LOOP ( 'NONE', ( #78120, #18827, #70788, #46253, #68382 ) ) ;
#17448=DIRECTION ( 'NONE',  ( 0.000000000000000000, 0.5000000000000004441, -0.8660254037844383745 ) ) ;
#17462=CONICAL_SURFACE ( 'NONE', #93211, 3.309500000000007880, 0.9599310885968770357 ) ;
#17486=PLANE ( 'NONE',  #3599 ) ;
#17500=EDGE_CURVE ( 'NONE', #84731, #20623, #89304, .T. ) ;
#17504=LINE ( 'NONE', #8320, #65806 ) ;
#17526=DIRECTION ( 'NONE',  ( 0.000000000000000000, -1.000000000000000000, 0.000000000000000000 ) ) ;
#17529=ORIENTED_EDGE ( 'NONE', *, *, #16638, .T. ) ;
#17531=VECTOR ( 'NONE', #78552, 1000.000000000000000 ) ;
#17582=LINE ( 'NONE', #8402, #71146 ) ;
#17596=DIRECTION ( 'NONE',  ( 0.000000000000000000, 0.000000000000000000, 1.000000000000000000 ) ) ;
#17597=CARTESIAN_POINT ( 'NONE',  ( 0.000000000000000000, 0.000000000000000000, 0.000000000000000000 ) ) ;
#17601=CARTESIAN_POINT ( 'NONE',  ( 74.56127108291157413, 6.975173280561618775E-15, 0.000000000000000000 ) ) ;
#17615=CIRCLE ( 'NONE', #41696, 4.000000000000007105 ) ;
#17650=LINE ( 'NONE', #83426, #99285 ) ;
#17655=DIRECTION ( 'NONE',  ( -1.000000000000000000, -1.224606353822377258E-16, -0.000000000000000000 ) ) ;
#17657=DIRECTION ( 'NONE',  ( 0.000000000000000000, -1.000000000000000000, 0.000000000000000000 ) ) ;
#17670=FACE_OUTER_BOUND ( 'NONE', #96617, .T. ) ;
#17671=LINE ( 'NONE', #52144, #34782 ) ;
#17675=CARTESIAN_POINT ( 'NONE',  ( 60.14984002819952025, 6.856755485862130937E-15, 0.000000000000000000 ) ) ;
#17692=DIRECTION ( 'NONE',  ( 0.000000000000000000, 0.000000000000000000, 1.000000000000000000 ) ) ;
#17702=EDGE_CURVE ( 'NONE', #59703, #66543, #105732, .T. ) ;
#17713=FACE_OUTER_BOUND ( 'NONE', #30618, .T. ) ;
#17758=DIRECTION ( 'NONE',  ( -0.5735764363510494901, -0.8191520442889894671, 0.000000000000000000 ) ) ;
#17766=EDGE_CURVE ( 'NONE', #71682, #1581, #62648, .T. ) ;
#17777=CARTESIAN_POINT ( 'NONE',  ( 61.37206225042174879, 4.898587196589294500E-16, -4.000000000000007105 ) ) ;
#17807=CIRCLE ( 'NONE', #45377, 3.309500000000007880 ) ;
#17809=CARTESIAN_POINT ( 'NONE',  ( 0.000000000000000000, 0.000000000000000000, 0.000000000000000000 ) ) ;
#17865=CARTESIAN_POINT ( 'NONE',  ( 53.78349330513380266, 6.975173280561618775E-15, 0.000000000000000000 ) ) ;
#17999=EDGE_CURVE ( 'NONE', #102083, #82654, #74779, .T. ) ;
#18027=DIRECTION ( 'NONE',  ( -1.000000000000000000, -1.224606353822377258E-16, -0.000000000000000000 ) ) ;
#18160=LINE ( 'NONE', #18707, #38522 ) ;
#18179=ORIENTED_EDGE ( 'NONE', *, *, #75852, .T. ) ;
#18188=ADVANCED_FACE ( 'NONE', ( #65154 ), #59326, .T. ) ;
#18201=AXIS2_PLACEMENT_3D ( 'NONE', #78598, #95332, #79669 ) ;
#18241=CARTESIAN_POINT ( 'NONE',  ( 0.000000000000000000, -5.629165124598853431, -3.249999999999994227 ) ) ;
#18243=CIRCLE ( 'NONE', #61356, 4.000000000000007105 ) ;
#18257=FACE_OUTER_BOUND ( 'NONE', #13367, .T. ) ;
#18261=DIRECTION ( 'NONE',  ( 0.000000000000000000, -1.000000000000000000, 0.000000000000000000 ) ) ;
#18265=DIRECTION ( 'NONE',  ( 0.000000000000000000, -1.000000000000000000, 0.000000000000000000 ) ) ;
#18274=ORIENTED_EDGE ( 'NONE', *, *, #39358, .T. ) ;
#18313=DIRECTION ( 'NONE',  ( -1.000000000000000000, -1.224606353822377258E-16, -0.000000000000000000 ) ) ;
#18338=CARTESIAN_POINT ( 'NONE',  ( 0.000000000000000000, 0.000000000000000000, 4.000000000000000000 ) ) ;
#18344=DIRECTION ( 'NONE',  ( -1.000000000000000000, -1.224606353822377258E-16, -0.000000000000000000 ) ) ;
#18385=DIRECTION ( 'NONE',  ( 0.000000000000000000, -1.000000000000000000, 0.000000000000000000 ) ) ;
#18414=EDGE_LOOP ( 'NONE', ( #77274, #41053, #104085, #73352, #12796 ) ) ;
#18415=CARTESIAN_POINT ( 'NONE',  ( 5.299999999999999822, 0.000000000000000000, 0.000000000000000000 ) ) ;
#18467=FACE_OUTER_BOUND ( 'NONE', #45649, .T. ) ;
#18521=AXIS2_PLACEMENT_3D ( 'NONE', #27064, #9754, #84728 ) ;
#18525=ORIENTED_EDGE ( 'NONE', *, *, #56843, .T. ) ;
#18559=CARTESIAN_POINT ( 'NONE',  ( 59.41111111111111143, -3.309500000000000774, 0.000000000000000000 ) ) ;
#18562=FACE_OUTER_BOUND ( 'NONE', #60689, .T. ) ;
#18575=CARTESIAN_POINT ( 'NONE',  ( 0.000000000000000000, 0.000000000000000000, 0.000000000000000000 ) ) ;
#18620=CARTESIAN_POINT ( 'NONE',  ( 67.48317336153286305, 6.856755485862130937E-15, 0.000000000000000000 ) ) ;
#18631=VECTOR ( 'NONE', #14328, 1000.000000000000000 ) ;
#18686=DIRECTION ( 'NONE',  ( -1.000000000000000000, -1.224606353822377258E-16, -0.000000000000000000 ) ) ;
#18692=CARTESIAN_POINT ( 'NONE',  ( 4.699999999999999289, 3.752776749732569694, 6.499999999999997335 ) ) ;
#18698=ORIENTED_EDGE ( 'NONE', *, *, #10560, .T. ) ;
#18707=CARTESIAN_POINT ( 'NONE',  ( 54.52222222222221859, -3.309500000000000774, 0.000000000000000000 ) ) ;
#18719=AXIS2_PLACEMENT_3D ( 'NONE', #3884, #12481, #37876 ) ;
#18722=DIRECTION ( 'NONE',  ( -1.000000000000000000, -1.224606353822377258E-16, -0.000000000000000000 ) ) ;
#18744=ORIENTED_EDGE ( 'NONE', *, *, #44473, .T. ) ;
#18769=DIRECTION ( 'NONE',  ( 0.000000000000000000, -0.5000000000000016653, -0.8660254037844375974 ) ) ;
#18791=CARTESIAN_POINT ( 'NONE',  ( 0.5805565836007648972, -7.505553499465138501, -1.190388518514737689E-16 ) ) ;
#18806=CARTESIAN_POINT ( 'NONE',  ( 74.56127108291157413, 4.000000000000014211, 0.000000000000000000 ) ) ;
#18808=LINE ( 'NONE', #85096, #56768 ) ;
#18822=VERTEX_POINT ( 'NONE', #1872 ) ;
#18827=ORIENTED_EDGE ( 'NONE', *, *, #88118, .T. ) ;
#18828=DIRECTION ( 'NONE',  ( -1.000000000000000000, -0.000000000000000000, -0.000000000000000000 ) ) ;
#18924=FACE_OUTER_BOUND ( 'NONE', #80716, .T. ) ;
#18926=EDGE_CURVE ( 'NONE', #105869, #81361, #24775, .T. ) ;
#18929=ORIENTED_EDGE ( 'NONE', *, *, #32172, .T. ) ;
#19016=ORIENTED_EDGE ( 'NONE', *, *, #33459, .F. ) ;
#19033=FACE_OUTER_BOUND ( 'NONE', #103270, .T. ) ;
#19100=AXIS2_PLACEMENT_3D ( 'NONE', #30205, #23174, #97551 ) ;
#19104=DIRECTION ( 'NONE',  ( 0.000000000000000000, -1.000000000000000000, 0.000000000000000000 ) ) ;
#19130=CARTESIAN_POINT ( 'NONE',  ( 0.000000000000000000, 0.000000000000000000, 0.000000000000000000 ) ) ;
#19185=DIRECTION ( 'NONE',  ( 0.000000000000000000, -1.000000000000000000, 0.000000000000000000 ) ) ;
#19204=EDGE_CURVE ( 'NONE', #31268, #21775, #55494, .T. ) ;
#19209=PRODUCT ( 'hex bolt gradeab_din_DIN EN 24014 - M8 x 70 x 22-S', 'hex bolt gradeab_din_DIN EN 24014 - M8 x 70 x 22-S', '', ( #14211 ) ) ;
#19218=EDGE_CURVE ( 'NONE', #1105, #98286, #66806, .T. ) ;
#19236=ORIENTED_EDGE ( 'NONE', *, *, #8594, .F. ) ;
#19251=AXIS2_PLACEMENT_3D ( 'NONE', #77347, #84908, #76271 ) ;
#19266=EDGE_CURVE ( 'NONE', #8468, #47738, #33003, .T. ) ;
#19298=EDGE_CURVE ( 'NONE', #71455, #2681, #32865, .T. ) ;
#19303=FACE_OUTER_BOUND ( 'NONE', #34166, .T. ) ;
#19330=CARTESIAN_POINT ( 'NONE',  ( 55.74444444444444713, 6.915964383211875250E-15, 0.000000000000000000 ) ) ;
#19355=CARTESIAN_POINT ( 'NONE',  ( 0.000000000000000000, 0.000000000000000000, 0.000000000000000000 ) ) ;
#19365=ORIENTED_EDGE ( 'NONE', *, *, #35280, .T. ) ;
#19370=CARTESIAN_POINT ( 'NONE',  ( 64.29999999999999716, 6.915964383211875250E-15, 0.000000000000000000 ) ) ;
#19384=ORIENTED_EDGE ( 'NONE', *, *, #76408, .F. ) ;
#19433=DIRECTION ( 'NONE',  ( -1.000000000000000000, -1.224606353822377258E-16, -0.000000000000000000 ) ) ;
#19445=CARTESIAN_POINT ( 'NONE',  ( -6.503518969018518003E-15, -5.948846446048894343, 2.696295709017757947 ) ) ;
#19463=CARTESIAN_POINT ( 'NONE',  ( 65.52222222222222570, 3.309500000000014541, 4.052968581778174646E-16 ) ) ;
#19475=LINE ( 'NONE', #96387, #16228 ) ;
#19476=CYLINDRICAL_SURFACE ( 'NONE', #3562, 4.000000000000000000 ) ;
#19492=ORIENTED_EDGE ( 'NONE', *, *, #6680, .T. ) ;
#19502=MANIFOLD_SOLID_BREP ( 'ThdSchPat', #98043 ) ;
#19511=CARTESIAN_POINT ( 'NONE',  ( 70.89460441624491693, 4.898587196589294500E-16, -4.000000000000007105 ) ) ;
#19575=CARTESIAN_POINT ( 'NONE',  ( 0.5805565836007618996, 3.752776749732569250, 6.499999999999997335 ) ) ;
#19577=CONICAL_SURFACE ( 'NONE', #76324, 4.000000000000007105, 0.9599310885968835860 ) ;
#19599=VERTEX_POINT ( 'NONE', #105018 ) ;
#19610=DIRECTION ( 'NONE',  ( 0.5735764363510442720, -0.8191520442889930198, 1.003171929053526349E-16 ) ) ;
#19611=FACE_OUTER_BOUND ( 'NONE', #62640, .T. ) ;
#19642=CARTESIAN_POINT ( 'NONE',  ( 61.37206225042174879, 6.856755485862130937E-15, 0.000000000000000000 ) ) ;
#19720=CARTESIAN_POINT ( 'NONE',  ( 72.11682663846713126, 6.975173280561618775E-15, 0.000000000000000000 ) ) ;
#19724=EDGE_CURVE ( 'NONE', #54493, #12412, #69357, .T. ) ;
#19726=ORIENTED_EDGE ( 'NONE', *, *, #93469, .F. ) ;
#19746=CARTESIAN_POINT ( 'NONE',  ( 55.74444444444444713, 3.309500000000014541, 0.000000000000000000 ) ) ;
#19753=CARTESIAN_POINT ( 'NONE',  ( 62.59428447264396311, 6.856755485862130937E-15, 0.000000000000000000 ) ) ;
#19772=ORIENTED_EDGE ( 'NONE', *, *, #103415, .T. ) ;
#19820=ORIENTED_EDGE ( 'NONE', *, *, #104594, .F. ) ;
#19836=DIRECTION ( 'NONE',  ( -1.000000000000000000, -0.000000000000000000, -0.000000000000000000 ) ) ;
#19898=DIRECTION ( 'NONE',  ( 0.000000000000000000, 0.000000000000000000, 1.000000000000000000 ) ) ;
#19924=CARTESIAN_POINT ( 'NONE',  ( 56.48317336153285595, -1.232595164407830946E-29, 4.000000000000007105 ) ) ;
#19955=DIRECTION ( 'NONE',  ( -1.000000000000000000, -0.000000000000000000, -0.000000000000000000 ) ) ;
#19967=CONICAL_SURFACE ( 'NONE', #76721, 4.000000000000007105, 0.9599310885968835860 ) ;
#20017=EDGE_CURVE ( 'NONE', #97524, #57259, #83140, .T. ) ;
#20105=AXIS2_PLACEMENT_3D ( 'NONE', #40670, #73556, #106459 ) ;
#20141=LINE ( 'NONE', #1212, #8077 ) ;
#20171=CIRCLE ( 'NONE', #6317, 4.000000000000007105 ) ;
#20194=CARTESIAN_POINT ( 'NONE',  ( 52.81650669486619165, 6.856755485862130937E-15, 0.000000000000000000 ) ) ;
#20218=CIRCLE ( 'NONE', #66658, 4.000000000000007105 ) ;
#20223=EDGE_CURVE ( 'NONE', #41303, #65608, #27076, .T. ) ;
#20224=DIRECTION ( 'NONE',  ( 0.000000000000000000, -1.000000000000000000, 0.000000000000000000 ) ) ;
#20255=CYLINDRICAL_SURFACE ( 'NONE', #76378, 4.000000000000000000 ) ;
#20266=CARTESIAN_POINT ( 'NONE',  ( 67.22793774957824553, 6.975173280561618775E-15, 0.000000000000000000 ) ) ;
#20305=CIRCLE ( 'NONE', #65043, 4.000000000000007105 ) ;
#20322=DIRECTION ( 'NONE',  ( -1.000000000000000000, -0.000000000000000000, -0.000000000000000000 ) ) ;
#20336=CARTESIAN_POINT ( 'NONE',  ( 4.699999999999999289, 1.502314598737160215E-15, -6.499999999999999112 ) ) ;
#20354=DIRECTION ( 'NONE',  ( -0.000000000000000000, 0.000000000000000000, -1.000000000000000000 ) ) ;
#20383=AXIS2_PLACEMENT_3D ( 'NONE', #17865, #50208, #66940 ) ;
#20385=AXIS2_PLACEMENT_3D ( 'NONE', #11715, #25845, #100208 ) ;
#20416=DIRECTION ( 'NONE',  ( -1.000000000000000000, -1.224606353822377258E-16, -0.000000000000000000 ) ) ;
#20421=EDGE_LOOP ( 'NONE', ( #7195, #67081, #50496, #67939, #6862 ) ) ;
#20434=CIRCLE ( 'NONE', #18719, 4.000000000000007105 ) ;
#20457=ORIENTED_EDGE ( 'NONE', *, *, #91027, .F. ) ;
#20476=ORIENTED_EDGE ( 'NONE', *, *, #44063, .T. ) ;
#20480=DIRECTION ( 'NONE',  ( -1.000000000000000000, -1.224606353822377258E-16, -0.000000000000000000 ) ) ;
#20500=CARTESIAN_POINT ( 'NONE',  ( 0.000000000000000000, 4.898587196589412829E-16, -4.000000000000000000 ) ) ;
#20501=DIRECTION ( 'NONE',  ( 0.000000000000000000, -1.000000000000000000, 0.000000000000000000 ) ) ;
#20502=ORIENTED_EDGE ( 'NONE', *, *, #71393, .T. ) ;
#20529=CIRCLE ( 'NONE', #34276, 4.000000000000007105 ) ;
#20553=ORIENTED_EDGE ( 'NONE', *, *, #4281, .T. ) ;
#20555=AXIS2_PLACEMENT_3D ( 'NONE', #41364, #99592, #90996 ) ;
#20574=VERTEX_POINT ( 'NONE', #22958 ) ;
#20577=DIRECTION ( 'NONE',  ( -1.000000000000000000, -0.000000000000000000, -0.000000000000000000 ) ) ;
#20623=VERTEX_POINT ( 'NONE', #62875 ) ;
#20627=LINE ( 'NONE', #43774, #71115 ) ;
#20643=DIRECTION ( 'NONE',  ( 0.000000000000000000, 1.000000000000000000, -2.311253228826402606E-16 ) ) ;
#20670=ORIENTED_EDGE ( 'NONE', *, *, #33068, .F. ) ;
#20751=ORIENTED_EDGE ( 'NONE', *, *, #69354, .T. ) ;
#20764=FACE_OUTER_BOUND ( 'NONE', #17438, .T. ) ;
#20770=VERTEX_POINT ( 'NONE', #12572 ) ;
#20778=EDGE_CURVE ( 'NONE', #4517, #99732, #84358, .T. ) ;
#20792=VERTEX_POINT ( 'NONE', #92972 ) ;
#20812=CIRCLE ( 'NONE', #19100, 4.000000000000007105 ) ;
#20889=DIRECTION ( 'NONE',  ( 0.000000000000000000, -1.000000000000000000, 0.000000000000000000 ) ) ;
#20916=CARTESIAN_POINT ( 'NONE',  ( 68.45015997180047407, -4.000000000000000000, 4.898587196589421703E-16 ) ) ;
#20921=EDGE_CURVE ( 'NONE', #61384, #103962, #48665, .T. ) ;
#20944=ORIENTED_EDGE ( 'NONE', *, *, #102935, .F. ) ;
#20952=CIRCLE ( 'NONE', #81172, 4.000000000000007105 ) ;
#20994=EDGE_LOOP ( 'NONE', ( #34298, #74438, #87803, #88676, #41785, #15289 ) ) ;
#21000=VERTEX_POINT ( 'NONE', #80 ) ;
#21003=CARTESIAN_POINT ( 'NONE',  ( 0.05458999538772964233, -1.264741368073340144, -6.500000000000001776 ) ) ;
#21012=DIRECTION ( 'NONE',  ( 0.000000000000000000, -1.000000000000000000, 0.000000000000000000 ) ) ;
#21013=ORIENTED_EDGE ( 'NONE', *, *, #85457, .T. ) ;
#21034=CARTESIAN_POINT ( 'NONE',  ( 54.52222222222221859, 3.309500000000014541, 4.052968581778174646E-16 ) ) ;
#21066=CYLINDRICAL_SURFACE ( 'NONE', #58017, 4.000000000000000000 ) ;
#21099=ORIENTED_EDGE ( 'NONE', *, *, #78109, .F. ) ;
#21125=VECTOR ( 'NONE', #19610, 1000.000000000000227 ) ;
#21140=CARTESIAN_POINT ( 'NONE',  ( 74.07777777777778283, 6.915964383211875250E-15, 0.000000000000000000 ) ) ;
#21166=FACE_OUTER_BOUND ( 'NONE', #21975, .T. ) ;
#21197=CARTESIAN_POINT ( 'NONE',  ( 5.299999999999999822, -7.505553499465137612, 3.546421054897781431E-16 ) ) ;
#21220=CONICAL_SURFACE ( 'NONE', #26383, 4.000000000000007105, 0.9599310885968835860 ) ;
#21246=DIRECTION ( 'NONE',  ( -1.000000000000000000, -1.224606353822377258E-16, -0.000000000000000000 ) ) ;
#21263=EDGE_CURVE ( 'NONE', #55118, #20770, #88413, .T. ) ;
#21274=ORIENTED_EDGE ( 'NONE', *, *, #81453, .F. ) ;
#21279=ADVANCED_FACE ( 'NONE', ( #58221 ), #33988, .T. ) ;
#21292=DIRECTION ( 'NONE',  ( 0.000000000000000000, 0.000000000000000000, -1.000000000000000000 ) ) ;
#21340=LINE ( 'NONE', #38062, #31674 ) ;
#21344=EDGE_CURVE ( 'NONE', #58101, #82907, #34525, .T. ) ;
#21353=LINE ( 'NONE', #30494, #42901 ) ;
#21374=DIRECTION ( 'NONE',  ( 1.000000000000000000, 0.000000000000000000, 0.000000000000000000 ) ) ;
#21387=DIRECTION ( 'NONE',  ( -1.000000000000000000, -1.224606353822377258E-16, -0.000000000000000000 ) ) ;
#21406=ADVANCED_FACE ( 'NONE', ( #63019 ), #22996, .T. ) ;
#21416=DIRECTION ( 'NONE',  ( -1.000000000000000000, -1.224606353822377258E-16, -0.000000000000000000 ) ) ;
#21458=DIRECTION ( 'NONE',  ( 0.000000000000000000, -1.000000000000000000, 0.000000000000000000 ) ) ;
#21523=CIRCLE ( 'NONE', #98920, 4.000000000000007105 ) ;
#21533=CARTESIAN_POINT ( 'NONE',  ( 0.5805565836007654523, 7.505553499465139389, 1.865978384307260116E-16 ) ) ;
#21541=CARTESIAN_POINT ( 'NONE',  ( 56.22793774957824553, 6.975173280561618775E-15, 0.000000000000000000 ) ) ;
#21577=CARTESIAN_POINT ( 'NONE',  ( 74.56127108291157413, 6.975173280561618775E-15, 0.000000000000000000 ) ) ;
#21582=DIRECTION ( 'NONE',  ( 0.000000000000000000, -1.000000000000000000, 0.000000000000000000 ) ) ;
#21588=CARTESIAN_POINT ( 'NONE',  ( 67.96666666666666856, 3.309500000000014541, 0.000000000000000000 ) ) ;
#21595=AXIS2_PLACEMENT_3D ( 'NONE', #95026, #44881, #21683 ) ;
#21605=DIRECTION ( 'NONE',  ( 0.000000000000000000, 0.000000000000000000, 1.000000000000000000 ) ) ;
#21654=CARTESIAN_POINT ( 'NONE',  ( 72.11682663846713126, 4.000000000000014211, 0.000000000000000000 ) ) ;
#21683=DIRECTION ( 'NONE',  ( 0.000000000000000000, 1.000000000000000000, 0.000000000000000000 ) ) ;
#21689=EDGE_CURVE ( 'NONE', #102866, #98734, #81520, .T. ) ;
#21693=CARTESIAN_POINT ( 'NONE',  ( 0.000000000000000000, 0.000000000000000000, 0.000000000000000000 ) ) ;
#21712=DIRECTION ( 'NONE',  ( -1.000000000000000000, -1.224606353822377258E-16, -0.000000000000000000 ) ) ;
#21714=DIRECTION ( 'NONE',  ( 0.000000000000000000, 0.5000000000000016653, 0.8660254037844375974 ) ) ;
#21720=EDGE_CURVE ( 'NONE', #66543, #69600, #53597, .T. ) ;
#21760=ORIENTED_EDGE ( 'NONE', *, *, #17702, .T. ) ;
#21775=VERTEX_POINT ( 'NONE', #78929 ) ;
#21852=VECTOR ( 'NONE', #15737, 1000.000000000000000 ) ;
#21854=EDGE_CURVE ( 'NONE', #37936, #38119, #5571, .T. ) ;
#21859=EDGE_LOOP ( 'NONE', ( #59590, #42573, #72784, #86621, #92699 ) ) ;
#21924=DIRECTION ( 'NONE',  ( 0.000000000000000000, -1.000000000000000000, 0.000000000000000000 ) ) ;
#21935=VERTEX_POINT ( 'NONE', #80740 ) ;
#21970=CARTESIAN_POINT ( 'NONE',  ( 70.89460441624491693, 6.975173280561618775E-15, 0.000000000000000000 ) ) ;
#21975=EDGE_LOOP ( 'NONE', ( #51437, #32667, #94259, #61749, #96976 ) ) ;
#21978=CARTESIAN_POINT ( 'NONE',  ( 56.96666666666666856, 6.915964383211875250E-15, 0.000000000000000000 ) ) ;
#21985=DIRECTION ( 'NONE',  ( 1.000000000000000000, 0.000000000000000000, 0.000000000000000000 ) ) ;
#22048=ADVANCED_FACE ( 'NONE', ( #33284 ), #16014, .T. ) ;
#22062=ORIENTED_EDGE ( 'NONE', *, *, #37892, .T. ) ;
#22070=DIRECTION ( 'NONE',  ( 0.000000000000000000, -1.000000000000000000, 0.000000000000000000 ) ) ;
#22102=CARTESIAN_POINT ( 'NONE',  ( 0.000000000000000000, 0.000000000000000000, 0.000000000000000000 ) ) ;
#22133=ORIENTED_EDGE ( 'NONE', *, *, #88118, .F. ) ;
#22154=ORIENTED_EDGE ( 'NONE', *, *, #22739, .F. ) ;
#22216=CIRCLE ( 'NONE', #49745, 4.000000000000007105 ) ;
#22273=ORIENTED_EDGE ( 'NONE', *, *, #21720, .T. ) ;
#22301=CARTESIAN_POINT ( 'NONE',  ( 58.18888888888888999, 6.915964383211875250E-15, 0.000000000000000000 ) ) ;
#22307=AXIS2_PLACEMENT_3D ( 'NONE', #79549, #38582, #5141 ) ;
#22331=AXIS2_PLACEMENT_3D ( 'NONE', #55947, #71619, #88361 ) ;
#22333=ORIENTED_EDGE ( 'NONE', *, *, #17766, .T. ) ;
#22363=CYLINDRICAL_SURFACE ( 'NONE', #72154, 4.000000000000000000 ) ;
#22415=DIRECTION ( 'NONE',  ( 0.000000000000000000, 0.000000000000000000, 1.000000000000000000 ) ) ;
#22438=ORIENTED_EDGE ( 'NONE', *, *, #7810, .F. ) ;
#22477=ADVANCED_FACE ( 'NONE', ( #89260 ), #57803, .T. ) ;
#22480=CIRCLE ( 'NONE', #17376, 3.309500000000007880 ) ;
#22529=DIRECTION ( 'NONE',  ( -1.000000000000000000, -1.224606353822377258E-16, -0.000000000000000000 ) ) ;
#22532=AXIS2_PLACEMENT_3D ( 'NONE', #54227, #87164, #86649 ) ;
#22536=CIRCLE ( 'NONE', #50051, 4.000000000000007105 ) ;
#22571=FACE_OUTER_BOUND ( 'NONE', #32242, .T. ) ;
#22577=AXIS2_PLACEMENT_3D ( 'NONE', #57908, #75153, #1246 ) ;
#22593=CARTESIAN_POINT ( 'NONE',  ( 72.85555555555556850, 6.915964383211875250E-15, 0.000000000000000000 ) ) ;
#22617=CARTESIAN_POINT ( 'NONE',  ( 59.41111111111111143, 6.915964383211875250E-15, 0.000000000000000000 ) ) ;
#22670=ORIENTED_EDGE ( 'NONE', *, *, #97534, .F. ) ;
#22700=ORIENTED_EDGE ( 'NONE', *, *, #79000, .F. ) ;
#22711=EDGE_CURVE ( 'NONE', #2515, #43471, #58485, .T. ) ;
#22739=EDGE_CURVE ( 'NONE', #8224, #61663, #37431, .T. ) ;
#22740=FACE_OUTER_BOUND ( 'NONE', #87414, .T. ) ;
#22764=ORIENTED_EDGE ( 'NONE', *, *, #90306, .T. ) ;
#22766=DIRECTION ( 'NONE',  ( -1.000000000000000000, -1.224606353822377258E-16, -0.000000000000000000 ) ) ;
#22780=DIRECTION ( 'NONE',  ( 0.000000000000000000, -1.000000000000000000, 0.000000000000000000 ) ) ;
#22931=VERTEX_POINT ( 'NONE', #69245 ) ;
#22958=CARTESIAN_POINT ( 'NONE',  ( 56.48317336153285595, 4.898587196589294500E-16, -4.000000000000007105 ) ) ;
#22966=ORIENTED_EDGE ( 'NONE', *, *, #71081, .F. ) ;
#22977=VERTEX_POINT ( 'NONE', #105312 ) ;
#22986=VECTOR ( 'NONE', #97671, 1000.000000000000114 ) ;
#22996=CONICAL_SURFACE ( 'NONE', #36794, 3.309500000000007880, 0.9599310885968770357 ) ;
#22997=EDGE_CURVE ( 'NONE', #76274, #97524, #37216, .T. ) ;
#23011=CIRCLE ( 'NONE', #93592, 4.000000000000007105 ) ;
#23030=DIRECTION ( 'NONE',  ( -1.000000000000000000, -1.224606353822377258E-16, -0.000000000000000000 ) ) ;
#23097=ORIENTED_EDGE ( 'NONE', *, *, #87507, .T. ) ;
#23098=DIRECTION ( 'NONE',  ( 0.000000000000000000, 0.000000000000000000, -1.000000000000000000 ) ) ;
#23104=DIRECTION ( 'NONE',  ( -1.000000000000000000, -1.224606353822377258E-16, -0.000000000000000000 ) ) ;
#23141=LINE ( 'NONE', #70079, #46531 ) ;
#23174=DIRECTION ( 'NONE',  ( -1.000000000000000000, -1.224606353822377258E-16, -0.000000000000000000 ) ) ;
#23208=AXIS2_PLACEMENT_3D ( 'NONE', #74812, #9551, #98563 ) ;
#23259=CARTESIAN_POINT ( 'NONE',  ( 0.000000000000000000, 0.000000000000000000, 0.000000000000000000 ) ) ;
#23260=EDGE_CURVE ( 'NONE', #65105, #104028, #86895, .T. ) ;
#23285=LINE ( 'NONE', #56123, #87586 ) ;
#23304=EDGE_LOOP ( 'NONE', ( #43859, #60440, #20944, #19016, #56565, #48278 ) ) ;
#23326=DIRECTION ( 'NONE',  ( 0.000000000000000000, 0.000000000000000000, 1.000000000000000000 ) ) ;
#23346=EDGE_LOOP ( 'NONE', ( #10983, #83479, #72508 ) ) ;
#23363=AXIS2_PLACEMENT_3D ( 'NONE', #12201, #76941, #92591 ) ;
#23410=ORIENTED_EDGE ( 'NONE', *, *, #35470, .F. ) ;
#23413=DIRECTION ( 'NONE',  ( -1.000000000000000000, -1.224606353822377258E-16, -0.000000000000000000 ) ) ;
#23418=CONICAL_SURFACE ( 'NONE', #90522, 3.309500000000007880, 0.9599310885968770357 ) ;
#23425=AXIS2_PLACEMENT_3D ( 'NONE', #92122, #33927, #35527 ) ;
#23441=VERTEX_POINT ( 'NONE', #93119 ) ;
#23449=ORIENTED_EDGE ( 'NONE', *, *, #87411, .F. ) ;
#23458=CARTESIAN_POINT ( 'NONE',  ( 63.56127108291158123, 6.975173280561618775E-15, 0.000000000000000000 ) ) ;
#23484=LINE ( 'NONE', #63410, #24496 ) ;
#23519=AXIS2_PLACEMENT_3D ( 'NONE', #24120, #22529, #56428 ) ;
#23524=VERTEX_POINT ( 'NONE', #34916 ) ;
#23526=AXIS2_PLACEMENT_3D ( 'NONE', #102461, #12371, #54404 ) ;
#23532=CONICAL_SURFACE ( 'NONE', #101014, 4.000000000000007105, 0.9599310885968835860 ) ;
#23567=CARTESIAN_POINT ( 'NONE',  ( 72.11682663846713126, -1.232595164407830946E-29, 4.000000000000007105 ) ) ;
#23569=DIRECTION ( 'NONE',  ( 0.000000000000000000, -1.000000000000000000, 0.000000000000000000 ) ) ;
#23592=EDGE_CURVE ( 'NONE', #57426, #105955, #17650, .T. ) ;
#23686=EDGE_CURVE ( 'NONE', #22931, #40289, #57959, .T. ) ;
#23692=DIRECTION ( 'NONE',  ( -1.000000000000000000, -1.224606353822377258E-16, -0.000000000000000000 ) ) ;
#23721=AXIS2_PLACEMENT_3D ( 'NONE', #35394, #84447, #68263 ) ;
#23723=AXIS2_PLACEMENT_3D ( 'NONE', #48480, #72754, #79798 ) ;
#23770=EDGE_CURVE ( 'NONE', #62199, #56292, #24568, .T. ) ;
#23771=AXIS2_PLACEMENT_3D ( 'NONE', #59014, #18027, #33688 ) ;
#23808=CARTESIAN_POINT ( 'NONE',  ( 66.26095113931063452, 6.856755485862130937E-15, 0.000000000000000000 ) ) ;
#23896=DIRECTION ( 'NONE',  ( -1.000000000000000000, -1.224606353822377258E-16, -0.000000000000000000 ) ) ;
#23903=EDGE_CURVE ( 'NONE', #27209, #57904, #70316, .T. ) ;
#23906=CARTESIAN_POINT ( 'NONE',  ( 0.5805565836007581249, -3.752776749732553263, 6.499999999999999112 ) ) ;
#23938=ORIENTED_EDGE ( 'NONE', *, *, #30692, .F. ) ;
#23956=DIRECTION ( 'NONE',  ( -1.000000000000000000, -1.224606353822377258E-16, -0.000000000000000000 ) ) ;
#23958=EDGE_CURVE ( 'NONE', #37118, #44950, #13223, .T. ) ;
#23976=CARTESIAN_POINT ( 'NONE',  ( 70.89460441624491693, -4.000000000000000888, 4.898587196589422689E-16 ) ) ;
#24003=ORIENTED_EDGE ( 'NONE', *, *, #73986, .T. ) ;
#24038=ORIENTED_EDGE ( 'NONE', *, *, #57748, .T. ) ;
#24063=AXIS2_PLACEMENT_3D ( 'NONE', #82712, #83760, #9868 ) ;
#24092=AXIS2_PLACEMENT_3D ( 'NONE', #97409, #73126, #23569 ) ;
#24099=CARTESIAN_POINT ( 'NONE',  ( 0.5805565836007667846, -3.752776749732578132, -6.500000000000000888 ) ) ;
#24120=CARTESIAN_POINT ( 'NONE',  ( 54.03872891708841308, 6.856755485862130937E-15, 0.000000000000000000 ) ) ;
#24163=ORIENTED_EDGE ( 'NONE', *, *, #100161, .F. ) ;
#24166=ORIENTED_EDGE ( 'NONE', *, *, #21263, .T. ) ;
#24180=AXIS2_PLACEMENT_3D ( 'NONE', #70385, #96264, #78995 ) ;
#24211=FACE_OUTER_BOUND ( 'NONE', #29233, .T. ) ;
#24264=DIRECTION ( 'NONE',  ( 1.000000000000000000, 1.224606353822377258E-16, 0.000000000000000000 ) ) ;
#24271=CARTESIAN_POINT ( 'NONE',  ( 58.92761780597729881, 4.898587196589294500E-16, -4.000000000000007105 ) ) ;
#24283=ORIENTED_EDGE ( 'NONE', *, *, #50056, .T. ) ;
#24410=CARTESIAN_POINT ( 'NONE',  ( 66.00571552735603120, -1.232595164407830946E-29, 4.000000000000007105 ) ) ;
#24475=FACE_OUTER_BOUND ( 'NONE', #33054, .T. ) ;
#24496=VECTOR ( 'NONE', #89258, 1000.000000000000000 ) ;
#24552=DIRECTION ( 'NONE',  ( 0.000000000000000000, -1.000000000000000000, 2.311253228826402606E-16 ) ) ;
#24566=ORIENTED_EDGE ( 'NONE', *, *, #68203, .T. ) ;
#24568=LINE ( 'NONE', #98416, #1029 ) ;
#24596=CARTESIAN_POINT ( 'NONE',  ( 61.37206225042174879, 4.000000000000015099, 4.898587196589422689E-16 ) ) ;
#24613=CARTESIAN_POINT ( 'NONE',  ( 73.59428447264397732, 6.856755485862130937E-15, 0.000000000000000000 ) ) ;
#24639=ORIENTED_EDGE ( 'NONE', *, *, #85366, .F. ) ;
#24665=CARTESIAN_POINT ( 'NONE',  ( 59.89460441624491693, 6.975173280561618775E-15, 0.000000000000000000 ) ) ;
#24759=ORIENTED_EDGE ( 'NONE', *, *, #56093, .T. ) ;
#24775=CIRCLE ( 'NONE', #74632, 4.000000000000007105 ) ;
#24780=CONICAL_SURFACE ( 'NONE', #33402, 3.309500000000007880, 0.9599310885968770357 ) ;
#24786=ORIENTED_EDGE ( 'NONE', *, *, #16808, .T. ) ;
#24854=( NAMED_UNIT ( * ) SI_UNIT ( $, .STERADIAN. ) SOLID_ANGLE_UNIT ( ) );
#24884=CIRCLE ( 'NONE', #42038, 3.309500000000007880 ) ;
#24959=CONICAL_SURFACE ( 'NONE', #105841, 3.309500000000007880, 0.9599310885968770357 ) ;
#24968=ADVANCED_FACE ( 'NONE', ( #17282 ), #87229, .T. ) ;
#24974=ORIENTED_EDGE ( 'NONE', *, *, #103415, .F. ) ;
#24996=DIRECTION ( 'NONE',  ( 0.000000000000000000, -1.000000000000000000, 0.000000000000000000 ) ) ;
#25049=CARTESIAN_POINT ( 'NONE',  ( 70.89460441624491693, 6.975173280561618775E-15, 0.000000000000000000 ) ) ;
#25059=FACE_OUTER_BOUND ( 'NONE', #79029, .T. ) ;
#25068=ADVANCED_FACE ( 'NONE', ( #90257 ), #100994, .T. ) ;
#25108=ORIENTED_EDGE ( 'NONE', *, *, #70750, .T. ) ;
#25114=DIRECTION ( 'NONE',  ( -1.000000000000000000, -1.224606353822377258E-16, -0.000000000000000000 ) ) ;
#25241=AXIS2_PLACEMENT_3D ( 'NONE', #19642, #2327, #3944 ) ;
#25266=CIRCLE ( 'NONE', #40777, 4.000000000000007105 ) ;
#25362=CARTESIAN_POINT ( 'NONE',  ( 5.299999999999999822, 0.000000000000000000, 0.000000000000000000 ) ) ;
#25365=CIRCLE ( 'NONE', #39138, 4.000000000000007105 ) ;
#25455=CARTESIAN_POINT ( 'NONE',  ( 74.56127108291157413, 4.898587196589294500E-16, -4.000000000000007105 ) ) ;
#25490=ORIENTED_EDGE ( 'NONE', *, *, #56013, .F. ) ;
#25508=DIRECTION ( 'NONE',  ( 1.000000000000000000, 1.224606353822377258E-16, 0.000000000000000000 ) ) ;
#25546=CIRCLE ( 'NONE', #87572, 3.309500000000007880 ) ;
#25551=CYLINDRICAL_SURFACE ( 'NONE', #1525, 4.000000000000000000 ) ;
#25562=AXIS2_PLACEMENT_3D ( 'NONE', #60764, #86641, #101205 ) ;
#25576=ORIENTED_EDGE ( 'NONE', *, *, #54281, .T. ) ;
#25583=FACE_OUTER_BOUND ( 'NONE', #91922, .T. ) ;
#25597=ORIENTED_EDGE ( 'NONE', *, *, #51259, .T. ) ;
#25607=DIRECTION ( 'NONE',  ( 0.000000000000000000, -1.000000000000000000, 0.000000000000000000 ) ) ;
#25638=ORIENTED_EDGE ( 'NONE', *, *, #33068, .T. ) ;
#25645=DIRECTION ( 'NONE',  ( -1.000000000000000000, -1.224606353822377258E-16, -0.000000000000000000 ) ) ;
#25660=EDGE_CURVE ( 'NONE', #96955, #23524, #25266, .T. ) ;
#25716=AXIS2_PLACEMENT_3D ( 'NONE', #89561, #57173, #65810 ) ;
#25733=DIRECTION ( 'NONE',  ( -1.000000000000000000, -1.224606353822377258E-16, -0.000000000000000000 ) ) ;
#25774=AXIS2_PLACEMENT_3D ( 'NONE', #89479, #90532, #41446 ) ;
#25775=VERTEX_POINT ( 'NONE', #87358 ) ;
#25789=FACE_OUTER_BOUND ( 'NONE', #14170, .T. ) ;
#25843=VERTEX_POINT ( 'NONE', #55479 ) ;
#25845=DIRECTION ( 'NONE',  ( -1.000000000000000000, -1.224606353822377258E-16, -0.000000000000000000 ) ) ;
#25850=EDGE_CURVE ( 'NONE', #6296, #106169, #20218, .T. ) ;
#25878=FACE_OUTER_BOUND ( 'NONE', #20994, .T. ) ;
#25904=DIRECTION ( 'NONE',  ( 0.000000000000000000, -1.000000000000000000, 0.000000000000000000 ) ) ;
#25923=ADVANCED_FACE ( 'NONE', ( #94930 ), #21066, .T. ) ;
#26024=AXIS2_PLACEMENT_3D ( 'NONE', #94740, #86653, #12723 ) ;
#26045=CARTESIAN_POINT ( 'NONE',  ( 0.05613245601036522675, 1.278525034529249149, -6.499999999999999112 ) ) ;
#26070=ORIENTED_EDGE ( 'NONE', *, *, #65638, .F. ) ;
#26110=FACE_OUTER_BOUND ( 'NONE', #67934, .T. ) ;
#26124=CONICAL_SURFACE ( 'NONE', #86395, 3.309500000000007880, 0.9599310885968770357 ) ;
#26138=DIRECTION ( 'NONE',  ( -1.000000000000000000, -1.224606353822377258E-16, -0.000000000000000000 ) ) ;
#26140=LINE ( 'NONE', #33143, #63089 ) ;
#26173=ADVANCED_FACE ( 'NONE', ( #60317 ), #6359, .T. ) ;
#26174=CARTESIAN_POINT ( 'NONE',  ( 65.03872891708842019, -1.232595164407830946E-29, 4.000000000000007105 ) ) ;
#26196=CARTESIAN_POINT ( 'NONE',  ( 0.000000000000000000, 0.000000000000000000, 4.000000000000000000 ) ) ;
#26200=ORIENTED_EDGE ( 'NONE', *, *, #99487, .F. ) ;
#26211=CARTESIAN_POINT ( 'NONE',  ( 70.41111111111112564, 6.915964383211875250E-15, 0.000000000000000000 ) ) ;
#26239=VECTOR ( 'NONE', #10357, 1000.000000000000000 ) ;
#26324=ORIENTED_EDGE ( 'NONE', *, *, #42428, .T. ) ;
#26337=ADVANCED_FACE ( 'NONE', ( #48334 ), #3070, .T. ) ;
#26356=DIRECTION ( 'NONE',  ( -1.000000000000000000, -0.000000000000000000, -0.000000000000000000 ) ) ;
#26369=CARTESIAN_POINT ( 'NONE',  ( 72.11682663846713126, 6.975173280561618775E-15, 0.000000000000000000 ) ) ;
#26378=DIRECTION ( 'NONE',  ( 0.000000000000000000, -1.000000000000000000, 0.000000000000000000 ) ) ;
#26383=AXIS2_PLACEMENT_3D ( 'NONE', #98115, #24264, #31806 ) ;
#26388=ORIENTED_EDGE ( 'NONE', *, *, #9741, .T. ) ;
#26403=DIRECTION ( 'NONE',  ( 0.000000000000000000, -1.000000000000000000, 0.000000000000000000 ) ) ;
#26422=ADVANCED_FACE ( 'NONE', ( #51532 ), #54699, .T. ) ;
#26427=CARTESIAN_POINT ( 'NONE',  ( 58.92761780597729881, -4.000000000000000000, 0.000000000000000000 ) ) ;
#26452=EDGE_CURVE ( 'NONE', #38217, #104028, #32343, .T. ) ;
#26494=EDGE_CURVE ( 'NONE', #17325, #31918, #66745, .T. ) ;
#26511=VERTEX_POINT ( 'NONE', #6159 ) ;
#26515=CIRCLE ( 'NONE', #47174, 4.000000000000007105 ) ;
#26526=ORIENTED_EDGE ( 'NONE', *, *, #38528, .T. ) ;
#26564=CARTESIAN_POINT ( 'NONE',  ( 0.2595206531158502639, 2.531175536751796962, -6.499999999999999112 ) ) ;
#26569=CARTESIAN_POINT ( 'NONE',  ( -1.997303689625640200E-15, 5.309483803148800973, 3.803704290982250491 ) ) ;
#26582=DIRECTION ( 'NONE',  ( 0.000000000000000000, -1.000000000000000000, 0.000000000000000000 ) ) ;
#26608=AXIS2_PLACEMENT_3D ( 'NONE', #48051, #72856, #31906 ) ;
#26665=CARTESIAN_POINT ( 'NONE',  ( 70.41111111111112564, 6.915964383211875250E-15, 0.000000000000000000 ) ) ;
#26677=VERTEX_POINT ( 'NONE', #9334 ) ;
#26718=ORIENTED_EDGE ( 'NONE', *, *, #103403, .T. ) ;
#26748=AXIS2_PLACEMENT_3D ( 'NONE', #53198, #54225, #20354 ) ;
#26774=EDGE_CURVE ( 'NONE', #99463, #72747, #9983, .T. ) ;
#26917=DIRECTION ( 'NONE',  ( 0.5735764363510440500, 0.8191520442889932418, 0.000000000000000000 ) ) ;
#26933=ORIENTED_EDGE ( 'NONE', *, *, #65772, .F. ) ;
#26968=AXIS2_PLACEMENT_3D ( 'NONE', #19330, #51626, #100705 ) ;
#26974=DIRECTION ( 'NONE',  ( 0.000000000000000000, -1.000000000000000000, 0.000000000000000000 ) ) ;
#26983=CARTESIAN_POINT ( 'NONE',  ( 59.41111111111111143, 6.915964383211875250E-15, 0.000000000000000000 ) ) ;
#27009=AXIS2_PLACEMENT_3D ( 'NONE', #91491, #25733, #50467 ) ;
#27012=CARTESIAN_POINT ( 'NONE',  ( 59.89460441624491693, 6.975173280561618775E-15, 0.000000000000000000 ) ) ;
#27023=DIRECTION ( 'NONE',  ( 0.000000000000000000, -2.311253228826400140E-16, 1.000000000000000000 ) ) ;
#27037=ORIENTED_EDGE ( 'NONE', *, *, #64124, .F. ) ;
#27039=CARTESIAN_POINT ( 'NONE',  ( 71.63333333333333997, 6.915964383211875250E-15, 0.000000000000000000 ) ) ;
#27063=ADVANCED_FACE ( 'NONE', ( #28505 ), #93744, .T. ) ;
#27064=CARTESIAN_POINT ( 'NONE',  ( 57.70539558375507738, 6.856755485862130937E-15, 0.000000000000000000 ) ) ;
#27072=AXIS2_PLACEMENT_3D ( 'NONE', #1759, #27696, #42228 ) ;
#27076=LINE ( 'NONE', #67501, #74450 ) ;
#27111=ADVANCED_FACE ( 'NONE', ( #69473 ), #78082, .T. ) ;
#27112=DIRECTION ( 'NONE',  ( -1.000000000000000000, -1.224606353822377258E-16, -0.000000000000000000 ) ) ;
#27182=ORIENTED_EDGE ( 'NONE', *, *, #2521, .F. ) ;
#27209=VERTEX_POINT ( 'NONE', #51672 ) ;
#27214=DIRECTION ( 'NONE',  ( 1.000000000000000000, 1.224606353822377258E-16, 0.000000000000000000 ) ) ;
#27217=CARTESIAN_POINT ( 'NONE',  ( 52.81650669486619165, 6.856755485862130937E-15, 0.000000000000000000 ) ) ;
#27287=VECTOR ( 'NONE', #67871, 1000.000000000000000 ) ;
#27311=CIRCLE ( 'NONE', #6528, 3.309500000000007880 ) ;
#27392=DIRECTION ( 'NONE',  ( -1.000000000000000000, -0.000000000000000000, -0.000000000000000000 ) ) ;
#27402=VECTOR ( 'NONE', #30929, 1000.000000000000227 ) ;
#27404=CIRCLE ( 'NONE', #87642, 4.000000000000007105 ) ;
#27418=EDGE_CURVE ( 'NONE', #45176, #54829, #82434, .T. ) ;
#27437=DIRECTION ( 'NONE',  ( -1.000000000000000000, -0.000000000000000000, -0.000000000000000000 ) ) ;
#27464=ADVANCED_FACE ( 'NONE', ( #69878 ), #78969, .T. ) ;
#27509=ADVANCED_FACE ( 'NONE', ( #25059 ), #70361, .T. ) ;
#27511=LINE ( 'NONE', #20500, #99484 ) ;
#27512=DIRECTION ( 'NONE',  ( -1.000000000000000000, -1.224606353822377258E-16, -0.000000000000000000 ) ) ;
#27523=ORIENTED_EDGE ( 'NONE', *, *, #14441, .F. ) ;
#27535=CIRCLE ( 'NONE', #99857, 4.000000000000007105 ) ;
#27552=CARTESIAN_POINT ( 'NONE',  ( 4.699999999999999289, 0.000000000000000000, 6.499999999999999112 ) ) ;
#27585=DIRECTION ( 'NONE',  ( 0.000000000000000000, 0.000000000000000000, 1.000000000000000000 ) ) ;
#27635=ORIENTED_EDGE ( 'NONE', *, *, #48127, .T. ) ;
#27660=CARTESIAN_POINT ( 'NONE',  ( 57.70539558375507738, 4.898587196589294500E-16, -4.000000000000007105 ) ) ;
#27690=CARTESIAN_POINT ( 'NONE',  ( 68.45015997180047407, 6.975173280561618775E-15, 0.000000000000000000 ) ) ;
#27696=DIRECTION ( 'NONE',  ( -1.000000000000000000, -1.224606353822377258E-16, -0.000000000000000000 ) ) ;
#27714=ADVANCED_FACE ( 'NONE', ( #10951 ), #76588, .T. ) ;
#27769=CONICAL_SURFACE ( 'NONE', #67376, 4.000000000000007105, 0.9599310885968835860 ) ;
#27813=LINE ( 'NONE', #35356, #47035 ) ;
#27849=CARTESIAN_POINT ( 'NONE',  ( 53.78349330513380266, 6.975173280561618775E-15, 0.000000000000000000 ) ) ;
#27930=DIRECTION ( 'NONE',  ( -1.000000000000000000, -0.000000000000000000, -0.000000000000000000 ) ) ;
#27955=CARTESIAN_POINT ( 'NONE',  ( 75.30000000000001137, 0.000000000000000000, 0.000000000000000000 ) ) ;
#27957=CARTESIAN_POINT ( 'NONE',  ( 57.70539558375507738, -1.232595164407830946E-29, 4.000000000000007105 ) ) ;
#27985=DIRECTION ( 'NONE',  ( 1.000000000000000000, 1.224606353822377258E-16, 0.000000000000000000 ) ) ;
#28084=CARTESIAN_POINT ( 'NONE',  ( 58.18888888888888999, 3.309500000000014541, 0.000000000000000000 ) ) ;
#28088=CARTESIAN_POINT ( 'NONE',  ( 71.14984002819953446, 4.898587196589294500E-16, -4.000000000000007105 ) ) ;
#28091=ORIENTED_EDGE ( 'NONE', *, *, #69975, .F. ) ;
#28103=EDGE_CURVE ( 'NONE', #13515, #61663, #66208, .T. ) ;
#28131=CARTESIAN_POINT ( 'NONE',  ( 73.33904886068935980, 4.000000000000013323, 0.000000000000000000 ) ) ;
#28158=EDGE_CURVE ( 'NONE', #103960, #59016, #74817, .T. ) ;
#28159=CONICAL_SURFACE ( 'NONE', #96951, 4.000000000000007105, 0.9599310885968835860 ) ;
#28181=DIRECTION ( 'NONE',  ( 0.000000000000000000, 1.000000000000000000, 0.000000000000000000 ) ) ;
#28190=CARTESIAN_POINT ( 'NONE',  ( 58.18888888888888999, -3.309500000000000774, 0.000000000000000000 ) ) ;
#28198=DIRECTION ( 'NONE',  ( -0.5735764363510497121, 0.8191520442889892450, 1.003171929053521665E-16 ) ) ;
#28218=DIRECTION ( 'NONE',  ( 0.000000000000000000, -1.000000000000000000, 0.000000000000000000 ) ) ;
#28242=ORIENTED_EDGE ( 'NONE', *, *, #3704, .T. ) ;
#28252=ORIENTED_EDGE ( 'NONE', *, *, #104265, .F. ) ;
#28269=AXIS2_PLACEMENT_3D ( 'NONE', #36802, #94488, #20643 ) ;
#28292=CARTESIAN_POINT ( 'NONE',  ( 66.26095113931063452, 6.856755485862130937E-15, 0.000000000000000000 ) ) ;
#28304=FACE_OUTER_BOUND ( 'NONE', #74034, .T. ) ;
#28324=AXIS2_PLACEMENT_3D ( 'NONE', #62006, #45277, #71642 ) ;
#28335=ORIENTED_EDGE ( 'NONE', *, *, #73401, .F. ) ;
#28410=DIRECTION ( 'NONE',  ( -1.000000000000000000, -1.224606353822377258E-16, -0.000000000000000000 ) ) ;
#28418=DIRECTION ( 'NONE',  ( -0.5735764363510494901, -0.8191520442889894671, 0.000000000000000000 ) ) ;
#28438=EDGE_CURVE ( 'NONE', #61663, #15295, #13172, .T. ) ;
#28466=CARTESIAN_POINT ( 'NONE',  ( 55.74444444444444713, 3.309500000000014541, 4.052968581778174646E-16 ) ) ;
#28482=CIRCLE ( 'NONE', #73146, 4.000000000000007105 ) ;
#28505=FACE_OUTER_BOUND ( 'NONE', #52864, .T. ) ;
#28520=EDGE_LOOP ( 'NONE', ( #26718, #82678, #43626, #53902, #44313, #28252 ) ) ;
#28523=AXIS2_PLACEMENT_3D ( 'NONE', #100205, #92108, #51111 ) ;
#28542=ORIENTED_EDGE ( 'NONE', *, *, #75093, .F. ) ;
#28558=ORIENTED_EDGE ( 'NONE', *, *, #69083, .F. ) ;
#28578=CARTESIAN_POINT ( 'NONE',  ( 0.000000000000000000, -5.629165124598843661, 3.250000000000011990 ) ) ;
#28587=CONICAL_SURFACE ( 'NONE', #68118, 4.000000000000007105, 0.9599310885968835860 ) ;
#28622=CARTESIAN_POINT ( 'NONE',  ( 52.81650669486619165, 6.856755485862130937E-15, 0.000000000000000000 ) ) ;
#28634=EDGE_CURVE ( 'NONE', #5888, #77883, #95817, .T. ) ;
#28691=AXIS2_PLACEMENT_3D ( 'NONE', #103515, #77660, #69571 ) ;
#28791=VERTEX_POINT ( 'NONE', #47690 ) ;
#28795=CARTESIAN_POINT ( 'NONE',  ( 75.30000000000001137, 0.000000000000000000, 3.309499999999999886 ) ) ;
#28817=DIRECTION ( 'NONE',  ( 0.000000000000000000, -1.000000000000000000, 0.000000000000000000 ) ) ;
#28848=CARTESIAN_POINT ( 'NONE',  ( 53.78349330513380266, 4.898587196589294500E-16, -4.000000000000007105 ) ) ;
#28865=EDGE_CURVE ( 'NONE', #34382, #87882, #72507, .T. ) ;
#28880=DIRECTION ( 'NONE',  ( 0.000000000000000000, 1.000000000000000000, 0.000000000000000000 ) ) ;
#28882=FACE_OUTER_BOUND ( 'NONE', #39938, .T. ) ;
#28937=EDGE_CURVE ( 'NONE', #15295, #28791, #99325, .T. ) ;
#28966=ORIENTED_EDGE ( 'NONE', *, *, #2395, .T. ) ;
#28995=ORIENTED_EDGE ( 'NONE', *, *, #56093, .F. ) ;
#28998=CARTESIAN_POINT ( 'NONE',  ( 0.5805565836007618996, 3.752776749732569250, 6.499999999999997335 ) ) ;
#29020=CIRCLE ( 'NONE', #44519, 3.309500000000007880 ) ;
#29021=DIRECTION ( 'NONE',  ( -0.5735764363510497121, 0.8191520442889892450, 1.003171929053521665E-16 ) ) ;
#29023=DIRECTION ( 'NONE',  ( -1.000000000000000000, -1.224606353822377258E-16, -0.000000000000000000 ) ) ;
#29025=AXIS2_PLACEMENT_3D ( 'NONE', #13233, #21374, #5165 ) ;
#29059=ORIENTED_EDGE ( 'NONE', *, *, #79102, .F. ) ;
#29080=EDGE_CURVE ( 'NONE', #33265, #37041, #20171, .T. ) ;
#29081=CARTESIAN_POINT ( 'NONE',  ( 74.60950000000003968, 0.000000000000000000, 0.000000000000000000 ) ) ;
#29150=DIRECTION ( 'NONE',  ( -1.000000000000000000, -0.000000000000000000, -0.000000000000000000 ) ) ;
#29151=ORIENTED_EDGE ( 'NONE', *, *, #58479, .F. ) ;
#29233=EDGE_LOOP ( 'NONE', ( #49849, #88941, #33384, #3174, #47527, #45622 ) ) ;
#29239=LINE ( 'NONE', #48006, #38097 ) ;
#29327=DIRECTION ( 'NONE',  ( 0.000000000000000000, 1.000000000000000000, 0.000000000000000000 ) ) ;
#29354=VERTEX_POINT ( 'NONE', #8702 ) ;
#29377=ORIENTED_EDGE ( 'NONE', *, *, #23686, .F. ) ;
#29404=DIRECTION ( 'NONE',  ( -1.000000000000000000, -1.224606353822377258E-16, -0.000000000000000000 ) ) ;
#29427=DIRECTION ( 'NONE',  ( 0.5735764363510442720, -0.8191520442889930198, 1.003171929053526349E-16 ) ) ;
#29442=DIRECTION ( 'NONE',  ( -1.000000000000000000, -1.224606353822377258E-16, -0.000000000000000000 ) ) ;
#29448=ORIENTED_EDGE ( 'NONE', *, *, #50201, .F. ) ;
#29454=FACE_OUTER_BOUND ( 'NONE', #10795, .T. ) ;
#29467=EDGE_CURVE ( 'NONE', #32062, #7306, #16729, .T. ) ;
#29481=CARTESIAN_POINT ( 'NONE',  ( 4.699999999999999289, 6.499999999999999112, 0.000000000000000000 ) ) ;
#29510=DIRECTION ( 'NONE',  ( 0.000000000000000000, -1.000000000000000000, 0.000000000000000000 ) ) ;
#29566=ORIENTED_EDGE ( 'NONE', *, *, #70750, .F. ) ;
#29584=EDGE_CURVE ( 'NONE', #12412, #53703, #96543, .T. ) ;
#29594=ORIENTED_EDGE ( 'NONE', *, *, #36377, .F. ) ;
#29622=CIRCLE ( 'NONE', #55432, 4.000000000000007105 ) ;
#29626=CARTESIAN_POINT ( 'NONE',  ( 69.18888888888888289, -3.309500000000000774, 4.475777889183797681E-16 ) ) ;
#29656=DIRECTION ( 'NONE',  ( 0.5735764363510440500, 0.8191520442889932418, 0.000000000000000000 ) ) ;
#29675=CARTESIAN_POINT ( 'NONE',  ( 0.2573354458087865893, -4.368923434677202344, -5.432802636760777126 ) ) ;
#29765=DIRECTION ( 'NONE',  ( -0.5735764363510497121, 0.8191520442889892450, 1.003171929053521665E-16 ) ) ;
#29768=AXIS2_PLACEMENT_3D ( 'NONE', #22617, #63044, #22070 ) ;
#29773=CARTESIAN_POINT ( 'NONE',  ( 73.33904886068935980, 6.975173280561618775E-15, 0.000000000000000000 ) ) ;
#29788=CYLINDRICAL_SURFACE ( 'NONE', #11251, 4.000000000000000000 ) ;
#29810=AXIS2_PLACEMENT_3D ( 'NONE', #71889, #48134, #30943 ) ;
#29863=LINE ( 'NONE', #104237, #82717 ) ;
#29904=DIRECTION ( 'NONE',  ( -1.000000000000000000, -1.224606353822377258E-16, -0.000000000000000000 ) ) ;
#29997=EDGE_CURVE ( 'NONE', #97524, #76274, #32387, .T. ) ;
#30002=CARTESIAN_POINT ( 'NONE',  ( 74.07777777777778283, -3.309500000000000774, 0.000000000000000000 ) ) ;
#30006=EDGE_CURVE ( 'NONE', #105730, #8358, #74640, .T. ) ;
#30012=LINE ( 'NONE', #88753, #70822 ) ;
#30029=CARTESIAN_POINT ( 'NONE',  ( 67.22793774957824553, 4.000000000000014211, 0.000000000000000000 ) ) ;
#30054=CONICAL_SURFACE ( 'NONE', #9298, 3.309500000000007880, 0.9599310885968770357 ) ;
#30123=CARTESIAN_POINT ( 'NONE',  ( 0.000000000000000000, 0.000000000000000000, 0.000000000000000000 ) ) ;
#30128=AXIS2_PLACEMENT_3D ( 'NONE', #90679, #16788, #49675 ) ;
#30131=AXIS2_PLACEMENT_3D ( 'NONE', #26665, #92412, #43871 ) ;
#30171=CARTESIAN_POINT ( 'NONE',  ( 53.78349330513380266, -4.000000000000000000, 4.898587196589421703E-16 ) ) ;
#30195=AXIS2_PLACEMENT_3D ( 'NONE', #44514, #86586, #59639 ) ;
#30205=CARTESIAN_POINT ( 'NONE',  ( 52.81650669486619165, 6.856755485862130937E-15, 0.000000000000000000 ) ) ;
#30314=DIRECTION ( 'NONE',  ( -1.000000000000000000, -1.224606353822377258E-16, -0.000000000000000000 ) ) ;
#30360=LINE ( 'NONE', #103696, #240 ) ;
#30374=CARTESIAN_POINT ( 'NONE',  ( 56.22793774957824553, 6.975173280561618775E-15, 0.000000000000000000 ) ) ;
#30480=ORIENTED_EDGE ( 'NONE', *, *, #19724, .F. ) ;
#30494=CARTESIAN_POINT ( 'NONE',  ( 71.63333333333333997, -3.309500000000000774, 0.000000000000000000 ) ) ;
#30595=ADVANCED_FACE ( 'NONE', ( #16153 ), #10024, .T. ) ;
#30604=VECTOR ( 'NONE', #82759, 1000.000000000000227 ) ;
#30618=EDGE_LOOP ( 'NONE', ( #41564, #19492, #39620, #68513, #64813, #4732 ) ) ;
#30621=( NAMED_UNIT ( * ) SI_UNIT ( $, .STERADIAN. ) SOLID_ANGLE_UNIT ( ) );
#30655=ORIENTED_EDGE ( 'NONE', *, *, #21344, .F. ) ;
#30664=CARTESIAN_POINT ( 'NONE',  ( 0.000000000000000000, 0.000000000000000000, 0.000000000000000000 ) ) ;
#30665=ORIENTED_EDGE ( 'NONE', *, *, #58880, .T. ) ;
#30692=EDGE_CURVE ( 'NONE', #69600, #86973, #56512, .T. ) ;
#30697=ADVANCED_FACE ( 'NONE', ( #67382 ), #36115, .T. ) ;
#30710=VECTOR ( 'NONE', #17758, 1000.000000000000000 ) ;
#30716=DIRECTION ( 'NONE',  ( -1.000000000000000000, -1.224606353822377258E-16, -0.000000000000000000 ) ) ;
#30719=EDGE_CURVE ( 'NONE', #99128, #83726, #39306, .T. ) ;
#30721=VERTEX_POINT ( 'NONE', #26427 ) ;
#30745=VERTEX_POINT ( 'NONE', #61425 ) ;
#30792=VERTEX_POINT ( 'NONE', #46812 ) ;
#30802=VECTOR ( 'NONE', #81776, 1000.000000000000000 ) ;
#30810=LINE ( 'NONE', #21654, #86099 ) ;
#30822=CIRCLE ( 'NONE', #46343, 6.499999999999999112 ) ;
#30835=EDGE_CURVE ( 'NONE', #94772, #3167, #25546, .T. ) ;
#30897=ORIENTED_EDGE ( 'NONE', *, *, #103365, .T. ) ;
#30924=DIRECTION ( 'NONE',  ( -1.000000000000000000, -0.000000000000000000, -0.000000000000000000 ) ) ;
#30929=DIRECTION ( 'NONE',  ( 0.5735764363510442720, -0.8191520442889930198, 1.003171929053526349E-16 ) ) ;
#30936=FACE_OUTER_BOUND ( 'NONE', #37770, .T. ) ;
#30943=DIRECTION ( 'NONE',  ( 0.000000000000000000, -1.000000000000000000, 0.000000000000000000 ) ) ;
#30958=CIRCLE ( 'NONE', #22331, 3.309500000000007880 ) ;
#30984=CARTESIAN_POINT ( 'NONE',  ( 0.000000000000000000, 0.000000000000000000, 0.000000000000000000 ) ) ;
#31010=LINE ( 'NONE', #47144, #95637 ) ;
#31029=LINE ( 'NONE', #81636, #56098 ) ;
#31048=CARTESIAN_POINT ( 'NONE',  ( 54.03872891708841308, 6.856755485862130937E-15, 0.000000000000000000 ) ) ;
#31086=ORIENTED_EDGE ( 'NONE', *, *, #78702, .T. ) ;
#31106=CARTESIAN_POINT ( 'NONE',  ( 75.30000000000001137, 0.000000000000000000, 3.309499999999999886 ) ) ;
#31147=DIRECTION ( 'NONE',  ( -1.000000000000000000, -0.000000000000000000, -0.000000000000000000 ) ) ;
#31232=ORIENTED_EDGE ( 'NONE', *, *, #68203, .F. ) ;
#31254=CARTESIAN_POINT ( 'NONE',  ( 75.30000000000001137, 0.000000000000000000, 0.000000000000000000 ) ) ;
#31261=ORIENTED_EDGE ( 'NONE', *, *, #72290, .F. ) ;
#31268=VERTEX_POINT ( 'NONE', #106304 ) ;
#31345=FACE_OUTER_BOUND ( 'NONE', #82559, .T. ) ;
#31412=AXIS2_PLACEMENT_3D ( 'NONE', #19130, #86505, #12566 ) ;
#31464=CARTESIAN_POINT ( 'NONE',  ( -5.200782296141404082E-16, -0.6346842323187715795, 6.499999999999998224 ) ) ;
#31477=LINE ( 'NONE', #62763, #12250 ) ;
#31532=AXIS2_PLACEMENT_3D ( 'NONE', #87496, #13041, #78849 ) ;
#31588=EDGE_CURVE ( 'NONE', #50186, #102336, #82547, .T. ) ;
#31650=FACE_OUTER_BOUND ( 'NONE', #97554, .T. ) ;
#31674=VECTOR ( 'NONE', #70918, 1000.000000000000227 ) ;
#31699=ORIENTED_EDGE ( 'NONE', *, *, #53378, .T. ) ;
#31709=ADVANCED_FACE ( 'NONE', ( #94701 ), #84248, .T. ) ;
#31726=DIRECTION ( 'NONE',  ( -1.000000000000000000, -1.224606353822377258E-16, -0.000000000000000000 ) ) ;
#31802=DIRECTION ( 'NONE',  ( -1.000000000000000000, -1.224606353822377258E-16, -0.000000000000000000 ) ) ;
#31806=DIRECTION ( 'NONE',  ( 0.000000000000000000, 1.000000000000000000, 0.000000000000000000 ) ) ;
#31831=ORIENTED_EDGE ( 'NONE', *, *, #50779, .T. ) ;
#31848=DIRECTION ( 'NONE',  ( 0.000000000000000000, 0.000000000000000000, -1.000000000000000000 ) ) ;
#31854=ADVANCED_FACE ( 'NONE', ( #29454 ), #104347, .T. ) ;
#31867=EDGE_CURVE ( 'NONE', #53571, #35344, #21353, .T. ) ;
#31886=EDGE_CURVE ( 'NONE', #55601, #58295, #8483, .T. ) ;
#31906=DIRECTION ( 'NONE',  ( 0.000000000000000000, 0.000000000000000000, -1.000000000000000000 ) ) ;
#31910=CYLINDRICAL_SURFACE ( 'NONE', #56569, 4.000000000000000000 ) ;
#31918=VERTEX_POINT ( 'NONE', #65495 ) ;
#31957=AXIS2_PLACEMENT_3D ( 'NONE', #71349, #6087, #54615 ) ;
#31973=CONICAL_SURFACE ( 'NONE', #33742, 3.309500000000007880, 0.9599310885968770357 ) ;
#32030=DIRECTION ( 'NONE',  ( 0.000000000000000000, -1.000000000000000000, 0.000000000000000000 ) ) ;
#32046=CIRCLE ( 'NONE', #23519, 4.000000000000007105 ) ;
#32062=VERTEX_POINT ( 'NONE', #52482 ) ;
#32088=DIRECTION ( 'NONE',  ( -1.000000000000000000, -1.224606353822377258E-16, -0.000000000000000000 ) ) ;
#32170=DIRECTION ( 'NONE',  ( 0.000000000000000000, 0.000000000000000000, 1.000000000000000000 ) ) ;
#32172=EDGE_CURVE ( 'NONE', #20574, #83726, #37946, .T. ) ;
#32184=EDGE_LOOP ( 'NONE', ( #70944, #100793, #97342 ) ) ;
#32217=CARTESIAN_POINT ( 'NONE',  ( 52.81650669486619165, -1.232595164407830946E-29, 4.000000000000007105 ) ) ;
#32242=EDGE_LOOP ( 'NONE', ( #20457, #72733, #41119, #69128, #62464 ) ) ;
#32281=VERTEX_POINT ( 'NONE', #24410 ) ;
#32306=AXIS2_PLACEMENT_3D ( 'NONE', #54360, #87303, #13386 ) ;
#32311=VERTEX_POINT ( 'NONE', #48097 ) ;
#32343=CIRCLE ( 'NONE', #70203, 4.000000000000007105 ) ;
#32376=VECTOR ( 'NONE', #11904, 1000.000000000000227 ) ;
#32387=CIRCLE ( 'NONE', #23771, 3.309500000000007880 ) ;
#32394=ORIENTED_EDGE ( 'NONE', *, *, #85026, .F. ) ;
#32413=LINE ( 'NONE', #74422, #97995 ) ;
#32419=SURFACE_SIDE_STYLE ('',( #106260 ) ) ;
#32422=AXIS2_PLACEMENT_3D ( 'NONE', #17597, #49937, #82842 ) ;
#32429=VECTOR ( 'NONE', #52714, 1000.000000000000000 ) ;
#32455=DIRECTION ( 'NONE',  ( -1.000000000000000000, -0.000000000000000000, -0.000000000000000000 ) ) ;
#32524=EDGE_CURVE ( 'NONE', #86309, #90844, #1605, .T. ) ;
#32580=DIRECTION ( 'NONE',  ( 0.000000000000000000, -1.000000000000000000, 0.000000000000000000 ) ) ;
#32610=DIRECTION ( 'NONE',  ( 0.000000000000000000, -1.000000000000000000, 0.000000000000000000 ) ) ;
#32634=CIRCLE ( 'NONE', #68809, 4.000000000000007105 ) ;
#32651=EDGE_CURVE ( 'NONE', #82907, #99696, #94506, .T. ) ;
#32667=ORIENTED_EDGE ( 'NONE', *, *, #13119, .T. ) ;
#32679=ORIENTED_EDGE ( 'NONE', *, *, #96676, .T. ) ;
#32695=ORIENTED_EDGE ( 'NONE', *, *, #43376, .F. ) ;
#32732=LINE ( 'NONE', #97962, #87153 ) ;
#32788=ORIENTED_EDGE ( 'NONE', *, *, #3398, .F. ) ;
#32794=AXIS2_PLACEMENT_3D ( 'NONE', #19753, #36465, #68806 ) ;
#32809=LINE ( 'NONE', #83450, #73555 ) ;
#32826=CARTESIAN_POINT ( 'NONE',  ( 0.000000000000000000, 0.000000000000000000, 0.000000000000000000 ) ) ;
#32859=AXIS2_PLACEMENT_3D ( 'NONE', #37665, #64042, #89367 ) ;
#32862=ORIENTED_EDGE ( 'NONE', *, *, #79102, .T. ) ;
#32865=LINE ( 'NONE', #100750, #100109 ) ;
#32885=ORIENTED_EDGE ( 'NONE', *, *, #21854, .F. ) ;
#32915=AXIS2_PLACEMENT_3D ( 'NONE', #27690, #102057, #28218 ) ;
#32932=CARTESIAN_POINT ( 'NONE',  ( 0.000000000000000000, 4.898587196589412829E-16, -4.000000000000000000 ) ) ;
#32935=AXIS2_PLACEMENT_3D ( 'NONE', #70597, #3203, #103488 ) ;
#32936=EDGE_CURVE ( 'NONE', #40695, #5888, #61868, .T. ) ;
#32938=ORIENTED_EDGE ( 'NONE', *, *, #75852, .F. ) ;
#32975=CARTESIAN_POINT ( 'NONE',  ( 4.699999999999999289, 6.499999999999999112, 0.000000000000000000 ) ) ;
#33003=CIRCLE ( 'NONE', #12258, 4.000000000000007105 ) ;
#33054=EDGE_LOOP ( 'NONE', ( #44775, #26324, #64305, #46029, #101959 ) ) ;
#33068=EDGE_CURVE ( 'NONE', #94772, #58831, #79962, .T. ) ;
#33100=DIRECTION ( 'NONE',  ( -1.000000000000000000, -1.224606353822377258E-16, -0.000000000000000000 ) ) ;
#33142=EDGE_LOOP ( 'NONE', ( #51653, #81459, #26526, #18525, #31086 ) ) ;
#33143=CARTESIAN_POINT ( 'NONE',  ( 53.78349330513380266, 4.000000000000014211, 0.000000000000000000 ) ) ;
#33161=ORIENTED_EDGE ( 'NONE', *, *, #77790, .F. ) ;
#33172=CARTESIAN_POINT ( 'NONE',  ( 69.67238219402268840, 4.000000000000014211, 0.000000000000000000 ) ) ;
#33191=ORIENTED_EDGE ( 'NONE', *, *, #84689, .T. ) ;
#33209=CARTESIAN_POINT ( 'NONE',  ( 0.5805565836007654523, 7.505553499465139389, 1.865978384307260116E-16 ) ) ;
#33223=VECTOR ( 'NONE', #43365, 1000.000000000000000 ) ;
#33239=CARTESIAN_POINT ( 'NONE',  ( 4.370690007832189750E-16, -5.309483803148808079, -3.803704290982246494 ) ) ;
#33265=VERTEX_POINT ( 'NONE', #56195 ) ;
#33284=FACE_OUTER_BOUND ( 'NONE', #41132, .T. ) ;
#33296=UNCERTAINTY_MEASURE_WITH_UNIT (LENGTH_MEASURE( 1.000000000000000082E-05 ), #73148, 'distance_accuracy_value', 'NONE');
#33312=DIRECTION ( 'NONE',  ( -1.000000000000000000, -1.224606353822377258E-16, -0.000000000000000000 ) ) ;
#33351=DIRECTION ( 'NONE',  ( -0.5735764363510497121, 0.8191520442889892450, 1.003171929053521665E-16 ) ) ;
#33384=ORIENTED_EDGE ( 'NONE', *, *, #54369, .T. ) ;
#33398=LINE ( 'NONE', #91100, #4834 ) ;
#33402=AXIS2_PLACEMENT_3D ( 'NONE', #35741, #93946, #86926 ) ;
#33413=ORIENTED_EDGE ( 'NONE', *, *, #53109, .T. ) ;
#33459=EDGE_CURVE ( 'NONE', #25843, #84625, #46055, .T. ) ;
#33598=DIRECTION ( 'NONE',  ( -1.000000000000000000, -0.000000000000000000, -0.000000000000000000 ) ) ;
#33681=CARTESIAN_POINT ( 'NONE',  ( 63.56127108291158123, 6.975173280561618775E-15, 0.000000000000000000 ) ) ;
#33688=DIRECTION ( 'NONE',  ( 0.000000000000000000, -1.000000000000000000, 0.000000000000000000 ) ) ;
#33742=AXIS2_PLACEMENT_3D ( 'NONE', #19370, #100223, #50589 ) ;
#33750=ORIENTED_EDGE ( 'NONE', *, *, #84789, .T. ) ;
#33781=ADVANCED_FACE ( 'NONE', ( #25583 ), #15401, .T. ) ;
#33790=FACE_OUTER_BOUND ( 'NONE', #74808, .T. ) ;
#33851=DIRECTION ( 'NONE',  ( -1.000000000000000000, -1.224606353822377258E-16, -0.000000000000000000 ) ) ;
#33866=CARTESIAN_POINT ( 'NONE',  ( 0.000000000000000000, 4.898587196589412829E-16, -4.000000000000000000 ) ) ;
#33923=EDGE_LOOP ( 'NONE', ( #101404, #93639, #24786 ) ) ;
#33927=DIRECTION ( 'NONE',  ( -1.000000000000000000, -1.224606353822377258E-16, -0.000000000000000000 ) ) ;
#33929=VECTOR ( 'NONE', #80062, 1000.000000000000000 ) ;
#33941=CARTESIAN_POINT ( 'NONE',  ( 70.41111111111112564, 3.309500000000014541, 4.052968581778174646E-16 ) ) ;
#33950=DIRECTION ( 'NONE',  ( 0.000000000000000000, 0.000000000000000000, 1.000000000000000000 ) ) ;
#33967=CARTESIAN_POINT ( 'NONE',  ( 55.74444444444444713, 6.915964383211875250E-15, 0.000000000000000000 ) ) ;
#33988=PLANE ( 'NONE',  #74604 ) ;
#33990=EDGE_CURVE ( 'NONE', #48389, #98734, #47904, .T. ) ;
#34035=ADVANCED_FACE ( 'NONE', ( #24211 ), #58132, .T. ) ;
#34040=ORIENTED_EDGE ( 'NONE', *, *, #2395, .F. ) ;
#34049=AXIS2_PLACEMENT_3D ( 'NONE', #24613, #74183, #49373 ) ;
#34056=CARTESIAN_POINT ( 'NONE',  ( 5.299999999999999822, 7.505553499465139389, 0.000000000000000000 ) ) ;
#34090=EDGE_LOOP ( 'NONE', ( #99751, #14018, #105368, #102199, #91711 ) ) ;
#34166=EDGE_LOOP ( 'NONE', ( #102157, #11344, #67634, #151, #86407 ) ) ;
#34179=FACE_OUTER_BOUND ( 'NONE', #70504, .T. ) ;
#34259=VERTEX_POINT ( 'NONE', #77521 ) ;
#34264=ORIENTED_EDGE ( 'NONE', *, *, #34407, .F. ) ;
#34276=AXIS2_PLACEMENT_3D ( 'NONE', #100685, #66737, #3063 ) ;
#34286=DIRECTION ( 'NONE',  ( -1.000000000000000000, -1.224606353822377258E-16, -0.000000000000000000 ) ) ;
#34298=ORIENTED_EDGE ( 'NONE', *, *, #90958, .F. ) ;
#34332=EDGE_CURVE ( 'NONE', #57426, #3882, #72302, .T. ) ;
#34345=ORIENTED_EDGE ( 'NONE', *, *, #89956, .F. ) ;
#34374=ORIENTED_EDGE ( 'NONE', *, *, #45544, .T. ) ;
#34382=VERTEX_POINT ( 'NONE', #5742 ) ;
#34387=DIRECTION ( 'NONE',  ( -1.000000000000000000, -0.000000000000000000, -0.000000000000000000 ) ) ;
#34391=LINE ( 'NONE', #58640, #5346 ) ;
#34401=B_SPLINE_CURVE_WITH_KNOTS ( 'NONE', 3,
 ( #12846, #37176, #68042, #53847, #26569, #13372 ),
 .UNSPECIFIED., .F., .F.,
 ( 4, 2, 4 ),
 ( 2.380733003139562229E-07, 0.001898835937927374632, 0.003797433802554435033 ),
 .UNSPECIFIED. ) ;
#34407=EDGE_CURVE ( 'NONE', #63428, #15295, #46215, .T. ) ;
#34428=CARTESIAN_POINT ( 'NONE',  ( 62.33904886068935980, 6.975173280561618775E-15, 0.000000000000000000 ) ) ;
#34456=AXIS2_PLACEMENT_3D ( 'NONE', #42529, #66818, #33950 ) ;
#34459=DIRECTION ( 'NONE',  ( 0.000000000000000000, 0.000000000000000000, 1.000000000000000000 ) ) ;
#34471=ORIENTED_EDGE ( 'NONE', *, *, #85918, .F. ) ;
#34488=CARTESIAN_POINT ( 'NONE',  ( 69.67238219402268840, 6.975173280561618775E-15, 0.000000000000000000 ) ) ;
#34491=AXIS2_PLACEMENT_3D ( 'NONE', #68017, #69100, #50234 ) ;
#34499=ORIENTED_EDGE ( 'NONE', *, *, #36895, .F. ) ;
#34525=LINE ( 'NONE', #67394, #60862 ) ;
#34545=EDGE_LOOP ( 'NONE', ( #12529, #48684, #24003, #79371, #10511 ) ) ;
#34579=ORIENTED_EDGE ( 'NONE', *, *, #31886, .T. ) ;
#34662=ORIENTED_EDGE ( 'NONE', *, *, #82849, .T. ) ;
#34671=DIRECTION ( 'NONE',  ( 0.000000000000000000, -1.000000000000000000, 0.000000000000000000 ) ) ;
#34698=AXIS2_PLACEMENT_3D ( 'NONE', #8747, #83173, #26582 ) ;
#34705=CIRCLE ( 'NONE', #72544, 4.000000000000007105 ) ;
#34782=VECTOR ( 'NONE', #41931, 1000.000000000000000 ) ;
#34819=AXIS2_PLACEMENT_3D ( 'NONE', #75248, #10521, #1349 ) ;
#34899=FACE_OUTER_BOUND ( 'NONE', #40220, .T. ) ;
#34916=CARTESIAN_POINT ( 'NONE',  ( 65.03872891708842019, 4.000000000000015099, 4.898587196589422689E-16 ) ) ;
#34923=DIRECTION ( 'NONE',  ( 0.000000000000000000, -1.000000000000000000, 0.000000000000000000 ) ) ;
#34948=ORIENTED_EDGE ( 'NONE', *, *, #63395, .T. ) ;
#34964=EDGE_CURVE ( 'NONE', #93530, #68880, #99075, .T. ) ;
#34985=ORIENTED_EDGE ( 'NONE', *, *, #48029, .T. ) ;
#35002=DIRECTION ( 'NONE',  ( -1.000000000000000000, -0.000000000000000000, -0.000000000000000000 ) ) ;
#35035=ORIENTED_EDGE ( 'NONE', *, *, #4281, .F. ) ;
#35051=CARTESIAN_POINT ( 'NONE',  ( 0.000000000000000000, 0.000000000000000000, 4.000000000000000000 ) ) ;
#35083=DIRECTION ( 'NONE',  ( -1.000000000000000000, -1.224606353822377258E-16, -0.000000000000000000 ) ) ;
#35102=VERTEX_POINT ( 'NONE', #71025 ) ;
#35193=DIRECTION ( 'NONE',  ( -1.000000000000000000, -0.000000000000000000, -0.000000000000000000 ) ) ;
#35199=DIRECTION ( 'NONE',  ( 0.000000000000000000, 0.000000000000000000, 1.000000000000000000 ) ) ;
#35260=VERTEX_POINT ( 'NONE', #19746 ) ;
#35280=EDGE_CURVE ( 'NONE', #51147, #50622, #80138, .T. ) ;
#35284=VERTEX_POINT ( 'NONE', #15312 ) ;
#35311=ADVANCED_FACE ( 'NONE', ( #72999 ), #7762, .T. ) ;
#35322=DIRECTION ( 'NONE',  ( 0.5735764363510442720, -0.8191520442889930198, 1.003171929053526349E-16 ) ) ;
#35344=VERTEX_POINT ( 'NONE', #95715 ) ;
#35356=CARTESIAN_POINT ( 'NONE',  ( 0.000000000000000000, 4.898587196589412829E-16, -4.000000000000000000 ) ) ;
#35361=EDGE_CURVE ( 'NONE', #22931, #23441, #31010, .T. ) ;
#35394=CARTESIAN_POINT ( 'NONE',  ( 57.45015997180046696, 6.975173280561618775E-15, 0.000000000000000000 ) ) ;
#35459=VECTOR ( 'NONE', #103195, 1000.000000000000000 ) ;
#35470=EDGE_CURVE ( 'NONE', #8224, #35344, #49095, .T. ) ;
#35527=DIRECTION ( 'NONE',  ( 0.000000000000000000, -1.000000000000000000, 0.000000000000000000 ) ) ;
#35528=DIRECTION ( 'NONE',  ( -1.000000000000000000, -1.224606353822377258E-16, -0.000000000000000000 ) ) ;
#35534=DIRECTION ( 'NONE',  ( -0.000000000000000000, 1.000000000000000000, 2.311253228826400140E-16 ) ) ;
#35544=DIRECTION ( 'NONE',  ( -1.000000000000000000, -1.224606353822377258E-16, -0.000000000000000000 ) ) ;
#35611=CARTESIAN_POINT ( 'NONE',  ( 0.05533025579361924157, -6.264553569211837036, 2.149474931388137389 ) ) ;
#35635=ORIENTED_EDGE ( 'NONE', *, *, #4287, .T. ) ;
#35646=FACE_OUTER_BOUND ( 'NONE', #64631, .T. ) ;
#35669=DIRECTION ( 'NONE',  ( 0.000000000000000000, 1.000000000000000000, 0.000000000000000000 ) ) ;
#35695=CONICAL_SURFACE ( 'NONE', #39140, 4.000000000000007105, 0.9599310885968835860 ) ;
#35741=CARTESIAN_POINT ( 'NONE',  ( 56.96666666666666856, 6.915964383211875250E-15, 0.000000000000000000 ) ) ;
#35792=DIRECTION ( 'NONE',  ( 0.000000000000000000, 0.000000000000000000, -1.000000000000000000 ) ) ;
#35866=ORIENTED_EDGE ( 'NONE', *, *, #35470, .T. ) ;
#35917=AXIS2_PLACEMENT_3D ( 'NONE', #79341, #104678, #53485 ) ;
#36015=DIRECTION ( 'NONE',  ( 0.000000000000000000, -1.000000000000000000, 0.000000000000000000 ) ) ;
#36016=CARTESIAN_POINT ( 'NONE',  ( 0.4053525175236814548, 3.145852061456249960, 6.499999999999998224 ) ) ;
#36115=CYLINDRICAL_SURFACE ( 'NONE', #49596, 6.499999999999999112 ) ;
#36130=EDGE_CURVE ( 'NONE', #53571, #87774, #44122, .T. ) ;
#36141=LINE ( 'NONE', #18338, #50669 ) ;
#36169=CARTESIAN_POINT ( 'NONE',  ( 67.22793774957824553, 4.000000000000013323, 0.000000000000000000 ) ) ;
#36239=AXIS2_PLACEMENT_3D ( 'NONE', #52213, #100236, #26403 ) ;
#36299=DIRECTION ( 'NONE',  ( -0.5735764363510494901, -0.8191520442889894671, 0.000000000000000000 ) ) ;
#36377=EDGE_CURVE ( 'NONE', #42645, #41303, #32046, .T. ) ;
#36465=DIRECTION ( 'NONE',  ( -1.000000000000000000, -1.224606353822377258E-16, -0.000000000000000000 ) ) ;
#36509=ORIENTED_EDGE ( 'NONE', *, *, #57360, .T. ) ;
#36531=ORIENTED_EDGE ( 'NONE', *, *, #44946, .F. ) ;
#36544=EDGE_LOOP ( 'NONE', ( #17198, #44590, #25576, #19820, #83101 ) ) ;
#36600=VERTEX_POINT ( 'NONE', #41721 ) ;
#36606=SURFACE_STYLE_USAGE ( .BOTH. , #44132 ) ;
#36608=DIRECTION ( 'NONE',  ( 0.000000000000000000, 0.000000000000000000, 1.000000000000000000 ) ) ;
#36624=DIRECTION ( 'NONE',  ( -1.000000000000000000, -0.000000000000000000, -0.000000000000000000 ) ) ;
#36649=CARTESIAN_POINT ( 'NONE',  ( 0.4042117618284710723, -3.141900367810050110, -6.500000000000000888 ) ) ;
#36679=CARTESIAN_POINT ( 'NONE',  ( 71.14984002819953446, 4.000000000000015099, 4.898587196589422689E-16 ) ) ;
#36715=ORIENTED_EDGE ( 'NONE', *, *, #100836, .T. ) ;
#36721=CARTESIAN_POINT ( 'NONE',  ( 68.45015997180047407, 6.975173280561618775E-15, 0.000000000000000000 ) ) ;
#36725=CARTESIAN_POINT ( 'NONE',  ( 73.59428447264397732, 4.000000000000015099, 4.898587196589422689E-16 ) ) ;
#36776=DIRECTION ( 'NONE',  ( -1.000000000000000000, -0.000000000000000000, -0.000000000000000000 ) ) ;
#36794=AXIS2_PLACEMENT_3D ( 'NONE', #12850, #45766, #63560 ) ;
#36802=CARTESIAN_POINT ( 'NONE',  ( 5.299999999999999822, 3.752776749732569694, 6.499999999999997335 ) ) ;
#36818=LINE ( 'NONE', #4408, #83751 ) ;
#36822=FACE_OUTER_BOUND ( 'NONE', #28520, .T. ) ;
#36895=EDGE_CURVE ( 'NONE', #58101, #59703, #99292, .T. ) ;
#36915=CARTESIAN_POINT ( 'NONE',  ( 73.33904886068935980, 6.975173280561618775E-15, 0.000000000000000000 ) ) ;
#36928=DIRECTION ( 'NONE',  ( -1.000000000000000000, -0.000000000000000000, -0.000000000000000000 ) ) ;
#36961=CARTESIAN_POINT ( 'NONE',  ( 55.26095113931063452, -1.232595164407830946E-29, 4.000000000000007105 ) ) ;
#36974=ORIENTED_EDGE ( 'NONE', *, *, #71220, .F. ) ;
#37007=ORIENTED_EDGE ( 'NONE', *, *, #5674, .T. ) ;
#37041=VERTEX_POINT ( 'NONE', #81490 ) ;
#37042=PLANE ( 'NONE',  #26748 ) ;
#37118=VERTEX_POINT ( 'NONE', #76610 ) ;
#37130=CIRCLE ( 'NONE', #31957, 4.000000000000007105 ) ;
#37145=ORIENTED_EDGE ( 'NONE', *, *, #103403, .F. ) ;
#37176=CARTESIAN_POINT ( 'NONE',  ( 0.4033376246892486083, 4.059728990630805612, 5.968343123267133343 ) ) ;
#37216=CIRCLE ( 'NONE', #38959, 3.309500000000007880 ) ;
#37261=CARTESIAN_POINT ( 'NONE',  ( 4.699999999999999289, 0.000000000000000000, 0.000000000000000000 ) ) ;
#37327=ADVANCED_FACE ( 'NONE', ( #8564 ), #89075, .T. ) ;
#37351=DIRECTION ( 'NONE',  ( 0.000000000000000000, -1.000000000000000000, 0.000000000000000000 ) ) ;
#37357=CARTESIAN_POINT ( 'NONE',  ( 5.299999999999999822, -7.505553499465137612, 3.546421054897781431E-16 ) ) ;
#37431=LINE ( 'NONE', #85417, #35459 ) ;
#37460=CONICAL_SURFACE ( 'NONE', #13225, 4.000000000000007105, 0.9599310885968835860 ) ;
#37461=VECTOR ( 'NONE', #32455, 1000.000000000000000 ) ;
#37476=DIRECTION ( 'NONE',  ( 1.000000000000000000, 1.224606353822377258E-16, 0.000000000000000000 ) ) ;
#37483=DIRECTION ( 'NONE',  ( 0.000000000000000000, -1.000000000000000000, 0.000000000000000000 ) ) ;
#37542=ORIENTED_EDGE ( 'NONE', *, *, #62779, .F. ) ;
#37548=VECTOR ( 'NONE', #104700, 1000.000000000000000 ) ;
#37575=FACE_OUTER_BOUND ( 'NONE', #46509, .T. ) ;
#37589=ORIENTED_EDGE ( 'NONE', *, *, #60688, .F. ) ;
#37599=ORIENTED_EDGE ( 'NONE', *, *, #55028, .F. ) ;
#37661=CIRCLE ( 'NONE', #41006, 3.309500000000007880 ) ;
#37665=CARTESIAN_POINT ( 'NONE',  ( 58.92761780597729881, 6.856755485862130937E-15, 0.000000000000000000 ) ) ;
#37713=CARTESIAN_POINT ( 'NONE',  ( 5.908054807098742893E-16, -0.6346842323187772417, -6.500000000000000000 ) ) ;
#37768=CARTESIAN_POINT ( 'NONE',  ( 0.4033376246892518835, -4.059728990630813605, -5.968343123267134231 ) ) ;
#37770=EDGE_LOOP ( 'NONE', ( #61180, #58634, #95445, #29448, #19726, #59060 ) ) ;
#37870=DIRECTION ( 'NONE',  ( -1.000000000000000000, -1.224606353822377258E-16, -0.000000000000000000 ) ) ;
#37876=DIRECTION ( 'NONE',  ( 0.000000000000000000, -1.000000000000000000, 0.000000000000000000 ) ) ;
#37880=EDGE_CURVE ( 'NONE', #22977, #65105, #44275, .T. ) ;
#37892=EDGE_CURVE ( 'NONE', #84395, #39378, #9917, .T. ) ;
#37897=AXIS2_PLACEMENT_3D ( 'NONE', #54256, #21416, #44619 ) ;
#37936=VERTEX_POINT ( 'NONE', #85954 ) ;
#37941=CARTESIAN_POINT ( 'NONE',  ( 71.63333333333333997, 6.915964383211875250E-15, 0.000000000000000000 ) ) ;
#37946=LINE ( 'NONE', #87006, #70551 ) ;
#37954=EDGE_LOOP ( 'NONE', ( #98817, #67469, #94579, #4850, #8681 ) ) ;
#37955=CARTESIAN_POINT ( 'NONE',  ( 74.60950000000003968, 0.000000000000000000, 0.000000000000000000 ) ) ;
#37980=DIRECTION ( 'NONE',  ( 1.000000000000000000, 0.000000000000000000, 0.000000000000000000 ) ) ;
#37992=EDGE_CURVE ( 'NONE', #27209, #30721, #43346, .T. ) ;
#38001=VECTOR ( 'NONE', #42950, 999.9999999999998863 ) ;
#38062=CARTESIAN_POINT ( 'NONE',  ( 55.00571552735602410, -4.000000000000000000, 4.898587196589421703E-16 ) ) ;
#38097=VECTOR ( 'NONE', #64230, 1000.000000000000227 ) ;
#38119=VERTEX_POINT ( 'NONE', #8714 ) ;
#38135=CARTESIAN_POINT ( 'NONE',  ( 70.89460441624491693, 4.000000000000013323, 0.000000000000000000 ) ) ;
#38138=CIRCLE ( 'NONE', #15675, 4.000000000000007105 ) ;
#38170=CARTESIAN_POINT ( 'NONE',  ( 67.96666666666666856, 6.915964383211875250E-15, 0.000000000000000000 ) ) ;
#38217=VERTEX_POINT ( 'NONE', #80999 ) ;
#38223=CARTESIAN_POINT ( 'NONE',  ( 63.07777777777777573, 6.915964383211875250E-15, 0.000000000000000000 ) ) ;
#38229=DIRECTION ( 'NONE',  ( 0.000000000000000000, -1.000000000000000000, 0.000000000000000000 ) ) ;
#38250=CARTESIAN_POINT ( 'NONE',  ( 0.2578475836320665016, -4.367703157927319779, 5.434916218090832807 ) ) ;
#38361=VERTEX_POINT ( 'NONE', #73050 ) ;
#38450=ORIENTED_EDGE ( 'NONE', *, *, #45010, .F. ) ;
#38486=DIRECTION ( 'NONE',  ( 0.000000000000000000, 0.000000000000000000, 1.000000000000000000 ) ) ;
#38488=EDGE_CURVE ( 'NONE', #1105, #12701, #15151, .T. ) ;
#38515=CARTESIAN_POINT ( 'NONE',  ( 61.37206225042174879, 6.856755485862130937E-15, 0.000000000000000000 ) ) ;
#38522=VECTOR ( 'NONE', #66694, 1000.000000000000000 ) ;
#38528=EDGE_CURVE ( 'NONE', #82654, #26677, #51449, .T. ) ;
#38533=CYLINDRICAL_SURFACE ( 'NONE', #42820, 4.000000000000000000 ) ;
#38550=VERTEX_POINT ( 'NONE', #59566 ) ;
#38559=CYLINDRICAL_SURFACE ( 'NONE', #8058, 4.000000000000000000 ) ;
#38582=DIRECTION ( 'NONE',  ( -1.000000000000000000, -0.000000000000000000, -0.000000000000000000 ) ) ;
#38596=ORIENTED_EDGE ( 'NONE', *, *, #77790, .T. ) ;
#38605=EDGE_LOOP ( 'NONE', ( #32885, #38596, #74757, #17044, #100150, #11406 ) ) ;
#38613=AXIS2_PLACEMENT_3D ( 'NONE', #23458, #29442, #54178 ) ;
#38614=DIRECTION ( 'NONE',  ( 0.000000000000000000, -1.000000000000000000, 0.000000000000000000 ) ) ;
#38620=CARTESIAN_POINT ( 'NONE',  ( 64.29999999999999716, 6.915964383211875250E-15, 0.000000000000000000 ) ) ;
#38662=DIRECTION ( 'NONE',  ( 0.000000000000000000, -1.000000000000000000, 0.000000000000000000 ) ) ;
#38755=ORIENTED_EDGE ( 'NONE', *, *, #88383, .F. ) ;
#38773=ORIENTED_EDGE ( 'NONE', *, *, #12202, .T. ) ;
#38809=CARTESIAN_POINT ( 'NONE',  ( 0.000000000000000000, 1.502314598737160017E-15, -6.500000000000000000 ) ) ;
#38887=CARTESIAN_POINT ( 'NONE',  ( 63.07777777777777573, 3.309500000000014541, 4.052968581778174646E-16 ) ) ;
#38929=EDGE_CURVE ( 'NONE', #21000, #102866, #8362, .T. ) ;
#38959=AXIS2_PLACEMENT_3D ( 'NONE', #22301, #23896, #97206 ) ;
#39017=DIRECTION ( 'NONE',  ( -1.000000000000000000, -0.000000000000000000, -0.000000000000000000 ) ) ;
#39025=CIRCLE ( 'NONE', #63113, 4.000000000000007105 ) ;
#39082=DIRECTION ( 'NONE',  ( 1.000000000000000000, 1.224606353822377258E-16, 0.000000000000000000 ) ) ;
#39126=VECTOR ( 'NONE', #103211, 1000.000000000000227 ) ;
#39138=AXIS2_PLACEMENT_3D ( 'NONE', #105410, #175, #89236 ) ;
#39140=AXIS2_PLACEMENT_3D ( 'NONE', #75659, #91853, #77268 ) ;
#39143=ORIENTED_EDGE ( 'NONE', *, *, #53045, .F. ) ;
#39162=ORIENTED_EDGE ( 'NONE', *, *, #90958, .T. ) ;
#39192=DIRECTION ( 'NONE',  ( 0.5735764363510442720, -0.8191520442889930198, 1.003171929053526349E-16 ) ) ;
#39198=CIRCLE ( 'NONE', #99447, 3.309500000000007880 ) ;
#39227=ADVANCED_FACE ( 'NONE', ( #10870 ), #93418, .T. ) ;
#39236=VERTEX_POINT ( 'NONE', #84788 ) ;
#39276=DIRECTION ( 'NONE',  ( -1.000000000000000000, -0.000000000000000000, -0.000000000000000000 ) ) ;
#39306=CIRCLE ( 'NONE', #84100, 4.000000000000007105 ) ;
#39308=VERTEX_POINT ( 'NONE', #27660 ) ;
#39313=ADVANCED_FACE ( 'NONE', ( #76149 ), #15233, .T. ) ;
#39358=EDGE_CURVE ( 'NONE', #20770, #55118, #65195, .T. ) ;
#39373=CARTESIAN_POINT ( 'NONE',  ( 0.000000000000000000, 0.000000000000000000, 4.000000000000000000 ) ) ;
#39378=VERTEX_POINT ( 'NONE', #96602 ) ;
#39383=ADVANCED_FACE ( 'NONE', ( #47495 ), #53124, .T. ) ;
#39388=CARTESIAN_POINT ( 'NONE',  ( 70.89460441624491693, 6.975173280561618775E-15, 0.000000000000000000 ) ) ;
#39410=VECTOR ( 'NONE', #97271, 1000.000000000000000 ) ;
#39437=CARTESIAN_POINT ( 'NONE',  ( 69.67238219402268840, 6.975173280561618775E-15, 0.000000000000000000 ) ) ;
#39545=EDGE_LOOP ( 'NONE', ( #80903, #50774, #33191, #12901, #82574, #16443 ) ) ;
#39553=CARTESIAN_POINT ( 'NONE',  ( 5.700000000000000178, 4.898587196589412829E-16, -4.000000000000000000 ) ) ;
#39575=CARTESIAN_POINT ( 'NONE',  ( 0.000000000000000000, 5.629165124598842773, -3.250000000000011990 ) ) ;
#39601=AXIS2_PLACEMENT_3D ( 'NONE', #32826, #26356, #17692 ) ;
#39604=CARTESIAN_POINT ( 'NONE',  ( 0.000000000000000000, 0.000000000000000000, 0.000000000000000000 ) ) ;
#39618=EDGE_CURVE ( 'NONE', #43619, #42218, #32413, .T. ) ;
#39620=ORIENTED_EDGE ( 'NONE', *, *, #5781, .T. ) ;
#39632=DIRECTION ( 'NONE',  ( -1.000000000000000000, -1.224606353822377258E-16, -0.000000000000000000 ) ) ;
#39679=DIRECTION ( 'NONE',  ( -0.5735764363510497121, 0.8191520442889892450, 1.003171929053521665E-16 ) ) ;
#39734=DIRECTION ( 'NONE',  ( 0.000000000000000000, -1.000000000000000000, 0.000000000000000000 ) ) ;
#39846=VECTOR ( 'NONE', #83992, 1000.000000000000000 ) ;
#39854=EDGE_CURVE ( 'NONE', #54950, #82447, #30822, .T. ) ;
#39869=CARTESIAN_POINT ( 'NONE',  ( 63.07777777777777573, -3.309500000000000774, 0.000000000000000000 ) ) ;
#39901=CIRCLE ( 'NONE', #70859, 4.000000000000007105 ) ;
#39909=FACE_OUTER_BOUND ( 'NONE', #63540, .T. ) ;
#39938=EDGE_LOOP ( 'NONE', ( #70672, #53772, #61122, #62863, #32695, #62941 ) ) ;
#39962=( NAMED_UNIT ( * ) PLANE_ANGLE_UNIT ( ) SI_UNIT ( $, .RADIAN. ) );
#39979=B_SPLINE_CURVE_WITH_KNOTS ( 'NONE', 3,
 ( #23906, #56202, #104786, #105321, #31464, #96702 ),
 .UNSPECIFIED., .F., .F.,
 ( 4, 2, 4 ),
 ( 0.006874058789394420221, 0.008773169699889928064, 0.01067228061038543591 ),
 .UNSPECIFIED. ) ;
#39991=CARTESIAN_POINT ( 'NONE',  ( 0.000000000000000000, 4.898587196589412829E-16, -4.000000000000000000 ) ) ;
#40024=CARTESIAN_POINT ( 'NONE',  ( 0.000000000000000000, 0.000000000000000000, 0.000000000000000000 ) ) ;
#40059=FACE_OUTER_BOUND ( 'NONE', #49819, .T. ) ;
#40074=VERTEX_POINT ( 'NONE', #100720 ) ;
#40079=CIRCLE ( 'NONE', #3898, 4.000000000000007105 ) ;
#40091=ORIENTED_EDGE ( 'NONE', *, *, #51112, .F. ) ;
#40202=EDGE_CURVE ( 'NONE', #87625, #68880, #99377, .T. ) ;
#40220=EDGE_LOOP ( 'NONE', ( #100654, #12715, #41242, #19772, #10590 ) ) ;
#40230=LINE ( 'NONE', #98974, #77638 ) ;
#40243=CYLINDRICAL_SURFACE ( 'NONE', #77340, 4.000000000000000000 ) ;
#40274=ORIENTED_EDGE ( 'NONE', *, *, #50800, .T. ) ;
#40289=VERTEX_POINT ( 'NONE', #62159 ) ;
#40297=ORIENTED_EDGE ( 'NONE', *, *, #46484, .T. ) ;
#40301=CARTESIAN_POINT ( 'NONE',  ( 54.52222222222221859, 6.915964383211875250E-15, 0.000000000000000000 ) ) ;
#40361=CARTESIAN_POINT ( 'NONE',  ( 61.11682663846713837, 4.000000000000013323, 0.000000000000000000 ) ) ;
#40382=FACE_OUTER_BOUND ( 'NONE', #89691, .T. ) ;
#40420=DIRECTION ( 'NONE',  ( -1.000000000000000000, -1.224606353822377258E-16, -0.000000000000000000 ) ) ;
#40471=DIRECTION ( 'NONE',  ( -1.000000000000000000, -0.000000000000000000, -0.000000000000000000 ) ) ;
#40474=CARTESIAN_POINT ( 'NONE',  ( 67.22793774957824553, -1.232595164407830946E-29, 4.000000000000007105 ) ) ;
#40480=( LENGTH_UNIT ( ) NAMED_UNIT ( * ) SI_UNIT ( .MILLI., .METRE. ) );
#40484=DIRECTION ( 'NONE',  ( 0.000000000000000000, -1.000000000000000000, 0.000000000000000000 ) ) ;
#40582=VECTOR ( 'NONE', #68080, 1000.000000000000000 ) ;
#40670=CARTESIAN_POINT ( 'NONE',  ( 53.29999999999999716, 6.915964383211875250E-15, 0.000000000000000000 ) ) ;
#40695=VERTEX_POINT ( 'NONE', #4831 ) ;
#40765=CIRCLE ( 'NONE', #64876, 4.000000000000007105 ) ;
#40777=AXIS2_PLACEMENT_3D ( 'NONE', #3248, #77672, #18385 ) ;
#40942=ADVANCED_FACE ( 'NONE', ( #73675 ), #17058, .T. ) ;
#40953=CARTESIAN_POINT ( 'NONE',  ( 55.74444444444444713, -3.309500000000000774, 0.000000000000000000 ) ) ;
#40993=AXIS2_PLACEMENT_3D ( 'NONE', #20266, #29404, #4561 ) ;
#40999=CIRCLE ( 'NONE', #54766, 4.000000000000007105 ) ;
#41003=ORIENTED_EDGE ( 'NONE', *, *, #73892, .T. ) ;
#41006=AXIS2_PLACEMENT_3D ( 'NONE', #82537, #35083, #9694 ) ;
#41018=AXIS2_PLACEMENT_3D ( 'NONE', #106460, #97846, #41207 ) ;
#41053=ORIENTED_EDGE ( 'NONE', *, *, #8594, .T. ) ;
#41106=VERTEX_POINT ( 'NONE', #48210 ) ;
#41119=ORIENTED_EDGE ( 'NONE', *, *, #28937, .T. ) ;
#41132=EDGE_LOOP ( 'NONE', ( #41660, #104774, #44496, #101073, #12786 ) ) ;
#41152=CIRCLE ( 'NONE', #25716, 4.000000000000007105 ) ;
#41162=DIRECTION ( 'NONE',  ( -1.000000000000000000, -1.224606353822377258E-16, -0.000000000000000000 ) ) ;
#41167=LINE ( 'NONE', #49778, #46293 ) ;
#41170=LINE ( 'NONE', #90787, #39410 ) ;
#41171=ORIENTED_EDGE ( 'NONE', *, *, #67860, .F. ) ;
#41174=VECTOR ( 'NONE', #49219, 1000.000000000000000 ) ;
#41207=DIRECTION ( 'NONE',  ( 0.000000000000000000, -1.000000000000000000, 0.000000000000000000 ) ) ;
#41242=ORIENTED_EDGE ( 'NONE', *, *, #83343, .T. ) ;
#41290=DIRECTION ( 'NONE',  ( 0.000000000000000000, 0.4999999999999991673, -0.8660254037844390407 ) ) ;
#41299=CIRCLE ( 'NONE', #32794, 4.000000000000007105 ) ;
#41303=VERTEX_POINT ( 'NONE', #41724 ) ;
#41364=CARTESIAN_POINT ( 'NONE',  ( 58.67238219402268840, 6.975173280561618775E-15, 0.000000000000000000 ) ) ;
#41383=CARTESIAN_POINT ( 'NONE',  ( 5.700000000000000178, 0.000000000000000000, 0.000000000000000000 ) ) ;
#41425=CIRCLE ( 'NONE', #55195, 3.309500000000007880 ) ;
#41442=AXIS2_PLACEMENT_3D ( 'NONE', #92191, #18344, #58239 ) ;
#41446=DIRECTION ( 'NONE',  ( 0.000000000000000000, 0.000000000000000000, -1.000000000000000000 ) ) ;
#41465=CARTESIAN_POINT ( 'NONE',  ( 66.00571552735603120, 6.975173280561618775E-15, 0.000000000000000000 ) ) ;
#41497=ORIENTED_EDGE ( 'NONE', *, *, #76408, .T. ) ;
#41550=VECTOR ( 'NONE', #29150, 1000.000000000000000 ) ;
#41564=ORIENTED_EDGE ( 'NONE', *, *, #105237, .F. ) ;
#41573=DIRECTION ( 'NONE',  ( 0.000000000000000000, -1.000000000000000000, 0.000000000000000000 ) ) ;
#41631=ORIENTED_EDGE ( 'NONE', *, *, #92924, .T. ) ;
#41660=ORIENTED_EDGE ( 'NONE', *, *, #70621, .T. ) ;
#41669=CYLINDRICAL_SURFACE ( 'NONE', #14078, 4.000000000000000000 ) ;
#41696=AXIS2_PLACEMENT_3D ( 'NONE', #34488, #35544, #42527 ) ;
#41721=CARTESIAN_POINT ( 'NONE',  ( 57.45015997180046696, 4.000000000000013323, 0.000000000000000000 ) ) ;
#41724=CARTESIAN_POINT ( 'NONE',  ( 54.03872891708841308, -1.232595164407830946E-29, 4.000000000000007105 ) ) ;
#41777=CARTESIAN_POINT ( 'NONE',  ( 71.14984002819953446, 6.856755485862130937E-15, 0.000000000000000000 ) ) ;
#41785=ORIENTED_EDGE ( 'NONE', *, *, #77636, .F. ) ;
#41801=CARTESIAN_POINT ( 'NONE',  ( 0.2578475836320717196, 6.890627091270373761, 1.065083781909172522 ) ) ;
#41812=ADVANCED_FACE ( 'NONE', ( #45615 ), #94151, .T. ) ;
#41848=ADVANCED_FACE ( 'NONE', ( #13210 ), #46139, .F. ) ;
#41911=DIRECTION ( 'NONE',  ( 0.000000000000000000, -1.000000000000000000, 0.000000000000000000 ) ) ;
#41930=AXIS2_PLACEMENT_3D ( 'NONE', #51728, #27512, #20501 ) ;
#41931=DIRECTION ( 'NONE',  ( -1.000000000000000000, -0.000000000000000000, -0.000000000000000000 ) ) ;
#41937=EDGE_LOOP ( 'NONE', ( #96596, #87562, #15932, #56476, #52194, #28995 ) ) ;
#41964=DIRECTION ( 'NONE',  ( 0.000000000000000000, -1.000000000000000000, 0.000000000000000000 ) ) ;
#41980=AXIS2_PLACEMENT_3D ( 'NONE', #29773, #11546, #76819 ) ;
#42027=ADVANCED_FACE ( 'NONE', ( #18562 ), #99547, .T. ) ;
#42038=AXIS2_PLACEMENT_3D ( 'NONE', #16761, #22766, #52311 ) ;
#42053=CARTESIAN_POINT ( 'NONE',  ( 0.000000000000000000, -5.629165124598843661, 3.250000000000011990 ) ) ;
#42099=AXIS2_PLACEMENT_3D ( 'NONE', #56596, #47446, #99587 ) ;
#42218=VERTEX_POINT ( 'NONE', #63791 ) ;
#42228=DIRECTION ( 'NONE',  ( 0.000000000000000000, -1.000000000000000000, 0.000000000000000000 ) ) ;
#42315=DIRECTION ( 'NONE',  ( 0.000000000000000000, -1.000000000000000000, 0.000000000000000000 ) ) ;
#42346=CONICAL_SURFACE ( 'NONE', #66451, 4.000000000000007105, 0.9599310885968835860 ) ;
#42376=DIRECTION ( 'NONE',  ( -1.000000000000000000, -1.224606353822377258E-16, -0.000000000000000000 ) ) ;
#42382=DIRECTION ( 'NONE',  ( 0.000000000000000000, -1.000000000000000000, 0.000000000000000000 ) ) ;
#42406=CARTESIAN_POINT ( 'NONE',  ( 4.699999999999999289, 3.752776749732553263, -6.499999999999999112 ) ) ;
#42408=LINE ( 'NONE', #83934, #60843 ) ;
#42416=CARTESIAN_POINT ( 'NONE',  ( 69.18888888888888289, 3.309500000000014541, 4.052968581778174646E-16 ) ) ;
#42425=DIRECTION ( 'NONE',  ( -1.000000000000000000, -1.224606353822377258E-16, -0.000000000000000000 ) ) ;
#42428=EDGE_CURVE ( 'NONE', #66517, #35102, #78237, .T. ) ;
#42463=CARTESIAN_POINT ( 'NONE',  ( 58.67238219402268840, 6.975173280561618775E-15, 0.000000000000000000 ) ) ;
#42503=DIRECTION ( 'NONE',  ( -1.000000000000000000, -0.000000000000000000, -0.000000000000000000 ) ) ;
#42515=EDGE_LOOP ( 'NONE', ( #102699, #96935, #9082, #83028, #95602 ) ) ;
#42519=DIRECTION ( 'NONE',  ( -1.000000000000000000, -1.224606353822377258E-16, -0.000000000000000000 ) ) ;
#42527=DIRECTION ( 'NONE',  ( 0.000000000000000000, -1.000000000000000000, 0.000000000000000000 ) ) ;
#42529=CARTESIAN_POINT ( 'NONE',  ( 0.000000000000000000, 0.000000000000000000, 0.000000000000000000 ) ) ;
#42567=AXIS2_PLACEMENT_3D ( 'NONE', #41465, #16125, #88441 ) ;
#42573=ORIENTED_EDGE ( 'NONE', *, *, #69083, .T. ) ;
#42612=ORIENTED_EDGE ( 'NONE', *, *, #25850, .T. ) ;
#42645=VERTEX_POINT ( 'NONE', #72781 ) ;
#42726=ORIENTED_EDGE ( 'NONE', *, *, #39358, .F. ) ;
#42731=CARTESIAN_POINT ( 'NONE',  ( 67.22793774957824553, 6.975173280561618775E-15, 0.000000000000000000 ) ) ;
#42755=ORIENTED_EDGE ( 'NONE', *, *, #29584, .T. ) ;
#42820=AXIS2_PLACEMENT_3D ( 'NONE', #47120, #71394, #6665 ) ;
#42835=ADVANCED_FACE ( 'NONE', ( #70434 ), #75459, .T. ) ;
#42901=VECTOR ( 'NONE', #54725, 1000.000000000000000 ) ;
#42931=AXIS2_PLACEMENT_3D ( 'NONE', #45429, #88003, #103126 ) ;
#42950=DIRECTION ( 'NONE',  ( -0.000000000000000000, 0.5000000000000018874, 0.8660254037844375974 ) ) ;
#43032=CARTESIAN_POINT ( 'NONE',  ( 0.01372220897662087928, -5.948365447239591042, -2.697128823393874164 ) ) ;
#43049=DIRECTION ( 'NONE',  ( 0.000000000000000000, 0.000000000000000000, 1.000000000000000000 ) ) ;
#43063=ORIENTED_EDGE ( 'NONE', *, *, #23903, .F. ) ;
#43069=LINE ( 'NONE', #33941, #27287 ) ;
#43119=AXIS2_PLACEMENT_3D ( 'NONE', #74763, #60226, #29327 ) ;
#43140=DIRECTION ( 'NONE',  ( 0.000000000000000000, 0.000000000000000000, -1.000000000000000000 ) ) ;
#43153=CIRCLE ( 'NONE', #51683, 4.000000000000007105 ) ;
#43161=DIRECTION ( 'NONE',  ( -1.000000000000000000, -0.000000000000000000, -0.000000000000000000 ) ) ;
#43229=CARTESIAN_POINT ( 'NONE',  ( 68.70539558375507738, 4.898587196589294500E-16, -4.000000000000007105 ) ) ;
#43247=EDGE_LOOP ( 'NONE', ( #101794, #76494, #74704, #34579, #91076 ) ) ;
#43248=ADVANCED_FACE ( 'NONE', ( #28882 ), #22363, .T. ) ;
#43250=DIRECTION ( 'NONE',  ( -1.000000000000000000, -0.000000000000000000, -0.000000000000000000 ) ) ;
#43258=CIRCLE ( 'NONE', #81117, 4.000000000000007105 ) ;
#43260=CARTESIAN_POINT ( 'NONE',  ( 0.000000000000000000, 0.000000000000000000, 0.000000000000000000 ) ) ;
#43286=DIRECTION ( 'NONE',  ( -0.5735764363510494901, -0.8191520442889894671, 0.000000000000000000 ) ) ;
#43296=ADVANCED_FACE ( 'NONE', ( #53628 ), #38533, .T. ) ;
#43304=CYLINDRICAL_SURFACE ( 'NONE', #91451, 4.000000000000000000 ) ;
#43346=LINE ( 'NONE', #18559, #61617 ) ;
#43358=ORIENTED_EDGE ( 'NONE', *, *, #106628, .F. ) ;
#43365=DIRECTION ( 'NONE',  ( 0.5735764363510440500, 0.8191520442889932418, 0.000000000000000000 ) ) ;
#43371=DIRECTION ( 'NONE',  ( 0.000000000000000000, -1.000000000000000000, 0.000000000000000000 ) ) ;
#43376=EDGE_CURVE ( 'NONE', #14336, #55601, #27404, .T. ) ;
#43399=EDGE_CURVE ( 'NONE', #69704, #49330, #22216, .T. ) ;
#43414=CARTESIAN_POINT ( 'NONE',  ( 0.06682554136338086925, 6.264794173742279426, 2.149058192116893196 ) ) ;
#43449=ORIENTED_EDGE ( 'NONE', *, *, #20223, .T. ) ;
#43458=DIRECTION ( 'NONE',  ( 0.000000000000000000, 1.000000000000000000, 0.000000000000000000 ) ) ;
#43471=VERTEX_POINT ( 'NONE', #81593 ) ;
#43489=ORIENTED_EDGE ( 'NONE', *, *, #60833, .T. ) ;
#43507=ORIENTED_EDGE ( 'NONE', *, *, #48638, .F. ) ;
#43515=DIRECTION ( 'NONE',  ( 0.000000000000000000, -1.000000000000000000, 0.000000000000000000 ) ) ;
#43518=EDGE_CURVE ( 'NONE', #37118, #32281, #41167, .T. ) ;
#43524=CIRCLE ( 'NONE', #38613, 4.000000000000007105 ) ;
#43525=ADVANCED_FACE ( 'NONE', ( #56799 ), #25551, .T. ) ;
#43527=AXIS2_PLACEMENT_3D ( 'NONE', #34428, #16606, #8506 ) ;
#43531=DIRECTION ( 'NONE',  ( -1.000000000000000000, -1.224606353822377258E-16, -0.000000000000000000 ) ) ;
#43555=EDGE_CURVE ( 'NONE', #101359, #17114, #83728, .T. ) ;
#43589=DIRECTION ( 'NONE',  ( 0.000000000000000000, -1.000000000000000000, 0.000000000000000000 ) ) ;
#43619=VERTEX_POINT ( 'NONE', #76171 ) ;
#43626=ORIENTED_EDGE ( 'NONE', *, *, #1136, .T. ) ;
#43629=VERTEX_POINT ( 'NONE', #101527 ) ;
#43751=DIRECTION ( 'NONE',  ( 1.000000000000000000, 1.224606353822377258E-16, 0.000000000000000000 ) ) ;
#43774=CARTESIAN_POINT ( 'NONE',  ( 0.000000000000000000, 0.000000000000000000, 6.499999999999999112 ) ) ;
#43854=EDGE_CURVE ( 'NONE', #55070, #7738, #4419, .T. ) ;
#43859=ORIENTED_EDGE ( 'NONE', *, *, #52159, .F. ) ;
#43871=DIRECTION ( 'NONE',  ( 0.000000000000000000, -1.000000000000000000, 0.000000000000000000 ) ) ;
#43893=AXIS2_PLACEMENT_3D ( 'NONE', #17178, #106689, #84024 ) ;
#43896=CONICAL_SURFACE ( 'NONE', #47351, 3.309500000000007880, 0.9599310885968770357 ) ;
#43918=DIRECTION ( 'NONE',  ( 0.000000000000000000, 1.224646799147353207E-16, 1.000000000000000000 ) ) ;
#43942=LINE ( 'NONE', #68772, #84397 ) ;
#43976=ORIENTED_EDGE ( 'NONE', *, *, #4983, .T. ) ;
#44003=DIRECTION ( 'NONE',  ( 1.000000000000000000, 0.000000000000000000, -0.000000000000000000 ) ) ;
#44009=ORIENTED_EDGE ( 'NONE', *, *, #62678, .F. ) ;
#44063=EDGE_CURVE ( 'NONE', #105730, #23524, #59893, .T. ) ;
#44068=DIRECTION ( 'NONE',  ( 0.000000000000000000, 0.000000000000000000, 1.000000000000000000 ) ) ;
#44104=DIRECTION ( 'NONE',  ( -1.000000000000000000, -0.000000000000000000, -0.000000000000000000 ) ) ;
#44106=ADVANCED_FACE ( 'NONE', ( #18924 ), #75516, .T. ) ;
#44109=ORIENTED_EDGE ( 'NONE', *, *, #28438, .T. ) ;
#44114=AXIS2_PLACEMENT_3D ( 'NONE', #76935, #101742, #20889 ) ;
#44122=CIRCLE ( 'NONE', #1032, 3.309500000000007880 ) ;
#44127=ORIENTED_EDGE ( 'NONE', *, *, #68360, .F. ) ;
#44132=SURFACE_SIDE_STYLE ('',( #93206 ) ) ;
#44161=EDGE_CURVE ( 'NONE', #57904, #102866, #16882, .T. ) ;
#44165=CARTESIAN_POINT ( 'NONE',  ( 71.63333333333333997, 6.915964383211875250E-15, 0.000000000000000000 ) ) ;
#44172=FACE_OUTER_BOUND ( 'NONE', #9910, .T. ) ;
#44202=EDGE_CURVE ( 'NONE', #4022, #84731, #29020, .T. ) ;
#44233=ADVANCED_FACE ( 'NONE', ( #48970 ), #7450, .F. ) ;
#44271=DIRECTION ( 'NONE',  ( 0.000000000000000000, 0.000000000000000000, -1.000000000000000000 ) ) ;
#44275=CIRCLE ( 'NONE', #104543, 4.000000000000007105 ) ;
#44313=ORIENTED_EDGE ( 'NONE', *, *, #31886, .F. ) ;
#44349=DIRECTION ( 'NONE',  ( -1.000000000000000000, -1.224606353822377258E-16, -0.000000000000000000 ) ) ;
#44363=B_SPLINE_CURVE_WITH_KNOTS ( 'NONE', 3,
 ( #85188, #103497, #102436, #35611, #19445, #28578 ),
 .UNSPECIFIED., .F., .F.,
 ( 4, 2, 4 ),
 ( 2.380733003134763523E-07, 0.001898835937927384606, 0.003797433802554455416 ),
 .UNSPECIFIED. ) ;
#44472=DIRECTION ( 'NONE',  ( 0.000000000000000000, 1.000000000000000000, 0.000000000000000000 ) ) ;
#44473=EDGE_CURVE ( 'NONE', #87774, #53571, #27311, .T. ) ;
#44496=ORIENTED_EDGE ( 'NONE', *, *, #51112, .T. ) ;
#44514=CARTESIAN_POINT ( 'NONE',  ( 5.700000000000000178, 0.000000000000000000, 0.000000000000000000 ) ) ;
#44519=AXIS2_PLACEMENT_3D ( 'NONE', #64651, #105113, #106148 ) ;
#44520=DIRECTION ( 'NONE',  ( 0.000000000000000000, 0.000000000000000000, 1.000000000000000000 ) ) ;
#44590=ORIENTED_EDGE ( 'NONE', *, *, #86440, .T. ) ;
#44616=LINE ( 'NONE', #20916, #101888 ) ;
#44619=DIRECTION ( 'NONE',  ( 0.000000000000000000, -1.000000000000000000, 0.000000000000000000 ) ) ;
#44648=DIRECTION ( 'NONE',  ( 0.000000000000000000, -1.000000000000000000, 0.000000000000000000 ) ) ;
#44656=ADVANCED_FACE ( 'NONE', ( #16768 ), #31910, .T. ) ;
#44708=DIRECTION ( 'NONE',  ( 0.000000000000000000, -1.000000000000000000, 0.000000000000000000 ) ) ;
#44743=EDGE_LOOP ( 'NONE', ( #29059, #14429, #67450, #19384, #5067, #8251 ) ) ;
#44775=ORIENTED_EDGE ( 'NONE', *, *, #10630, .F. ) ;
#44881=DIRECTION ( 'NONE',  ( 1.000000000000000000, 1.224606353822377258E-16, 0.000000000000000000 ) ) ;
#44904=ORIENTED_EDGE ( 'NONE', *, *, #62879, .T. ) ;
#44927=CIRCLE ( 'NONE', #69029, 4.000000000000007105 ) ;
#44946=EDGE_CURVE ( 'NONE', #49330, #56292, #97928, .T. ) ;
#44950=VERTEX_POINT ( 'NONE', #103010 ) ;
#45002=DIRECTION ( 'NONE',  ( 0.000000000000000000, 0.000000000000000000, 1.000000000000000000 ) ) ;
#45010=EDGE_CURVE ( 'NONE', #21775, #79502, #15316, .T. ) ;
#45058=CARTESIAN_POINT ( 'NONE',  ( 66.00571552735603120, -4.000000000000000000, 4.898587196589421703E-16 ) ) ;
#45078=AXIS2_PLACEMENT_3D ( 'NONE', #53222, #19836, #44068 ) ;
#45115=AXIS2_PLACEMENT_3D ( 'NONE', #65215, #31802, #6430 ) ;
#45118=LINE ( 'NONE', #30002, #12902 ) ;
#45138=ADVANCED_FACE ( 'NONE', ( #40382 ), #57608, .T. ) ;
#45176=VERTEX_POINT ( 'NONE', #60321 ) ;
#45206=FILL_AREA_STYLE ('',( #3673 ) ) ;
#45224=ORIENTED_EDGE ( 'NONE', *, *, #101942, .F. ) ;
#45235=B_SPLINE_CURVE_WITH_KNOTS ( 'NONE', 3,
 ( #93782, #37713, #21003, #86774, #36649, #101865 ),
 .UNSPECIFIED., .F., .F.,
 ( 4, 2, 4 ),
 ( 0.02294124189247799192, 0.02484059228080997411, 0.02673994266914195284 ),
 .UNSPECIFIED. ) ;
#45242=ORIENTED_EDGE ( 'NONE', *, *, #46140, .F. ) ;
#45256=DIRECTION ( 'NONE',  ( 0.000000000000000000, -1.000000000000000000, 0.000000000000000000 ) ) ;
#45277=DIRECTION ( 'NONE',  ( -1.000000000000000000, -1.224606353822377258E-16, -0.000000000000000000 ) ) ;
#45287=DIRECTION ( 'NONE',  ( 0.000000000000000000, 0.000000000000000000, 1.000000000000000000 ) ) ;
#45377=AXIS2_PLACEMENT_3D ( 'NONE', #1626, #99806, #41573 ) ;
#45411=ORIENTED_EDGE ( 'NONE', *, *, #21263, .F. ) ;
#45422=DIRECTION ( 'NONE',  ( -1.000000000000000000, -0.000000000000000000, -0.000000000000000000 ) ) ;
#45429=CARTESIAN_POINT ( 'NONE',  ( 70.41111111111112564, 6.915964383211875250E-15, 0.000000000000000000 ) ) ;
#45474=CARTESIAN_POINT ( 'NONE',  ( 60.63333333333333286, 6.915964383211875250E-15, 0.000000000000000000 ) ) ;
#45483=DIRECTION ( 'NONE',  ( 0.000000000000000000, -1.000000000000000000, 0.000000000000000000 ) ) ;
#45500=ORIENTED_EDGE ( 'NONE', *, *, #5611, .T. ) ;
#45528=ADVANCED_FACE ( 'NONE', ( #33790 ), #67212, .T. ) ;
#45536=ORIENTED_EDGE ( 'NONE', *, *, #84689, .F. ) ;
#45544=EDGE_CURVE ( 'NONE', #106169, #41106, #27535, .T. ) ;
#45587=ORIENTED_EDGE ( 'NONE', *, *, #67541, .T. ) ;
#45615=FACE_OUTER_BOUND ( 'NONE', #38605, .T. ) ;
#45622=ORIENTED_EDGE ( 'NONE', *, *, #38929, .F. ) ;
#45646=EDGE_LOOP ( 'NONE', ( #105055, #7886, #7430, #32938, #91842 ) ) ;
#45649=EDGE_LOOP ( 'NONE', ( #30665, #9479, #106120, #22966, #80289 ) ) ;
#45670=VECTOR ( 'NONE', #35534, 1000.000000000000000 ) ;
#45714=CARTESIAN_POINT ( 'NONE',  ( 52.81650669486619165, -4.000000000000000000, 0.000000000000000000 ) ) ;
#45766=DIRECTION ( 'NONE',  ( -1.000000000000000000, -1.224606353822377258E-16, -0.000000000000000000 ) ) ;
#45781=CARTESIAN_POINT ( 'NONE',  ( 0.06682554136337581774, -4.993536075455411449, 4.350941807883112133 ) ) ;
#45815=AXIS2_PLACEMENT_3D ( 'NONE', #69741, #53551, #19104 ) ;
#45828=CARTESIAN_POINT ( 'NONE',  ( 0.000000000000000000, -5.629165124598853431, -3.249999999999994227 ) ) ;
#45832=DIRECTION ( 'NONE',  ( 0.000000000000000000, 0.000000000000000000, 1.000000000000000000 ) ) ;
#45845=EDGE_LOOP ( 'NONE', ( #57116, #87497, #2714, #43507 ) ) ;
#45878=B_SPLINE_CURVE_WITH_KNOTS ( 'NONE', 3,
 ( #42053, #5839, #13924, #45781, #70592, #38250, #71113, #4793 ),
 .UNSPECIFIED., .F., .F.,
 ( 4, 2, 2, 4 ),
 ( 0.003797433802554455416, 0.004743183970586251769, 0.005688934138618045519, 0.007580434474681635622 ),
 .UNSPECIFIED. ) ;
#45881=VERTEX_POINT ( 'NONE', #82465 ) ;
#45884=DIRECTION ( 'NONE',  ( -1.000000000000000000, -1.224606353822377258E-16, -0.000000000000000000 ) ) ;
#45929=DIRECTION ( 'NONE',  ( 0.000000000000000000, -1.000000000000000000, 0.000000000000000000 ) ) ;
#45956=ORIENTED_EDGE ( 'NONE', *, *, #16808, .F. ) ;
#45997=CARTESIAN_POINT ( 'NONE',  ( 0.000000000000000000, 0.000000000000000000, 0.000000000000000000 ) ) ;
#46011=ADVANCED_FACE ( 'NONE', ( #25878 ), #9620, .T. ) ;
#46015=DIRECTION ( 'NONE',  ( -1.000000000000000000, -1.224606353822377258E-16, -0.000000000000000000 ) ) ;
#46029=ORIENTED_EDGE ( 'NONE', *, *, #72290, .T. ) ;
#46055=B_SPLINE_CURVE_WITH_KNOTS ( 'NONE', 3,
 ( #83160, #77197, #26564, #26045, #59436, #9256 ),
 .UNSPECIFIED., .F., .F.,
 ( 4, 2, 4 ),
 ( 0.01913986446880882805, 0.02104055318064340999, 0.02294124189247799192 ),
 .UNSPECIFIED. ) ;
#46135=AXIS2_PLACEMENT_3D ( 'NONE', #24665, #80738, #82342 ) ;
#46136=CARTESIAN_POINT ( 'NONE',  ( 75.30000000000001137, 0.000000000000000000, 0.000000000000000000 ) ) ;
#46139=PLANE ( 'NONE',  #61151 ) ;
#46140=EDGE_CURVE ( 'NONE', #44950, #30745, #68927, .T. ) ;
#46190=CARTESIAN_POINT ( 'NONE',  ( 0.05613245601036537941, 1.278525034529256699, 6.499999999999999112 ) ) ;
#46215=LINE ( 'NONE', #71530, #82690 ) ;
#46236=ADVANCED_FACE ( 'NONE', ( #86215 ), #79220, .T. ) ;
#46253=ORIENTED_EDGE ( 'NONE', *, *, #69880, .T. ) ;
#46266=CARTESIAN_POINT ( 'NONE',  ( 69.18888888888888289, 6.915964383211875250E-15, 0.000000000000000000 ) ) ;
#46292=DIRECTION ( 'NONE',  ( 0.000000000000000000, 0.000000000000000000, 1.000000000000000000 ) ) ;
#46293=VECTOR ( 'NONE', #74047, 1000.000000000000000 ) ;
#46343=AXIS2_PLACEMENT_3D ( 'NONE', #63057, #6388, #45287 ) ;
#46376=ORIENTED_EDGE ( 'NONE', *, *, #50377, .T. ) ;
#46377=DIRECTION ( 'NONE',  ( 0.000000000000000000, -1.000000000000000000, 0.000000000000000000 ) ) ;
#46413=ORIENTED_EDGE ( 'NONE', *, *, #29080, .F. ) ;
#46464=DIRECTION ( 'NONE',  ( 1.000000000000000000, 0.000000000000000000, -0.000000000000000000 ) ) ;
#46477=ADVANCED_FACE ( 'NONE', ( #9494 ), #58676, .T. ) ;
#46484=EDGE_CURVE ( 'NONE', #81058, #82447, #82872, .T. ) ;
#46509=EDGE_LOOP ( 'NONE', ( #47358, #93658, #102968 ) ) ;
#46531=VECTOR ( 'NONE', #29656, 1000.000000000000000 ) ;
#46537=ORIENTED_EDGE ( 'NONE', *, *, #26774, .F. ) ;
#46564=AXIS2_PLACEMENT_3D ( 'NONE', #26211, #34286, #37483 ) ;
#46569=CARTESIAN_POINT ( 'NONE',  ( 75.30000000000001137, 0.000000000000000000, 0.000000000000000000 ) ) ;
#46585=CARTESIAN_POINT ( 'NONE',  ( 55.26095113931063452, 6.856755485862130937E-15, 0.000000000000000000 ) ) ;
#46627=ORIENTED_EDGE ( 'NONE', *, *, #51259, .F. ) ;
#46635=ORIENTED_EDGE ( 'NONE', *, *, #53034, .F. ) ;
#46724=ORIENTED_EDGE ( 'NONE', *, *, #105016, .F. ) ;
#46755=DIRECTION ( 'NONE',  ( 0.000000000000000000, -1.000000000000000000, 0.000000000000000000 ) ) ;
#46812=CARTESIAN_POINT ( 'NONE',  ( 56.22793774957824553, -1.232595164407830946E-29, 4.000000000000007105 ) ) ;
#46830=ORIENTED_EDGE ( 'NONE', *, *, #50537, .T. ) ;
#46833=DIRECTION ( 'NONE',  ( -1.000000000000000000, -1.224606353822377258E-16, -0.000000000000000000 ) ) ;
#46874=DIRECTION ( 'NONE',  ( -1.000000000000000000, -1.224606353822377258E-16, -0.000000000000000000 ) ) ;
#46884=AXIS2_PLACEMENT_3D ( 'NONE', #61058, #37870, #45929 ) ;
#46954=DIRECTION ( 'NONE',  ( -0.5735764363510497121, 0.8191520442889892450, 1.003171929053521665E-16 ) ) ;
#46979=LINE ( 'NONE', #71777, #90703 ) ;
#47032=CYLINDRICAL_SURFACE ( 'NONE', #49250, 4.000000000000000000 ) ;
#47035=VECTOR ( 'NONE', #12095, 1000.000000000000000 ) ;
#47052=ADVANCED_FACE ( 'NONE', ( #39909 ), #60463, .T. ) ;
#47084=ORIENTED_EDGE ( 'NONE', *, *, #10560, .F. ) ;
#47120=CARTESIAN_POINT ( 'NONE',  ( 0.000000000000000000, 0.000000000000000000, 0.000000000000000000 ) ) ;
#47144=CARTESIAN_POINT ( 'NONE',  ( 64.78349330513380266, 4.000000000000014211, 0.000000000000000000 ) ) ;
#47158=VERTEX_POINT ( 'NONE', #102387 ) ;
#47162=CARTESIAN_POINT ( 'NONE',  ( 0.000000000000000000, 4.898587196589412829E-16, -4.000000000000000000 ) ) ;
#47174=AXIS2_PLACEMENT_3D ( 'NONE', #99970, #68697, #101036 ) ;
#47186=DIRECTION ( 'NONE',  ( 0.000000000000000000, -1.000000000000000000, 0.000000000000000000 ) ) ;
#47196=VECTOR ( 'NONE', #31147, 1000.000000000000000 ) ;
#47260=AXIS2_PLACEMENT_3D ( 'NONE', #51234, #27023, #68520 ) ;
#47313=CARTESIAN_POINT ( 'NONE',  ( 0.000000000000000000, 0.000000000000000000, 0.000000000000000000 ) ) ;
#47335=LINE ( 'NONE', #87287, #61571 ) ;
#47351=AXIS2_PLACEMENT_3D ( 'NONE', #92446, #25645, #17526 ) ;
#47358=ORIENTED_EDGE ( 'NONE', *, *, #60882, .T. ) ;
#47366=EDGE_LOOP ( 'NONE', ( #989, #77140, #79299, #45536, #100016 ) ) ;
#47373=DIRECTION ( 'NONE',  ( 1.000000000000000000, 1.224606353822377258E-16, 0.000000000000000000 ) ) ;
#47389=ADVANCED_FACE ( 'NONE', ( #22571 ), #27769, .T. ) ;
#47441=FACE_OUTER_BOUND ( 'NONE', #4182, .T. ) ;
#47446=DIRECTION ( 'NONE',  ( 1.000000000000000000, 0.000000000000000000, -0.000000000000000000 ) ) ;
#47495=FACE_OUTER_BOUND ( 'NONE', #33142, .T. ) ;
#47527=ORIENTED_EDGE ( 'NONE', *, *, #21689, .F. ) ;
#47548=DIRECTION ( 'NONE',  ( 0.000000000000000000, -1.000000000000000000, 0.000000000000000000 ) ) ;
#47563=CARTESIAN_POINT ( 'NONE',  ( 58.67238219402268840, -4.000000000000000888, 4.898587196589422689E-16 ) ) ;
#47614=EDGE_LOOP ( 'NONE', ( #12596, #85575, #45500 ) ) ;
#47617=ORIENTED_EDGE ( 'NONE', *, *, #5781, .F. ) ;
#47690=CARTESIAN_POINT ( 'NONE',  ( 70.89460441624491693, -1.232595164407830946E-29, 4.000000000000007105 ) ) ;
#47697=CARTESIAN_POINT ( 'NONE',  ( 58.92761780597729881, 6.856755485862130937E-15, 0.000000000000000000 ) ) ;
#47700=EDGE_CURVE ( 'NONE', #2917, #32311, #10533, .T. ) ;
#47738=VERTEX_POINT ( 'NONE', #62883 ) ;
#47751=CIRCLE ( 'NONE', #85657, 6.499999999999999112 ) ;
#47793=DIRECTION ( 'NONE',  ( -1.000000000000000000, -0.000000000000000000, -0.000000000000000000 ) ) ;
#47800=CONICAL_SURFACE ( 'NONE', #77084, 6.499999999999999112, 1.047197551196600296 ) ;
#47835=CARTESIAN_POINT ( 'NONE',  ( 0.5805565836007654523, 7.505553499465139389, 1.865978384307260116E-16 ) ) ;
#47838=ORIENTED_EDGE ( 'NONE', *, *, #66029, .T. ) ;
#47878=DIRECTION ( 'NONE',  ( 1.000000000000000000, 0.000000000000000000, 0.000000000000000000 ) ) ;
#47880=CARTESIAN_POINT ( 'NONE',  ( 63.56127108291158123, 6.975173280561618775E-15, 0.000000000000000000 ) ) ;
#47896=ADVANCED_FACE ( 'NONE', ( #37575 ), #70440, .T. ) ;
#47904=LINE ( 'NONE', #98060, #105032 ) ;
#47909=CARTESIAN_POINT ( 'NONE',  ( 69.92761780597730592, 6.856755485862130937E-15, 0.000000000000000000 ) ) ;
#48006=CARTESIAN_POINT ( 'NONE',  ( 74.56127108291157413, -4.000000000000000000, 4.898587196589421703E-16 ) ) ;
#48029=EDGE_CURVE ( 'NONE', #90738, #72747, #81674, .T. ) ;
#48051=CARTESIAN_POINT ( 'NONE',  ( 4.699999999999999289, 6.499999999999999112, 0.000000000000000000 ) ) ;
#48067=ORIENTED_EDGE ( 'NONE', *, *, #8222, .F. ) ;
#48097=CARTESIAN_POINT ( 'NONE',  ( 64.78349330513380266, -4.000000000000000888, 4.898587196589422689E-16 ) ) ;
#48122=DIRECTION ( 'NONE',  ( -1.000000000000000000, -1.224606353822377258E-16, -0.000000000000000000 ) ) ;
#48127=EDGE_CURVE ( 'NONE', #76519, #39308, #87421, .T. ) ;
#48134=DIRECTION ( 'NONE',  ( -1.000000000000000000, -1.224606353822377258E-16, -0.000000000000000000 ) ) ;
#48140=DIRECTION ( 'NONE',  ( 0.5735764363510440500, 0.8191520442889932418, 0.000000000000000000 ) ) ;
#48176=DIRECTION ( 'NONE',  ( 0.000000000000000000, -1.000000000000000000, 0.000000000000000000 ) ) ;
#48192=DIRECTION ( 'NONE',  ( 0.000000000000000000, 1.000000000000000000, 0.000000000000000000 ) ) ;
#48201=CARTESIAN_POINT ( 'NONE',  ( 63.56127108291158123, 6.975173280561618775E-15, 0.000000000000000000 ) ) ;
#48210=CARTESIAN_POINT ( 'NONE',  ( 74.56127108291157413, -4.000000000000000888, 4.898587196589422689E-16 ) ) ;
#48256=ORIENTED_EDGE ( 'NONE', *, *, #102318, .F. ) ;
#48278=ORIENTED_EDGE ( 'NONE', *, *, #56497, .F. ) ;
#48288=ADVANCED_FACE ( 'NONE', ( #70310 ), #47800, .T. ) ;
#48307=CARTESIAN_POINT ( 'NONE',  ( 61.85555555555556140, 6.915964383211875250E-15, 0.000000000000000000 ) ) ;
#48334=FACE_OUTER_BOUND ( 'NONE', #70858, .T. ) ;
#48389=VERTEX_POINT ( 'NONE', #79969 ) ;
#48399=CARTESIAN_POINT ( 'NONE',  ( 69.67238219402268840, -1.232595164407830946E-29, 4.000000000000007105 ) ) ;
#48440=CIRCLE ( 'NONE', #32935, 6.499999999999999112 ) ;
#48480=CARTESIAN_POINT ( 'NONE',  ( 69.18888888888888289, 6.915964383211875250E-15, 0.000000000000000000 ) ) ;
#48560=FILL_AREA_STYLE ('',( #89574 ) ) ;
#48581=ORIENTED_EDGE ( 'NONE', *, *, #64374, .F. ) ;
#48588=LINE ( 'NONE', #39991, #3840 ) ;
#48600=ADVANCED_BREP_SHAPE_REPRESENTATION ( '', ( #19502, #10728 ), #66175 ) ;
#48638=EDGE_CURVE ( 'NONE', #45881, #34259, #15497, .T. ) ;
#48665=CIRCLE ( 'NONE', #5638, 4.000000000000007105 ) ;
#48684=ORIENTED_EDGE ( 'NONE', *, *, #20017, .T. ) ;
#48705=CARTESIAN_POINT ( 'NONE',  ( 66.74444444444444002, 6.915964383211875250E-15, 0.000000000000000000 ) ) ;
#48743=DIRECTION ( 'NONE',  ( -1.000000000000000000, -1.224606353822377258E-16, -0.000000000000000000 ) ) ;
#48750=CIRCLE ( 'NONE', #2253, 4.000000000000007105 ) ;
#48810=ORIENTED_EDGE ( 'NONE', *, *, #73688, .F. ) ;
#48844=ORIENTED_EDGE ( 'NONE', *, *, #50377, .F. ) ;
#48875=CIRCLE ( 'NONE', #62690, 6.499999999999999112 ) ;
#48882=LINE ( 'NONE', #50478, #30802 ) ;
#48896=CARTESIAN_POINT ( 'NONE',  ( 0.05533025579361913748, 6.264553569211839701, -2.149474931388137833 ) ) ;
#48917=ORIENTED_EDGE ( 'NONE', *, *, #34332, .F. ) ;
#48970=FACE_OUTER_BOUND ( 'NONE', #9096, .T. ) ;
#48995=ORIENTED_EDGE ( 'NONE', *, *, #20223, .F. ) ;
#49078=ORIENTED_EDGE ( 'NONE', *, *, #23592, .T. ) ;
#49095=CIRCLE ( 'NONE', #90472, 4.000000000000007105 ) ;
#49096=AXIS2_PLACEMENT_3D ( 'NONE', #80334, #40420, #6447 ) ;
#49110=DIRECTION ( 'NONE',  ( 1.000000000000000000, 0.000000000000000000, 0.000000000000000000 ) ) ;
#49143=ORIENTED_EDGE ( 'NONE', *, *, #38488, .T. ) ;
#49167=AXIS2_PLACEMENT_3D ( 'NONE', #20194, #21246, #28817 ) ;
#49179=CIRCLE ( 'NONE', #18201, 4.000000000000007105 ) ;
#49189=AXIS2_PLACEMENT_3D ( 'NONE', #71379, #37476, #44472 ) ;
#49219=DIRECTION ( 'NONE',  ( -0.7071067811865314745, 8.659560562355128841E-17, -0.7071067811865635599 ) ) ;
#49229=CONICAL_SURFACE ( 'NONE', #9578, 3.309500000000007880, 0.9599310885968770357 ) ;
#49235=DIRECTION ( 'NONE',  ( -1.000000000000000000, -1.224606353822377258E-16, -0.000000000000000000 ) ) ;
#49250=AXIS2_PLACEMENT_3D ( 'NONE', #45997, #78346, #71841 ) ;
#49253=FACE_OUTER_BOUND ( 'NONE', #34545, .T. ) ;
#49256=ORIENTED_EDGE ( 'NONE', *, *, #60293, .T. ) ;
#49299=CARTESIAN_POINT ( 'NONE',  ( 64.29999999999999716, 6.915964383211875250E-15, 0.000000000000000000 ) ) ;
#49303=CARTESIAN_POINT ( 'NONE',  ( 68.45015997180047407, 4.000000000000013323, 0.000000000000000000 ) ) ;
#49330=VERTEX_POINT ( 'NONE', #49303 ) ;
#49373=DIRECTION ( 'NONE',  ( 0.000000000000000000, -1.000000000000000000, 0.000000000000000000 ) ) ;
#49464=DIRECTION ( 'NONE',  ( 1.000000000000000000, 0.000000000000000000, -0.000000000000000000 ) ) ;
#49535=LINE ( 'NONE', #39869, #66352 ) ;
#49595=CARTESIAN_POINT ( 'NONE',  ( 4.699999999999999289, 6.499999999999999112, 0.000000000000000000 ) ) ;
#49596=AXIS2_PLACEMENT_3D ( 'NONE', #77596, #68985, #101339 ) ;
#49615=CONICAL_SURFACE ( 'NONE', #106426, 4.000000000000007105, 0.9599310885968835860 ) ;
#49675=DIRECTION ( 'NONE',  ( 0.000000000000000000, -1.000000000000000000, 0.000000000000000000 ) ) ;
#49693=ORIENTED_EDGE ( 'NONE', *, *, #91217, .T. ) ;
#49745=AXIS2_PLACEMENT_3D ( 'NONE', #64911, #23413, #32030 ) ;
#49778=CARTESIAN_POINT ( 'NONE',  ( 0.000000000000000000, 0.000000000000000000, 4.000000000000000000 ) ) ;
#49787=DIRECTION ( 'NONE',  ( 0.000000000000000000, -0.8660254037844383745, -0.5000000000000004441 ) ) ;
#49819=EDGE_LOOP ( 'NONE', ( #48067, #24038, #87975, #99834, #24163 ) ) ;
#49849=ORIENTED_EDGE ( 'NONE', *, *, #3927, .T. ) ;
#49864=DIRECTION ( 'NONE',  ( 0.000000000000000000, -1.000000000000000000, 0.000000000000000000 ) ) ;
#49937=DIRECTION ( 'NONE',  ( -1.000000000000000000, -0.000000000000000000, -0.000000000000000000 ) ) ;
#49949=ORIENTED_EDGE ( 'NONE', *, *, #5622, .T. ) ;
#49977=DIRECTION ( 'NONE',  ( 0.000000000000000000, -1.000000000000000000, 0.000000000000000000 ) ) ;
#50019=EDGE_CURVE ( 'NONE', #75420, #33265, #34391, .T. ) ;
#50051=AXIS2_PLACEMENT_3D ( 'NONE', #1431, #33312, #66184 ) ;
#50056=EDGE_CURVE ( 'NONE', #17114, #93530, #22536, .T. ) ;
#50060=ADVANCED_FACE ( 'NONE', ( #82904 ), #84569, .T. ) ;
#50078=CARTESIAN_POINT ( 'NONE',  ( 0.000000000000000000, 0.000000000000000000, 4.000000000000000000 ) ) ;
#50186=VERTEX_POINT ( 'NONE', #53203 ) ;
#50201=EDGE_CURVE ( 'NONE', #23441, #2917, #12181, .T. ) ;
#50208=DIRECTION ( 'NONE',  ( -1.000000000000000000, -1.224606353822377258E-16, -0.000000000000000000 ) ) ;
#50220=ORIENTED_EDGE ( 'NONE', *, *, #60882, .F. ) ;
#50234=DIRECTION ( 'NONE',  ( 0.000000000000000000, -1.000000000000000000, 0.000000000000000000 ) ) ;
#50314=CARTESIAN_POINT ( 'NONE',  ( 61.11682663846713837, 6.975173280561618775E-15, 0.000000000000000000 ) ) ;
#50325=CARTESIAN_POINT ( 'NONE',  ( 71.14984002819953446, 6.856755485862130937E-15, 0.000000000000000000 ) ) ;
#50377=EDGE_CURVE ( 'NONE', #43629, #85509, #63434, .T. ) ;
#50457=FACE_OUTER_BOUND ( 'NONE', #86721, .T. ) ;
#50467=DIRECTION ( 'NONE',  ( 0.000000000000000000, -1.000000000000000000, 0.000000000000000000 ) ) ;
#50478=CARTESIAN_POINT ( 'NONE',  ( 0.000000000000000000, 4.898587196589412829E-16, -4.000000000000000000 ) ) ;
#50496=ORIENTED_EDGE ( 'NONE', *, *, #4287, .F. ) ;
#50537=EDGE_CURVE ( 'NONE', #12701, #11751, #69104, .T. ) ;
#50565=FACE_OUTER_BOUND ( 'NONE', #5880, .T. ) ;
#50573=CYLINDRICAL_SURFACE ( 'NONE', #79247, 4.000000000000000000 ) ;
#50589=DIRECTION ( 'NONE',  ( 0.000000000000000000, -1.000000000000000000, 0.000000000000000000 ) ) ;
#50592=STYLED_ITEM ( 'NONE', ( #65289 ), #48600 ) ;
#50605=ORIENTED_EDGE ( 'NONE', *, *, #29997, .T. ) ;
#50622=VERTEX_POINT ( 'NONE', #39553 ) ;
#50641=DIRECTION ( 'NONE',  ( 0.000000000000000000, -1.000000000000000000, 0.000000000000000000 ) ) ;
#50661=DIRECTION ( 'NONE',  ( 1.000000000000000000, 0.000000000000000000, 0.000000000000000000 ) ) ;
#50669=VECTOR ( 'NONE', #3198, 1000.000000000000000 ) ;
#50701=DIRECTION ( 'NONE',  ( 0.000000000000000000, -1.000000000000000000, 0.000000000000000000 ) ) ;
#50709=ORIENTED_EDGE ( 'NONE', *, *, #61966, .T. ) ;
#50761=ORIENTED_EDGE ( 'NONE', *, *, #53045, .T. ) ;
#50774=ORIENTED_EDGE ( 'NONE', *, *, #88212, .T. ) ;
#50776=CONICAL_SURFACE ( 'NONE', #83508, 4.000000000000007105, 0.9599310885968835860 ) ;
#50779=EDGE_CURVE ( 'NONE', #87625, #36600, #31477, .T. ) ;
#50800=EDGE_CURVE ( 'NONE', #53314, #13515, #71360, .T. ) ;
#50885=DIRECTION ( 'NONE',  ( 0.000000000000000000, 1.000000000000000000, 0.000000000000000000 ) ) ;
#50892=PRODUCT_DEFINITION ( 'UNKNOWN', '', #66242, #89899 ) ;
#50895=CARTESIAN_POINT ( 'NONE',  ( 73.33904886068935980, 6.975173280561618775E-15, 0.000000000000000000 ) ) ;
#50907=DIRECTION ( 'NONE',  ( -1.000000000000000000, -1.224606353822377258E-16, -0.000000000000000000 ) ) ;
#50915=FACE_OUTER_BOUND ( 'NONE', #84250, .T. ) ;
#50946=LINE ( 'NONE', #68771, #6819 ) ;
#50958=ORIENTED_EDGE ( 'NONE', *, *, #76890, .F. ) ;
#51048=ORIENTED_EDGE ( 'NONE', *, *, #102935, .T. ) ;
#51098=CIRCLE ( 'NONE', #85557, 3.309500000000007880 ) ;
#51111=DIRECTION ( 'NONE',  ( 0.000000000000000000, -1.000000000000000000, 0.000000000000000000 ) ) ;
#51112=EDGE_CURVE ( 'NONE', #79502, #50622, #66875, .T. ) ;
#51116=DIRECTION ( 'NONE',  ( -1.000000000000000000, -0.000000000000000000, -0.000000000000000000 ) ) ;
#51147=VERTEX_POINT ( 'NONE', #16185 ) ;
#51161=ORIENTED_EDGE ( 'NONE', *, *, #51329, .T. ) ;
#51231=AXIS2_PLACEMENT_3D ( 'NONE', #7346, #1908, #43458 ) ;
#51234=CARTESIAN_POINT ( 'NONE',  ( 5.299999999999999822, 3.752776749732553263, -6.499999999999999112 ) ) ;
#51258=DIRECTION ( 'NONE',  ( 0.000000000000000000, -1.000000000000000000, 0.000000000000000000 ) ) ;
#51259=EDGE_CURVE ( 'NONE', #98861, #21000, #29622, .T. ) ;
#51329=EDGE_CURVE ( 'NONE', #93530, #30792, #17671, .T. ) ;
#51331=CONICAL_SURFACE ( 'NONE', #20385, 3.309500000000007880, 0.9599310885968770357 ) ;
#51342=CARTESIAN_POINT ( 'NONE',  ( 0.000000000000000000, 0.000000000000000000, 0.000000000000000000 ) ) ;
#51352=AXIS2_PLACEMENT_3D ( 'NONE', #31254, #89984, #96495 ) ;
#51357=LINE ( 'NONE', #53496, #79172 ) ;
#51426=DIRECTION ( 'NONE',  ( 1.000000000000000000, 1.224606353822377258E-16, 0.000000000000000000 ) ) ;
#51427=AXIS2_PLACEMENT_3D ( 'NONE', #36721, #70638, #54418 ) ;
#51437=ORIENTED_EDGE ( 'NONE', *, *, #17999, .F. ) ;
#51438=CYLINDRICAL_SURFACE ( 'NONE', #31412, 4.000000000000000000 ) ;
#51446=ORIENTED_EDGE ( 'NONE', *, *, #69880, .F. ) ;
#51449=LINE ( 'NONE', #33172, #58189 ) ;
#51451=DIRECTION ( 'NONE',  ( 0.000000000000000000, -1.000000000000000000, 0.000000000000000000 ) ) ;
#51454=EDGE_LOOP ( 'NONE', ( #8016, #11812, #25597, #104704, #80213, #24639 ) ) ;
#51481=DIRECTION ( 'NONE',  ( 0.000000000000000000, -1.000000000000000000, 0.000000000000000000 ) ) ;
#51532=FACE_OUTER_BOUND ( 'NONE', #52320, .T. ) ;
#51544=DIRECTION ( 'NONE',  ( 0.000000000000000000, -1.000000000000000000, 0.000000000000000000 ) ) ;
#51569=DIRECTION ( 'NONE',  ( -0.5735764363510497121, 0.8191520442889892450, 1.003171929053521665E-16 ) ) ;
#51626=DIRECTION ( 'NONE',  ( -1.000000000000000000, -1.224606353822377258E-16, -0.000000000000000000 ) ) ;
#51649=ORIENTED_EDGE ( 'NONE', *, *, #100243, .F. ) ;
#51652=AXIS2_PLACEMENT_3D ( 'NONE', #52024, #86023, #19185 ) ;
#51653=ORIENTED_EDGE ( 'NONE', *, *, #13119, .F. ) ;
#51668=EDGE_CURVE ( 'NONE', #97524, #32062, #2255, .T. ) ;
#51672=CARTESIAN_POINT ( 'NONE',  ( 59.41111111111111143, -3.309500000000000774, 4.475777889183797681E-16 ) ) ;
#51683=AXIS2_PLACEMENT_3D ( 'NONE', #77324, #77854, #76247 ) ;
#51728=CARTESIAN_POINT ( 'NONE',  ( 60.14984002819952025, 6.856755485862130937E-15, 0.000000000000000000 ) ) ;
#51778=DIRECTION ( 'NONE',  ( 0.000000000000000000, 0.000000000000000000, 1.000000000000000000 ) ) ;
#51894=CIRCLE ( 'NONE', #55348, 4.000000000000007105 ) ;
#51907=AXIS2_PLACEMENT_3D ( 'NONE', #12341, #52809, #11805 ) ;
#51999=CARTESIAN_POINT ( 'NONE',  ( 5.700000000000000178, 5.388445916248354013E-16, 4.400000000000000355 ) ) ;
#52022=EDGE_CURVE ( 'NONE', #38119, #29354, #96875, .T. ) ;
#52024=CARTESIAN_POINT ( 'NONE',  ( 66.26095113931063452, 6.856755485862130937E-15, 0.000000000000000000 ) ) ;
#52033=B_SPLINE_CURVE_WITH_KNOTS ( 'NONE', 3,
 ( #18241, #84016, #43032, #59756, #75921, #67832, #100722, #18791 ),
 .UNSPECIFIED., .F., .F.,
 ( 4, 2, 2, 4 ),
 ( 0.003797433802554441972, 0.004743183970586237891, 0.005688934138618033376, 0.007580434474681623479 ),
 .UNSPECIFIED. ) ;
#52078=ADVANCED_FACE ( 'NONE', ( #31650 ), #28159, .T. ) ;
#52144=CARTESIAN_POINT ( 'NONE',  ( 0.000000000000000000, 0.000000000000000000, 4.000000000000000000 ) ) ;
#52159=EDGE_CURVE ( 'NONE', #43619, #11977, #17582, .T. ) ;
#52168=DIRECTION ( 'NONE',  ( -1.000000000000000000, -0.000000000000000000, -0.000000000000000000 ) ) ;
#52171=CARTESIAN_POINT ( 'NONE',  ( 67.48317336153286305, -1.232595164407830946E-29, 4.000000000000007105 ) ) ;
#52174=ORIENTED_EDGE ( 'NONE', *, *, #104594, .T. ) ;
#52194=ORIENTED_EDGE ( 'NONE', *, *, #83343, .F. ) ;
#52213=CARTESIAN_POINT ( 'NONE',  ( 66.26095113931063452, 6.856755485862130937E-15, 0.000000000000000000 ) ) ;
#52302=CONICAL_SURFACE ( 'NONE', #2334, 3.309500000000007880, 0.9599310885968770357 ) ;
#52311=DIRECTION ( 'NONE',  ( 0.000000000000000000, -1.000000000000000000, 0.000000000000000000 ) ) ;
#52320=EDGE_LOOP ( 'NONE', ( #96472, #23097, #90782, #75396, #93224 ) ) ;
#52330=AXIS2_PLACEMENT_3D ( 'NONE', #2329, #67087, #74623 ) ;
#52361=CARTESIAN_POINT ( 'NONE',  ( 73.33904886068935980, -4.000000000000000000, 4.898587196589421703E-16 ) ) ;
#52371=DIRECTION ( 'NONE',  ( -0.5735764363510497121, 0.8191520442889892450, 1.003171929053521665E-16 ) ) ;
#52482=CARTESIAN_POINT ( 'NONE',  ( 57.70539558375507738, -4.000000000000000000, 0.000000000000000000 ) ) ;
#52493=EDGE_CURVE ( 'NONE', #54493, #54950, #78019, .T. ) ;
#52518=CARTESIAN_POINT ( 'NONE',  ( 0.000000000000000000, 0.000000000000000000, 0.000000000000000000 ) ) ;
#52587=DIRECTION ( 'NONE',  ( -1.000000000000000000, -0.000000000000000000, -0.000000000000000000 ) ) ;
#52591=DIRECTION ( 'NONE',  ( 0.000000000000000000, -1.000000000000000000, 0.000000000000000000 ) ) ;
#52615=VERTEX_POINT ( 'NONE', #91738 ) ;
#52671=ORIENTED_EDGE ( 'NONE', *, *, #48638, .T. ) ;
#52714=DIRECTION ( 'NONE',  ( 0.5735764363510440500, 0.8191520442889932418, 0.000000000000000000 ) ) ;
#52718=CARTESIAN_POINT ( 'NONE',  ( 72.85555555555556850, 6.915964383211875250E-15, 0.000000000000000000 ) ) ;
#52720=CARTESIAN_POINT ( 'NONE',  ( 74.07777777777778283, 6.915964383211875250E-15, 0.000000000000000000 ) ) ;
#52782=ORIENTED_EDGE ( 'NONE', *, *, #27418, .F. ) ;
#52795=CARTESIAN_POINT ( 'NONE',  ( 63.56127108291158123, 6.975173280561618775E-15, 0.000000000000000000 ) ) ;
#52809=DIRECTION ( 'NONE',  ( -1.000000000000000000, -0.000000000000000000, -0.000000000000000000 ) ) ;
#52850=DIRECTION ( 'NONE',  ( -1.000000000000000000, -0.000000000000000000, -0.000000000000000000 ) ) ;
#52864=EDGE_LOOP ( 'NONE', ( #78022, #78073, #3405, #22438, #34040, #56189 ) ) ;
#52966=AXIS2_PLACEMENT_3D ( 'NONE', #85104, #60845, #77007 ) ;
#53007=AXIS2_PLACEMENT_3D ( 'NONE', #9513, #42425, #75318 ) ;
#53034=EDGE_CURVE ( 'NONE', #59650, #34382, #79686, .T. ) ;
#53041=CIRCLE ( 'NONE', #23723, 3.309500000000007880 ) ;
#53045=EDGE_CURVE ( 'NONE', #58831, #70947, #43524, .T. ) ;
#53083=ADVANCED_FACE ( 'NONE', ( #5647 ), #76216, .T. ) ;
#53091=FACE_OUTER_BOUND ( 'NONE', #64718, .T. ) ;
#53102=DIRECTION ( 'NONE',  ( -1.000000000000000000, -0.000000000000000000, -0.000000000000000000 ) ) ;
#53105=FACE_OUTER_BOUND ( 'NONE', #43247, .T. ) ;
#53109=EDGE_CURVE ( 'NONE', #102808, #29354, #21340, .T. ) ;
#53112=AXIS2_PLACEMENT_3D ( 'NONE', #71992, #104904, #96810 ) ;
#53124=CONICAL_SURFACE ( 'NONE', #73743, 4.000000000000007105, 0.9599310885968835860 ) ;
#53178=EDGE_LOOP ( 'NONE', ( #75746, #92270, #43976, #79590, #101053 ) ) ;
#53198=CARTESIAN_POINT ( 'NONE',  ( 5.299999999999999822, 7.505553499465139389, -6.505213034913023646E-16 ) ) ;
#53203=CARTESIAN_POINT ( 'NONE',  ( 0.000000000000000000, -5.629165124598843661, 3.250000000000011990 ) ) ;
#53216=DIRECTION ( 'NONE',  ( 0.000000000000000000, -1.000000000000000000, 0.000000000000000000 ) ) ;
#53222=CARTESIAN_POINT ( 'NONE',  ( 0.000000000000000000, 0.000000000000000000, 0.000000000000000000 ) ) ;
#53231=AXIS2_PLACEMENT_3D ( 'NONE', #67747, #44003, #76888 ) ;
#53256=EDGE_CURVE ( 'NONE', #37041, #38119, #57270, .T. ) ;
#53314=VERTEX_POINT ( 'NONE', #2729 ) ;
#53378=EDGE_CURVE ( 'NONE', #59016, #103960, #48875, .T. ) ;
#53379=VERTEX_POINT ( 'NONE', #66953 ) ;
#53447=EDGE_LOOP ( 'NONE', ( #63615, #80398, #48581, #10808, #87688, #50220 ) ) ;
#53456=CARTESIAN_POINT ( 'NONE',  ( 0.000000000000000000, 4.898587196589412829E-16, -4.000000000000000000 ) ) ;
#53476=CIRCLE ( 'NONE', #98188, 4.000000000000007105 ) ;
#53485=DIRECTION ( 'NONE',  ( 0.000000000000000000, 0.000000000000000000, -1.000000000000000000 ) ) ;
#53490=ORIENTED_EDGE ( 'NONE', *, *, #43555, .F. ) ;
#53496=CARTESIAN_POINT ( 'NONE',  ( 60.63333333333333286, -3.309500000000000774, 0.000000000000000000 ) ) ;
#53551=DIRECTION ( 'NONE',  ( -1.000000000000000000, -1.224606353822377258E-16, -0.000000000000000000 ) ) ;
#53571=VERTEX_POINT ( 'NONE', #4336 ) ;
#53588=CARTESIAN_POINT ( 'NONE',  ( 0.000000000000000000, 0.000000000000000000, 0.000000000000000000 ) ) ;
#53597=LINE ( 'NONE', #11525, #71235 ) ;
#53604=AXIS2_PLACEMENT_3D ( 'NONE', #50314, #15831, #1206 ) ;
#53608=VECTOR ( 'NONE', #48140, 1000.000000000000000 ) ;
#53625=ORIENTED_EDGE ( 'NONE', *, *, #40202, .F. ) ;
#53628=FACE_OUTER_BOUND ( 'NONE', #98414, .T. ) ;
#53656=FACE_OUTER_BOUND ( 'NONE', #92567, .T. ) ;
#53685=CARTESIAN_POINT ( 'NONE',  ( 72.37206225042174879, 6.856755485862130937E-15, 0.000000000000000000 ) ) ;
#53703=VERTEX_POINT ( 'NONE', #80323 ) ;
#53704=EDGE_CURVE ( 'NONE', #96955, #80696, #98636, .T. ) ;
#53715=ORIENTED_EDGE ( 'NONE', *, *, #7810, .T. ) ;
#53735=ADVANCED_FACE ( 'NONE', ( #105671 ), #21220, .T. ) ;
#53743=CARTESIAN_POINT ( 'NONE',  ( 58.92761780597729881, 6.856755485862130937E-15, 0.000000000000000000 ) ) ;
#53772=ORIENTED_EDGE ( 'NONE', *, *, #65638, .T. ) ;
#53774=DIRECTION ( 'NONE',  ( 1.000000000000000000, 1.224606353822377258E-16, 0.000000000000000000 ) ) ;
#53783=AXIS2_PLACEMENT_3D ( 'NONE', #15699, #80431, #64278 ) ;
#53814=FACE_OUTER_BOUND ( 'NONE', #13422, .T. ) ;
#53838=DIRECTION ( 'NONE',  ( -1.000000000000000000, -1.224606353822377258E-16, -0.000000000000000000 ) ) ;
#53847=CARTESIAN_POINT ( 'NONE',  ( 0.05533025579362222529, 4.993776679985858280, 4.350525068611868384 ) ) ;
#53864=AXIS2_PLACEMENT_3D ( 'NONE', #21140, #64225, #63157 ) ;
#53902=ORIENTED_EDGE ( 'NONE', *, *, #79990, .F. ) ;
#54056=LINE ( 'NONE', #28795, #95388 ) ;
#54070=VECTOR ( 'NONE', #46954, 1000.000000000000000 ) ;
#54113=AXIS2_PLACEMENT_3D ( 'NONE', #6728, #88191, #14809 ) ;
#54138=CARTESIAN_POINT ( 'NONE',  ( 72.11682663846713126, 6.975173280561618775E-15, 0.000000000000000000 ) ) ;
#54164=CARTESIAN_POINT ( 'NONE',  ( 0.000000000000000000, 7.505553499465139389, -6.505213034913023646E-16 ) ) ;
#54178=DIRECTION ( 'NONE',  ( 0.000000000000000000, -1.000000000000000000, 0.000000000000000000 ) ) ;
#54194=CARTESIAN_POINT ( 'NONE',  ( 72.11682663846713126, 6.975173280561618775E-15, 0.000000000000000000 ) ) ;
#54220=DIRECTION ( 'NONE',  ( -1.000000000000000000, -1.224606353822377258E-16, -0.000000000000000000 ) ) ;
#54225=DIRECTION ( 'NONE',  ( 1.000000000000000000, 0.000000000000000000, -0.000000000000000000 ) ) ;
#54227=CARTESIAN_POINT ( 'NONE',  ( 5.700000000000000178, 0.000000000000000000, 0.000000000000000000 ) ) ;
#54256=CARTESIAN_POINT ( 'NONE',  ( 67.48317336153286305, 6.856755485862130937E-15, 0.000000000000000000 ) ) ;
#54276=ORIENTED_EDGE ( 'NONE', *, *, #16673, .F. ) ;
#54281=EDGE_CURVE ( 'NONE', #102808, #42645, #18160, .T. ) ;
#54289=CARTESIAN_POINT ( 'NONE',  ( 53.78349330513380266, -4.000000000000000888, 4.898587196589422689E-16 ) ) ;
#54345=EDGE_LOOP ( 'NONE', ( #99023, #46376, #37145, #52782, #58958 ) ) ;
#54360=CARTESIAN_POINT ( 'NONE',  ( 57.70539558375507738, 6.856755485862130937E-15, 0.000000000000000000 ) ) ;
#54369=EDGE_CURVE ( 'NONE', #38361, #7404, #42408, .T. ) ;
#54376=DIRECTION ( 'NONE',  ( -1.000000000000000000, -1.224606353822377258E-16, -0.000000000000000000 ) ) ;
#54404=DIRECTION ( 'NONE',  ( 0.000000000000000000, -1.000000000000000000, 0.000000000000000000 ) ) ;
#54418=DIRECTION ( 'NONE',  ( 0.000000000000000000, -1.000000000000000000, 0.000000000000000000 ) ) ;
#54468=EDGE_CURVE ( 'NONE', #34259, #45881, #16086, .T. ) ;
#54493=VERTEX_POINT ( 'NONE', #27552 ) ;
#54615=DIRECTION ( 'NONE',  ( 0.000000000000000000, -1.000000000000000000, 0.000000000000000000 ) ) ;
#54642=ORIENTED_EDGE ( 'NONE', *, *, #84789, .F. ) ;
#54655=AXIS2_PLACEMENT_3D ( 'NONE', #83817, #50907, #51451 ) ;
#54699=CONICAL_SURFACE ( 'NONE', #23721, 4.000000000000007105, 0.9599310885968835860 ) ;
#54712=CIRCLE ( 'NONE', #52966, 4.000000000000007105 ) ;
#54725=DIRECTION ( 'NONE',  ( -0.5735764363510494901, -0.8191520442889894671, 0.000000000000000000 ) ) ;
#54766=AXIS2_PLACEMENT_3D ( 'NONE', #57529, #331, #74255 ) ;
#54784=DIRECTION ( 'NONE',  ( -1.000000000000000000, -1.224606353822377258E-16, -0.000000000000000000 ) ) ;
#54829=VERTEX_POINT ( 'NONE', #103261 ) ;
#54832=DIRECTION ( 'NONE',  ( -1.000000000000000000, -1.224606353822377258E-16, -0.000000000000000000 ) ) ;
#54844=VERTEX_POINT ( 'NONE', #103781 ) ;
#54950=VERTEX_POINT ( 'NONE', #71406 ) ;
#55028=EDGE_CURVE ( 'NONE', #63428, #105869, #58960, .T. ) ;
#55070=VERTEX_POINT ( 'NONE', #96099 ) ;
#55081=CIRCLE ( 'NONE', #105087, 6.499999999999999112 ) ;
#55118=VERTEX_POINT ( 'NONE', #5494 ) ;
#55126=AXIS2_PLACEMENT_3D ( 'NONE', #11176, #44104, #76995 ) ;
#55155=CARTESIAN_POINT ( 'NONE',  ( 64.78349330513380266, 4.898587196589294500E-16, -4.000000000000007105 ) ) ;
#55193=ORIENTED_EDGE ( 'NONE', *, *, #71799, .F. ) ;
#55195=AXIS2_PLACEMENT_3D ( 'NONE', #85220, #59367, #84163 ) ;
#55199=DIRECTION ( 'NONE',  ( 0.000000000000000000, -1.000000000000000000, 0.000000000000000000 ) ) ;
#55224=ADVANCED_FACE ( 'NONE', ( #97664 ), #15165, .T. ) ;
#55232=DIRECTION ( 'NONE',  ( 1.000000000000000000, 0.000000000000000000, -0.000000000000000000 ) ) ;
#55243=AXIS2_PLACEMENT_3D ( 'NONE', #41383, #49464, #100677 ) ;
#55288=EDGE_CURVE ( 'NONE', #40289, #22931, #24884, .T. ) ;
#55302=ADVANCED_FACE ( 'NONE', ( #66920 ), #60443, .F. ) ;
#55321=DIRECTION ( 'NONE',  ( 0.000000000000000000, -1.000000000000000000, 0.000000000000000000 ) ) ;
#55348=AXIS2_PLACEMENT_3D ( 'NONE', #47880, #46833, #96467 ) ;
#55388=AXIS2_PLACEMENT_3D ( 'NONE', #75443, #59279, #92154 ) ;
#55415=DIRECTION ( 'NONE',  ( 0.000000000000000000, -1.000000000000000000, 0.000000000000000000 ) ) ;
#55432=AXIS2_PLACEMENT_3D ( 'NONE', #74291, #99089, #97493 ) ;
#55462=EDGE_CURVE ( 'NONE', #7306, #91765, #19475, .T. ) ;
#55479=CARTESIAN_POINT ( 'NONE',  ( 0.5805565836007582359, 3.752776749732553263, -6.499999999999999112 ) ) ;
#55488=EDGE_LOOP ( 'NONE', ( #72276, #25108, #86388, #88433, #3278, #79849 ) ) ;
#55494=LINE ( 'NONE', #14506, #100034 ) ;
#55549=ADVANCED_FACE ( 'NONE', ( #6816 ), #30054, .T. ) ;
#55601=VERTEX_POINT ( 'NONE', #23567 ) ;
#55711=EDGE_LOOP ( 'NONE', ( #62628, #100527, #97496 ) ) ;
#55844=CARTESIAN_POINT ( 'NONE',  ( 0.2578475836320663905, 4.367703157927318891, -5.434916218090831030 ) ) ;
#55847=AXIS2_PLACEMENT_3D ( 'NONE', #62224, #64, #73982 ) ;
#55875=ADVANCED_FACE ( 'NONE', ( #53656 ), #86588, .F. ) ;
#55886=ORIENTED_EDGE ( 'NONE', *, *, #9395, .T. ) ;
#55940=CARTESIAN_POINT ( 'NONE',  ( 74.07777777777778283, 6.915964383211875250E-15, 0.000000000000000000 ) ) ;
#55947=CARTESIAN_POINT ( 'NONE',  ( 56.96666666666666856, 6.915964383211875250E-15, 0.000000000000000000 ) ) ;
#56003=VECTOR ( 'NONE', #81893, 1000.000000000000227 ) ;
#56013=EDGE_CURVE ( 'NONE', #102336, #84625, #16314, .T. ) ;
#56046=CIRCLE ( 'NONE', #11322, 4.000000000000007105 ) ;
#56093=EDGE_CURVE ( 'NONE', #6495, #35284, #7759, .T. ) ;
#56098=VECTOR ( 'NONE', #73017, 1000.000000000000000 ) ;
#56103=AXIS2_PLACEMENT_3D ( 'NONE', #48705, #49235, #63870 ) ;
#56123=CARTESIAN_POINT ( 'NONE',  ( 56.22793774957824553, 4.000000000000014211, 0.000000000000000000 ) ) ;
#56189=ORIENTED_EDGE ( 'NONE', *, *, #93477, .F. ) ;
#56195=CARTESIAN_POINT ( 'NONE',  ( 55.00571552735602410, -1.232595164407830946E-29, 4.000000000000007105 ) ) ;
#56202=CARTESIAN_POINT ( 'NONE',  ( 0.4042117618284652436, -3.141900367810030126, 6.500000000000000000 ) ) ;
#56239=CARTESIAN_POINT ( 'NONE',  ( 58.67238219402268840, 4.898587196589294500E-16, -4.000000000000007105 ) ) ;
#56259=DIRECTION ( 'NONE',  ( -1.000000000000000000, -1.224606353822377258E-16, -0.000000000000000000 ) ) ;
#56292=VERTEX_POINT ( 'NONE', #76071 ) ;
#56329=CARTESIAN_POINT ( 'NONE',  ( 4.699999999999999289, 3.752776749732569694, 6.499999999999997335 ) ) ;
#56395=AXIS2_PLACEMENT_3D ( 'NONE', #17809, #50661, #43140 ) ;
#56428=DIRECTION ( 'NONE',  ( 0.000000000000000000, -1.000000000000000000, 0.000000000000000000 ) ) ;
#56465=CARTESIAN_POINT ( 'NONE',  ( 60.63333333333333286, 6.915964383211875250E-15, 0.000000000000000000 ) ) ;
#56466=AXIS2_PLACEMENT_3D ( 'NONE', #79084, #104960, #55321 ) ;
#56467=EDGE_LOOP ( 'NONE', ( #58798, #8426, #6099, #89729, #24759 ) ) ;
#56476=ORIENTED_EDGE ( 'NONE', *, *, #19218, .T. ) ;
#56497=EDGE_CURVE ( 'NONE', #11977, #81058, #84048, .T. ) ;
#56512=CIRCLE ( 'NONE', #13473, 4.000000000000007105 ) ;
#56540=ORIENTED_EDGE ( 'NONE', *, *, #70245, .F. ) ;
#56565=ORIENTED_EDGE ( 'NONE', *, *, #93956, .F. ) ;
#56566=ADVANCED_FACE ( 'NONE', ( #2584 ), #31973, .T. ) ;
#56569=AXIS2_PLACEMENT_3D ( 'NONE', #64789, #90126, #73387 ) ;
#56596=CARTESIAN_POINT ( 'NONE',  ( 5.299999999999999822, 0.000000000000000000, 0.000000000000000000 ) ) ;
#56610=CARTESIAN_POINT ( 'NONE',  ( 54.52222222222221859, -3.309500000000000774, 4.475777889183797681E-16 ) ) ;
#56622=ORIENTED_EDGE ( 'NONE', *, *, #56843, .F. ) ;
#56710=ADVANCED_FACE ( 'NONE', ( #102354 ), #11289, .T. ) ;
#56768=VECTOR ( 'NONE', #51116, 1000.000000000000000 ) ;
#56790=CARTESIAN_POINT ( 'NONE',  ( 0.000000000000000000, 0.000000000000000000, 0.000000000000000000 ) ) ;
#56799=FACE_OUTER_BOUND ( 'NONE', #15274, .T. ) ;
#56843=EDGE_CURVE ( 'NONE', #26677, #79305, #49179, .T. ) ;
#56854=CARTESIAN_POINT ( 'NONE',  ( 54.52222222222221859, 6.915964383211875250E-15, 0.000000000000000000 ) ) ;
#56937=ORIENTED_EDGE ( 'NONE', *, *, #14823, .T. ) ;
#56941=CARTESIAN_POINT ( 'NONE',  ( 0.05533025579362507718, -4.993776679985868050, -4.350525068611865720 ) ) ;
#56956=DIRECTION ( 'NONE',  ( -1.000000000000000000, -0.000000000000000000, -0.000000000000000000 ) ) ;
#57017=CARTESIAN_POINT ( 'NONE',  ( 56.96666666666666856, -3.309500000000000774, 4.475777889183797681E-16 ) ) ;
#57033=DIRECTION ( 'NONE',  ( 0.000000000000000000, 0.000000000000000000, 1.000000000000000000 ) ) ;
#57091=EDGE_LOOP ( 'NONE', ( #40091, #60390, #55886, #104061, #19365 ) ) ;
#57093=ORIENTED_EDGE ( 'NONE', *, *, #88027, .F. ) ;
#57116=ORIENTED_EDGE ( 'NONE', *, *, #90306, .F. ) ;
#57156=EDGE_CURVE ( 'NONE', #18822, #16756, #4460, .T. ) ;
#57173=DIRECTION ( 'NONE',  ( -1.000000000000000000, -1.224606353822377258E-16, -0.000000000000000000 ) ) ;
#57180=DIRECTION ( 'NONE',  ( -1.000000000000000000, -0.000000000000000000, -0.000000000000000000 ) ) ;
#57202=VECTOR ( 'NONE', #71526, 1000.000000000000000 ) ;
#57235=VERTEX_POINT ( 'NONE', #103691 ) ;
#57246=ADVANCED_FACE ( 'NONE', ( #78877 ), #75115, .T. ) ;
#57259=VERTEX_POINT ( 'NONE', #47563 ) ;
#57270=CIRCLE ( 'NONE', #78157, 4.000000000000007105 ) ;
#57278=ADVANCED_FACE ( 'NONE', ( #104210 ), #47032, .T. ) ;
#57333=PLANE ( 'NONE',  #74218 ) ;
#57360=EDGE_CURVE ( 'NONE', #75872, #57426, #76828, .T. ) ;
#57426=VERTEX_POINT ( 'NONE', #82053 ) ;
#57433=AXIS2_PLACEMENT_3D ( 'NONE', #60130, #92994, #20224 ) ;
#57489=VECTOR ( 'NONE', #10900, 1000.000000000000000 ) ;
#57512=UNCERTAINTY_MEASURE_WITH_UNIT (LENGTH_MEASURE( 1.000000000000000082E-05 ), #104150, 'distance_accuracy_value', 'NONE');
#57529=CARTESIAN_POINT ( 'NONE',  ( 61.11682663846713837, 6.975173280561618775E-15, 0.000000000000000000 ) ) ;
#57601=AXIS2_PLACEMENT_3D ( 'NONE', #100813, #19433, #26974 ) ;
#57608=PLANE ( 'NONE',  #25774 ) ;
#57625=CARTESIAN_POINT ( 'NONE',  ( 73.33904886068935980, 4.000000000000014211, 0.000000000000000000 ) ) ;
#57646=AXIS2_PLACEMENT_3D ( 'NONE', #37261, #20577, #27585 ) ;
#57649=CARTESIAN_POINT ( 'NONE',  ( 75.30000000000001137, 4.475777889183788807E-16, -3.309499999999999886 ) ) ;
#57658=ORIENTED_EDGE ( 'NONE', *, *, #75093, .T. ) ;
#57748=EDGE_CURVE ( 'NONE', #66339, #65683, #86293, .T. ) ;
#57752=DIRECTION ( 'NONE',  ( -1.000000000000000000, -1.224606353822377258E-16, -0.000000000000000000 ) ) ;
#57782=CARTESIAN_POINT ( 'NONE',  ( 58.67238219402268840, -4.000000000000000000, 4.898587196589421703E-16 ) ) ;
#57803=CONICAL_SURFACE ( 'NONE', #9533, 3.309500000000007880, 0.9599310885968770357 ) ;
#57862=DIRECTION ( 'NONE',  ( -0.5735764363510497121, 0.8191520442889892450, 1.003171929053521665E-16 ) ) ;
#57880=AXIS2_PLACEMENT_3D ( 'NONE', #13010, #46464, #77773 ) ;
#57904=VERTEX_POINT ( 'NONE', #95961 ) ;
#57908=CARTESIAN_POINT ( 'NONE',  ( 4.699999999999999289, 0.000000000000000000, 0.000000000000000000 ) ) ;
#57959=CIRCLE ( 'NONE', #63140, 3.309500000000007880 ) ;
#57961=AXIS2_PLACEMENT_3D ( 'NONE', #98285, #66996, #16849 ) ;
#58017=AXIS2_PLACEMENT_3D ( 'NONE', #22102, #86835, #45832 ) ;
#58026=ORIENTED_EDGE ( 'NONE', *, *, #94623, .F. ) ;
#58101=VERTEX_POINT ( 'NONE', #52171 ) ;
#58113=CIRCLE ( 'NONE', #34049, 4.000000000000007105 ) ;
#58118=EDGE_LOOP ( 'NONE', ( #96129, #105909, #94411, #37542, #26933, #30480 ) ) ;
#58132=CYLINDRICAL_SURFACE ( 'NONE', #39601, 4.000000000000000000 ) ;
#58189=VECTOR ( 'NONE', #66576, 1000.000000000000000 ) ;
#58221=FACE_OUTER_BOUND ( 'NONE', #65526, .T. ) ;
#58239=DIRECTION ( 'NONE',  ( 0.000000000000000000, -1.000000000000000000, 0.000000000000000000 ) ) ;
#58280=EDGE_CURVE ( 'NONE', #102336, #7738, #52033, .T. ) ;
#58295=VERTEX_POINT ( 'NONE', #92634 ) ;
#58396=ADVANCED_FACE ( 'NONE', ( #78050 ), #37460, .T. ) ;
#58457=DIRECTION ( 'NONE',  ( 0.000000000000000000, -1.000000000000000000, 0.000000000000000000 ) ) ;
#58467=EDGE_CURVE ( 'NONE', #20623, #58101, #80512, .T. ) ;
#58479=EDGE_CURVE ( 'NONE', #3882, #25775, #58113, .T. ) ;
#58480=DIRECTION ( 'NONE',  ( 0.5735764363510440500, 0.8191520442889932418, 0.000000000000000000 ) ) ;
#58485=LINE ( 'NONE', #60630, #105994 ) ;
#58499=CARTESIAN_POINT ( 'NONE',  ( 74.56127108291157413, 6.975173280561618775E-15, 0.000000000000000000 ) ) ;
#58505=DIRECTION ( 'NONE',  ( -1.000000000000000000, -1.224606353822377258E-16, -0.000000000000000000 ) ) ;
#58511=ORIENTED_EDGE ( 'NONE', *, *, #53256, .F. ) ;
#58516=CIRCLE ( 'NONE', #11985, 4.000000000000007105 ) ;
#58584=ORIENTED_EDGE ( 'NONE', *, *, #30835, .T. ) ;
#58634=ORIENTED_EDGE ( 'NONE', *, *, #2438, .T. ) ;
#58635=EDGE_LOOP ( 'NONE', ( #4894, #33413, #72893, #84967, #36974 ) ) ;
#58640=CARTESIAN_POINT ( 'NONE',  ( 0.000000000000000000, 0.000000000000000000, 4.000000000000000000 ) ) ;
#58641=VERTEX_POINT ( 'NONE', #60176 ) ;
#58647=CARTESIAN_POINT ( 'NONE',  ( 69.67238219402268840, 6.975173280561618775E-15, 0.000000000000000000 ) ) ;
#58657=ORIENTED_EDGE ( 'NONE', *, *, #86616, .F. ) ;
#58676=CONICAL_SURFACE ( 'NONE', #43119, 4.000000000000007105, 0.9599310885968835860 ) ;
#58678=LINE ( 'NONE', #83467, #65260 ) ;
#58707=CIRCLE ( 'NONE', #94908, 3.309500000000007880 ) ;
#58762=ORIENTED_EDGE ( 'NONE', *, *, #103365, .F. ) ;
#58798=ORIENTED_EDGE ( 'NONE', *, *, #104878, .F. ) ;
#58831=VERTEX_POINT ( 'NONE', #98348 ) ;
#58880=EDGE_CURVE ( 'NONE', #27209, #48389, #39198, .T. ) ;
#58897=ORIENTED_EDGE ( 'NONE', *, *, #65772, .T. ) ;
#58944=ADVANCED_FACE ( 'NONE', ( #80556 ), #6676, .T. ) ;
#58957=AXIS2_PLACEMENT_3D ( 'NONE', #18575, #30924, #96169 ) ;
#58958=ORIENTED_EDGE ( 'NONE', *, *, #5066, .F. ) ;
#58960=LINE ( 'NONE', #91846, #57489 ) ;
#59014=CARTESIAN_POINT ( 'NONE',  ( 58.18888888888888999, 6.915964383211875250E-15, 0.000000000000000000 ) ) ;
#59016=VERTEX_POINT ( 'NONE', #65975 ) ;
#59055=DIRECTION ( 'NONE',  ( -1.000000000000000000, -0.000000000000000000, -0.000000000000000000 ) ) ;
#59060=ORIENTED_EDGE ( 'NONE', *, *, #53704, .F. ) ;
#59212=ADVANCED_FACE ( 'NONE', ( #68929 ), #51331, .T. ) ;
#59256=ORIENTED_EDGE ( 'NONE', *, *, #80996, .T. ) ;
#59257=EDGE_CURVE ( 'NONE', #85895, #6296, #9588, .T. ) ;
#59279=DIRECTION ( 'NONE',  ( -1.000000000000000000, -1.224606353822377258E-16, -0.000000000000000000 ) ) ;
#59292=DIRECTION ( 'NONE',  ( 0.000000000000000000, -1.000000000000000000, 0.000000000000000000 ) ) ;
#59326=CONICAL_SURFACE ( 'NONE', #97180, 4.000000000000007105, 0.9599310885968835860 ) ;
#59367=DIRECTION ( 'NONE',  ( -1.000000000000000000, -1.224606353822377258E-16, -0.000000000000000000 ) ) ;
#59384=ORIENTED_EDGE ( 'NONE', *, *, #90120, .F. ) ;
#59407=ORIENTED_EDGE ( 'NONE', *, *, #11871, .F. ) ;
#59436=CARTESIAN_POINT ( 'NONE',  ( 4.235164736271502188E-16, 0.6351314446025461136, -6.500000000000000000 ) ) ;
#59499=DIRECTION ( 'NONE',  ( -1.000000000000000000, -0.000000000000000000, -0.000000000000000000 ) ) ;
#59506=AXIS2_PLACEMENT_3D ( 'NONE', #3606, #43531, #83975 ) ;
#59522=ORIENTED_EDGE ( 'NONE', *, *, #54468, .F. ) ;
#59536=CIRCLE ( 'NONE', #81896, 4.000000000000007105 ) ;
#59553=CYLINDRICAL_SURFACE ( 'NONE', #58957, 4.000000000000000000 ) ;
#59562=ADVANCED_FACE ( 'NONE', ( #103799 ), #38559, .T. ) ;
#59566=CARTESIAN_POINT ( 'NONE',  ( 68.45015997180047407, -4.000000000000000888, 4.898587196589422689E-16 ) ) ;
#59573=VERTEX_POINT ( 'NONE', #62305 ) ;
#59577=DIRECTION ( 'NONE',  ( 0.000000000000000000, 1.000000000000000000, 0.000000000000000000 ) ) ;
#59586=DIRECTION ( 'NONE',  ( -1.000000000000000000, -1.224606353822377258E-16, -0.000000000000000000 ) ) ;
#59590=ORIENTED_EDGE ( 'NONE', *, *, #60833, .F. ) ;
#59611=DIRECTION ( 'NONE',  ( -0.5735764363510497121, 0.8191520442889892450, 1.003171929053521665E-16 ) ) ;
#59639=DIRECTION ( 'NONE',  ( 0.000000000000000000, 0.000000000000000000, -1.000000000000000000 ) ) ;
#59650=VERTEX_POINT ( 'NONE', #81106 ) ;
#59703=VERTEX_POINT ( 'NONE', #88159 ) ;
#59756=CARTESIAN_POINT ( 'NONE',  ( 0.06682554136338283990, -6.264794173742283867, -2.149058192116890531 ) ) ;
#59786=VERTEX_POINT ( 'NONE', #104871 ) ;
#59850=CONICAL_SURFACE ( 'NONE', #92542, 4.000000000000007105, 0.9599310885968835860 ) ;
#59891=VECTOR ( 'NONE', #70474, 1000.000000000000000 ) ;
#59893=LINE ( 'NONE', #19463, #103192 ) ;
#59931=DIRECTION ( 'NONE',  ( -1.000000000000000000, -1.224606353822377258E-16, -0.000000000000000000 ) ) ;
#60108=CARTESIAN_POINT ( 'NONE',  ( 61.37206225042174879, 6.856755485862130937E-15, 0.000000000000000000 ) ) ;
#60119=ORIENTED_EDGE ( 'NONE', *, *, #32524, .F. ) ;
#60130=CARTESIAN_POINT ( 'NONE',  ( 59.89460441624491693, 6.975173280561618775E-15, 0.000000000000000000 ) ) ;
#60176=CARTESIAN_POINT ( 'NONE',  ( 65.52222222222222570, -3.309500000000000774, 4.475777889183797681E-16 ) ) ;
#60226=DIRECTION ( 'NONE',  ( 1.000000000000000000, 1.224606353822377258E-16, 0.000000000000000000 ) ) ;
#60292=EDGE_CURVE ( 'NONE', #65608, #38217, #73568, .T. ) ;
#60293=EDGE_CURVE ( 'NONE', #102372, #62199, #3071, .T. ) ;
#60317=FACE_OUTER_BOUND ( 'NONE', #64235, .T. ) ;
#60321=CARTESIAN_POINT ( 'NONE',  ( 72.37206225042174879, -4.000000000000000000, 0.000000000000000000 ) ) ;
#60356=CARTESIAN_POINT ( 'NONE',  ( 61.85555555555556140, -3.309500000000000774, 4.475777889183797681E-16 ) ) ;
#60370=ORIENTED_EDGE ( 'NONE', *, *, #80508, .F. ) ;
#60384=VERTEX_POINT ( 'NONE', #8155 ) ;
#60390=ORIENTED_EDGE ( 'NONE', *, *, #72319, .T. ) ;
#60440=ORIENTED_EDGE ( 'NONE', *, *, #39618, .T. ) ;
#60443=PLANE ( 'NONE',  #47260 ) ;
#60463=CONICAL_SURFACE ( 'NONE', #63925, 3.309500000000007880, 0.9599310885968770357 ) ;
#60502=ORIENTED_EDGE ( 'NONE', *, *, #81930, .F. ) ;
#60503=CARTESIAN_POINT ( 'NONE',  ( 64.29999999999999716, 3.309500000000014541, 4.052968581778174646E-16 ) ) ;
#60624=ORIENTED_EDGE ( 'NONE', *, *, #54281, .F. ) ;
#60626=EDGE_CURVE ( 'NONE', #82654, #102083, #53041, .T. ) ;
#60628=FACE_OUTER_BOUND ( 'NONE', #84610, .T. ) ;
#60630=CARTESIAN_POINT ( 'NONE',  ( 66.74444444444444002, -3.309500000000000774, 0.000000000000000000 ) ) ;
#60643=ORIENTED_EDGE ( 'NONE', *, *, #76977, .F. ) ;
#60688=EDGE_CURVE ( 'NONE', #47738, #79305, #5391, .T. ) ;
#60689=EDGE_LOOP ( 'NONE', ( #20670, #55193, #105823, #69374, #68850 ) ) ;
#60693=ADVANCED_FACE ( 'NONE', ( #14510 ), #80312, .T. ) ;
#60703=ORIENTED_EDGE ( 'NONE', *, *, #62678, .T. ) ;
#60711=ORIENTED_EDGE ( 'NONE', *, *, #85026, .T. ) ;
#60764=CARTESIAN_POINT ( 'NONE',  ( 74.56127108291157413, 6.975173280561618775E-15, 0.000000000000000000 ) ) ;
#60766=EDGE_CURVE ( 'NONE', #43629, #71682, #82989, .T. ) ;
#60773=DIRECTION ( 'NONE',  ( -1.000000000000000000, -1.224606353822377258E-16, -0.000000000000000000 ) ) ;
#60833=EDGE_CURVE ( 'NONE', #53314, #8468, #43069, .T. ) ;
#60836=CYLINDRICAL_SURFACE ( 'NONE', #89509, 4.000000000000000000 ) ;
#60843=VECTOR ( 'NONE', #75303, 1000.000000000000000 ) ;
#60844=CARTESIAN_POINT ( 'NONE',  ( 0.000000000000000000, 0.000000000000000000, 0.000000000000000000 ) ) ;
#60845=DIRECTION ( 'NONE',  ( -1.000000000000000000, -1.224606353822377258E-16, -0.000000000000000000 ) ) ;
#60862=VECTOR ( 'NONE', #100276, 1000.000000000000000 ) ;
#60882=EDGE_CURVE ( 'NONE', #82447, #75804, #33398, .T. ) ;
#60890=CARTESIAN_POINT ( 'NONE',  ( 56.22793774957824553, 6.975173280561618775E-15, 0.000000000000000000 ) ) ;
#60909=FACE_OUTER_BOUND ( 'NONE', #99332, .T. ) ;
#60974=ORIENTED_EDGE ( 'NONE', *, *, #105179, .F. ) ;
#61049=LINE ( 'NONE', #78797, #83973 ) ;
#61058=CARTESIAN_POINT ( 'NONE',  ( 61.11682663846713837, 6.975173280561618775E-15, 0.000000000000000000 ) ) ;
#61072=AXIS2_PLACEMENT_3D ( 'NONE', #39388, #14013, #49977 ) ;
#61085=EDGE_CURVE ( 'NONE', #85509, #26511, #106442, .T. ) ;
#61092=CARTESIAN_POINT ( 'NONE',  ( 71.63333333333333997, 6.915964383211875250E-15, 0.000000000000000000 ) ) ;
#61120=ORIENTED_EDGE ( 'NONE', *, *, #30719, .F. ) ;
#61122=ORIENTED_EDGE ( 'NONE', *, *, #27418, .T. ) ;
#61147=AXIS2_PLACEMENT_3D ( 'NONE', #47313, #89907, #65098 ) ;
#61151=AXIS2_PLACEMENT_3D ( 'NONE', #79026, #14807, #105940 ) ;
#61166=DIRECTION ( 'NONE',  ( -1.000000000000000000, -1.224606353822377258E-16, -0.000000000000000000 ) ) ;
#61177=ORIENTED_EDGE ( 'NONE', *, *, #43518, .F. ) ;
#61178=CARTESIAN_POINT ( 'NONE',  ( 66.00571552735603120, -4.000000000000000888, 4.898587196589422689E-16 ) ) ;
#61180=ORIENTED_EDGE ( 'NONE', *, *, #25660, .T. ) ;
#61259=CIRCLE ( 'NONE', #16430, 4.000000000000007105 ) ;
#61290=EDGE_CURVE ( 'NONE', #53379, #14336, #26515, .T. ) ;
#61293=ORIENTED_EDGE ( 'NONE', *, *, #73401, .T. ) ;
#61304=EDGE_CURVE ( 'NONE', #82447, #11977, #7511, .T. ) ;
#61334=CARTESIAN_POINT ( 'NONE',  ( 60.63333333333333286, -3.309500000000000774, 4.475777889183797681E-16 ) ) ;
#61356=AXIS2_PLACEMENT_3D ( 'NONE', #103405, #78586, #14907 ) ;
#61379=EDGE_CURVE ( 'NONE', #90844, #34259, #54056, .T. ) ;
#61384=VERTEX_POINT ( 'NONE', #78349 ) ;
#61404=CARTESIAN_POINT ( 'NONE',  ( 64.78349330513380266, 6.975173280561618775E-15, 0.000000000000000000 ) ) ;
#61415=CIRCLE ( 'NONE', #25241, 4.000000000000007105 ) ;
#61425=CARTESIAN_POINT ( 'NONE',  ( 66.26095113931063452, 4.898587196589294500E-16, -4.000000000000007105 ) ) ;
#61509=ADVANCED_FACE ( 'NONE', ( #63781 ), #105286, .T. ) ;
#61546=DIRECTION ( 'NONE',  ( 0.000000000000000000, -1.000000000000000000, 0.000000000000000000 ) ) ;
#61571=VECTOR ( 'NONE', #4769, 1000.000000000000000 ) ;
#61593=FACE_OUTER_BOUND ( 'NONE', #58118, .T. ) ;
#61617=VECTOR ( 'NONE', #76230, 1000.000000000000000 ) ;
#61634=AXIS2_PLACEMENT_3D ( 'NONE', #33681, #51426, #50885 ) ;
#61663=VERTEX_POINT ( 'NONE', #19511 ) ;
#61717=DIRECTION ( 'NONE',  ( 0.000000000000000000, -1.000000000000000000, 0.000000000000000000 ) ) ;
#61728=ORIENTED_EDGE ( 'NONE', *, *, #85366, .T. ) ;
#61744=DIRECTION ( 'NONE',  ( 0.000000000000000000, -1.000000000000000000, 0.000000000000000000 ) ) ;
#61749=ORIENTED_EDGE ( 'NONE', *, *, #86814, .T. ) ;
#61807=DIRECTION ( 'NONE',  ( 0.000000000000000000, -1.000000000000000000, 0.000000000000000000 ) ) ;
#61821=ORIENTED_EDGE ( 'NONE', *, *, #60626, .T. ) ;
#61849=CARTESIAN_POINT ( 'NONE',  ( 55.26095113931063452, 6.856755485862130937E-15, 0.000000000000000000 ) ) ;
#61865=CARTESIAN_POINT ( 'NONE',  ( 0.000000000000000000, 1.502314598737161398E-15, 6.499999999999999112 ) ) ;
#61868=CIRCLE ( 'NONE', #20555, 4.000000000000007105 ) ;
#61913=FACE_OUTER_BOUND ( 'NONE', #93070, .T. ) ;
#61914=ORIENTED_EDGE ( 'NONE', *, *, #53034, .T. ) ;
#61940=DIRECTION ( 'NONE',  ( -1.000000000000000000, -1.224606353822377258E-16, -0.000000000000000000 ) ) ;
#61966=EDGE_CURVE ( 'NONE', #99028, #102372, #7581, .T. ) ;
#61978=CIRCLE ( 'NONE', #63655, 3.309500000000007880 ) ;
#62006=CARTESIAN_POINT ( 'NONE',  ( 69.18888888888888289, 6.915964383211875250E-15, 0.000000000000000000 ) ) ;
#62064=FACE_OUTER_BOUND ( 'NONE', #56467, .T. ) ;
#62115=ORIENTED_EDGE ( 'NONE', *, *, #30006, .T. ) ;
#62132=ORIENTED_EDGE ( 'NONE', *, *, #72946, .T. ) ;
#62159=CARTESIAN_POINT ( 'NONE',  ( 64.29999999999999716, -3.309500000000000774, 4.475777889183797681E-16 ) ) ;
#62160=VECTOR ( 'NONE', #24552, 1000.000000000000000 ) ;
#62178=ORIENTED_EDGE ( 'NONE', *, *, #71799, .T. ) ;
#62183=CONICAL_SURFACE ( 'NONE', #63873, 3.309500000000007880, 0.9599310885968770357 ) ;
#62189=VECTOR ( 'NONE', #92129, 1000.000000000000000 ) ;
#62199=VERTEX_POINT ( 'NONE', #43229 ) ;
#62224=CARTESIAN_POINT ( 'NONE',  ( 68.70539558375507738, 6.856755485862130937E-15, 0.000000000000000000 ) ) ;
#62227=ADVANCED_FACE ( 'NONE', ( #3838 ), #50776, .T. ) ;
#62258=ADVANCED_FACE ( 'NONE', ( #69111 ), #74870, .T. ) ;
#62280=DIRECTION ( 'NONE',  ( 0.000000000000000000, 0.000000000000000000, 1.000000000000000000 ) ) ;
#62305=CARTESIAN_POINT ( 'NONE',  ( 74.56127108291157413, -1.232595164407830946E-29, 4.000000000000007105 ) ) ;
#62357=DIRECTION ( 'NONE',  ( 1.000000000000000000, 0.000000000000000000, 0.000000000000000000 ) ) ;
#62387=CARTESIAN_POINT ( 'NONE',  ( 0.000000000000000000, 4.898587196589412829E-16, -4.000000000000000000 ) ) ;
#62402=LINE ( 'NONE', #28466, #96819 ) ;
#62464=ORIENTED_EDGE ( 'NONE', *, *, #50800, .F. ) ;
#62498=ADVANCED_FACE ( 'NONE', ( #77594 ), #24959, .T. ) ;
#62513=AXIS2_PLACEMENT_3D ( 'NONE', #52518, #37980, #3986 ) ;
#62554=CARTESIAN_POINT ( 'NONE',  ( 61.85555555555556140, -3.309500000000000774, 0.000000000000000000 ) ) ;
#62628=ORIENTED_EDGE ( 'NONE', *, *, #64374, .T. ) ;
#62640=EDGE_LOOP ( 'NONE', ( #6458, #65796, #103022, #6217, #9424 ) ) ;
#62648=CIRCLE ( 'NONE', #41980, 4.000000000000007105 ) ;
#62678=EDGE_CURVE ( 'NONE', #20574, #17114, #80039, .T. ) ;
#62690=AXIS2_PLACEMENT_3D ( 'NONE', #18415, #75011, #44271 ) ;
#62691=ORIENTED_EDGE ( 'NONE', *, *, #96365, .F. ) ;
#62717=DIRECTION ( 'NONE',  ( -0.7071067811865314745, 0.000000000000000000, 0.7071067811865635599 ) ) ;
#62763=CARTESIAN_POINT ( 'NONE',  ( 57.45015997180046696, 4.000000000000014211, 0.000000000000000000 ) ) ;
#62768=ADVANCED_FACE ( 'NONE', ( #30936 ), #15240, .T. ) ;
#62779=EDGE_CURVE ( 'NONE', #59786, #17325, #39979, .T. ) ;
#62863=ORIENTED_EDGE ( 'NONE', *, *, #104265, .T. ) ;
#62875=CARTESIAN_POINT ( 'NONE',  ( 67.48317336153286305, -4.000000000000000000, 0.000000000000000000 ) ) ;
#62879=EDGE_CURVE ( 'NONE', #70947, #93228, #37130, .T. ) ;
#62883=CARTESIAN_POINT ( 'NONE',  ( 69.92761780597730592, 4.898587196589294500E-16, -4.000000000000007105 ) ) ;
#62919=VECTOR ( 'NONE', #39017, 1000.000000000000000 ) ;
#62941=ORIENTED_EDGE ( 'NONE', *, *, #61290, .F. ) ;
#63019=FACE_OUTER_BOUND ( 'NONE', #54345, .T. ) ;
#63044=DIRECTION ( 'NONE',  ( -1.000000000000000000, -1.224606353822377258E-16, -0.000000000000000000 ) ) ;
#63057=CARTESIAN_POINT ( 'NONE',  ( 4.699999999999999289, 0.000000000000000000, 0.000000000000000000 ) ) ;
#63089=VECTOR ( 'NONE', #65490, 1000.000000000000000 ) ;
#63096=CARTESIAN_POINT ( 'NONE',  ( 0.000000000000000000, 0.000000000000000000, 0.000000000000000000 ) ) ;
#63113=AXIS2_PLACEMENT_3D ( 'NONE', #38515, #31726, #64613 ) ;
#63140=AXIS2_PLACEMENT_3D ( 'NONE', #38620, #21387, #71483 ) ;
#63157=DIRECTION ( 'NONE',  ( 0.000000000000000000, -1.000000000000000000, 0.000000000000000000 ) ) ;
#63193=AXIS2_PLACEMENT_3D ( 'NONE', #91317, #41162, #24996 ) ;
#63194=AXIS2_PLACEMENT_3D ( 'NONE', #46569, #36928, #45002 ) ;
#63201=CARTESIAN_POINT ( 'NONE',  ( 69.67238219402268840, 4.898587196589294500E-16, -4.000000000000007105 ) ) ;
#63372=ADVANCED_FACE ( 'NONE', ( #66862 ), #23418, .T. ) ;
#63383=AXIS2_PLACEMENT_3D ( 'NONE', #79255, #78711, #70642 ) ;
#63395=EDGE_CURVE ( 'NONE', #34259, #59573, #84637, .T. ) ;
#63407=ORIENTED_EDGE ( 'NONE', *, *, #23592, .F. ) ;
#63410=CARTESIAN_POINT ( 'NONE',  ( 0.000000000000000000, 0.000000000000000000, 4.000000000000000000 ) ) ;
#63427=CIRCLE ( 'NONE', #85832, 4.000000000000007105 ) ;
#63428=VERTEX_POINT ( 'NONE', #92178 ) ;
#63434=LINE ( 'NONE', #88748, #81155 ) ;
#63505=ORIENTED_EDGE ( 'NONE', *, *, #98738, .F. ) ;
#63510=ORIENTED_EDGE ( 'NONE', *, *, #28103, .F. ) ;
#63540=EDGE_LOOP ( 'NONE', ( #106156, #74641, #36715, #33161, #54642 ) ) ;
#63545=AXIS2_PLACEMENT_3D ( 'NONE', #23808, #90634, #40484 ) ;
#63560=DIRECTION ( 'NONE',  ( 0.000000000000000000, -1.000000000000000000, 0.000000000000000000 ) ) ;
#63586=DIRECTION ( 'NONE',  ( -0.5735764363510497121, 0.8191520442889892450, 1.003171929053521665E-16 ) ) ;
#63615=ORIENTED_EDGE ( 'NONE', *, *, #46484, .F. ) ;
#63624=VERTEX_POINT ( 'NONE', #89425 ) ;
#63655=AXIS2_PLACEMENT_3D ( 'NONE', #21978, #54832, #46755 ) ;
#63662=DIRECTION ( 'NONE',  ( 0.000000000000000000, -1.000000000000000000, 0.000000000000000000 ) ) ;
#63677=ORIENTED_EDGE ( 'NONE', *, *, #88867, .F. ) ;
#63735=EDGE_CURVE ( 'NONE', #92331, #35260, #88830, .T. ) ;
#63781=FACE_OUTER_BOUND ( 'NONE', #64494, .T. ) ;
#63791=CARTESIAN_POINT ( 'NONE',  ( 0.5805565836007667846, -3.752776749732578132, -6.500000000000000888 ) ) ;
#63831=APPLICATION_CONTEXT ( 'automotive_design' ) ;
#63870=DIRECTION ( 'NONE',  ( 0.000000000000000000, -1.000000000000000000, 0.000000000000000000 ) ) ;
#63873=AXIS2_PLACEMENT_3D ( 'NONE', #48307, #72592, #97388 ) ;
#63924=EDGE_CURVE ( 'NONE', #25775, #75872, #76817, .T. ) ;
#63925=AXIS2_PLACEMENT_3D ( 'NONE', #33967, #16148, #106203 ) ;
#63964=VECTOR ( 'NONE', #18769, 1000.000000000000114 ) ;
#64012=CARTESIAN_POINT ( 'NONE',  ( 67.48317336153286305, 6.856755485862130937E-15, 0.000000000000000000 ) ) ;
#64028=COLOUR_RGB ( '', 0.66274510, 0.83137255, 0.94901961) ;
#64042=DIRECTION ( 'NONE',  ( -1.000000000000000000, -1.224606353822377258E-16, -0.000000000000000000 ) ) ;
#64051=DIRECTION ( 'NONE',  ( -1.000000000000000000, -1.224606353822377258E-16, -0.000000000000000000 ) ) ;
#64086=DIRECTION ( 'NONE',  ( 1.000000000000000000, 0.000000000000000000, -0.000000000000000000 ) ) ;
#64124=EDGE_CURVE ( 'NONE', #35260, #92331, #66496, .T. ) ;
#64143=ORIENTED_EDGE ( 'NONE', *, *, #53704, .T. ) ;
#64170=DIRECTION ( 'NONE',  ( 0.000000000000000000, 0.000000000000000000, 1.000000000000000000 ) ) ;
#64204=DIRECTION ( 'NONE',  ( 0.000000000000000000, -1.000000000000000000, 0.000000000000000000 ) ) ;
#64225=DIRECTION ( 'NONE',  ( -1.000000000000000000, -1.224606353822377258E-16, -0.000000000000000000 ) ) ;
#64230=DIRECTION ( 'NONE',  ( 0.5735764363510442720, -0.8191520442889930198, 1.003171929053526349E-16 ) ) ;
#64235=EDGE_LOOP ( 'NONE', ( #48844, #81482, #95165, #26070, #99223 ) ) ;
#64260=ORIENTED_EDGE ( 'NONE', *, *, #34332, .T. ) ;
#64278=DIRECTION ( 'NONE',  ( 0.000000000000000000, -1.000000000000000000, 0.000000000000000000 ) ) ;
#64305=ORIENTED_EDGE ( 'NONE', *, *, #68757, .T. ) ;
#64325=CARTESIAN_POINT ( 'NONE',  ( 72.37206225042174879, 4.000000000000015099, 4.898587196589422689E-16 ) ) ;
#64374=EDGE_CURVE ( 'NONE', #14056, #25843, #86156, .T. ) ;
#64447=DIRECTION ( 'NONE',  ( -1.000000000000000000, -1.224606353822377258E-16, -0.000000000000000000 ) ) ;
#64494=EDGE_LOOP ( 'NONE', ( #86325, #85781, #15711, #62691, #86254, #61177 ) ) ;
#64520=CARTESIAN_POINT ( 'NONE',  ( 0.000000000000000000, 4.898587196589412829E-16, -4.000000000000000000 ) ) ;
#64521=CARTESIAN_POINT ( 'NONE',  ( 73.59428447264397732, 6.856755485862130937E-15, 0.000000000000000000 ) ) ;
#64561=( NAMED_UNIT ( * ) PLANE_ANGLE_UNIT ( ) SI_UNIT ( $, .RADIAN. ) );
#64609=DIRECTION ( 'NONE',  ( 0.000000000000000000, -1.000000000000000000, 0.000000000000000000 ) ) ;
#64613=DIRECTION ( 'NONE',  ( 0.000000000000000000, -1.000000000000000000, 0.000000000000000000 ) ) ;
#64631=EDGE_LOOP ( 'NONE', ( #82827, #75622, #103009, #89288, #16965, #48995 ) ) ;
#64634=DIRECTION ( 'NONE',  ( 0.000000000000000000, 1.000000000000000000, 0.000000000000000000 ) ) ;
#64639=CARTESIAN_POINT ( 'NONE',  ( 69.67238219402268840, 6.975173280561618775E-15, 0.000000000000000000 ) ) ;
#64651=CARTESIAN_POINT ( 'NONE',  ( 67.96666666666666856, 6.915964383211875250E-15, 0.000000000000000000 ) ) ;
#64718=EDGE_LOOP ( 'NONE', ( #86226, #7279, #102820, #17241, #73192 ) ) ;
#64748=ADVANCED_FACE ( 'NONE', ( #53105 ), #19967, .T. ) ;
#64789=CARTESIAN_POINT ( 'NONE',  ( 0.000000000000000000, 0.000000000000000000, 0.000000000000000000 ) ) ;
#64790=CARTESIAN_POINT ( 'NONE',  ( 4.699999999999999289, -3.752776749732578132, -6.500000000000000888 ) ) ;
#64813=ORIENTED_EDGE ( 'NONE', *, *, #79841, .F. ) ;
#64876=AXIS2_PLACEMENT_3D ( 'NONE', #9398, #59586, #42315 ) ;
#64911=CARTESIAN_POINT ( 'NONE',  ( 68.45015997180047407, 6.975173280561618775E-15, 0.000000000000000000 ) ) ;
#64956=CARTESIAN_POINT ( 'NONE',  ( 5.299999999999999822, -3.752776749732578132, -6.500000000000000888 ) ) ;
#64996=LINE ( 'NONE', #14839, #98992 ) ;
#65043=AXIS2_PLACEMENT_3D ( 'NONE', #88946, #12916, #5381 ) ;
#65056=ORIENTED_EDGE ( 'NONE', *, *, #95989, .F. ) ;
#65098=DIRECTION ( 'NONE',  ( 0.000000000000000000, 0.000000000000000000, 1.000000000000000000 ) ) ;
#65105=VERTEX_POINT ( 'NONE', #94515 ) ;
#65116=AXIS2_PLACEMENT_3D ( 'NONE', #4200, #18828, #19898 ) ;
#65154=FACE_OUTER_BOUND ( 'NONE', #58635, .T. ) ;
#65163=DIRECTION ( 'NONE',  ( 0.000000000000000000, -1.000000000000000000, 0.000000000000000000 ) ) ;
#65195=CIRCLE ( 'NONE', #35917, 4.400000000000000355 ) ;
#65215=CARTESIAN_POINT ( 'NONE',  ( 66.00571552735603120, 6.975173280561618775E-15, 0.000000000000000000 ) ) ;
#65249=EDGE_LOOP ( 'NONE', ( #84326, #48256, #45587, #4361, #101605 ) ) ;
#65260=VECTOR ( 'NONE', #33351, 1000.000000000000000 ) ;
#65289=PRESENTATION_STYLE_ASSIGNMENT (( #71254 ) ) ;
#65490=DIRECTION ( 'NONE',  ( 0.5735764363510440500, 0.8191520442889932418, 0.000000000000000000 ) ) ;
#65494=DIRECTION ( 'NONE',  ( -0.000000000000000000, 0.8660254037844391517, 0.4999999999999992228 ) ) ;
#65495=CARTESIAN_POINT ( 'NONE',  ( 0.000000000000000000, 5.629165124598848990, 3.250000000000002220 ) ) ;
#65497=ADVANCED_FACE ( 'NONE', ( #61913 ), #49229, .T. ) ;
#65526=EDGE_LOOP ( 'NONE', ( #102527, #91046, #15777 ) ) ;
#65608=VERTEX_POINT ( 'NONE', #80704 ) ;
#65638=EDGE_CURVE ( 'NONE', #26511, #45176, #18243, .T. ) ;
#65679=CYLINDRICAL_SURFACE ( 'NONE', #23208, 4.000000000000000000 ) ;
#65683=VERTEX_POINT ( 'NONE', #54289 ) ;
#65698=AXIS2_PLACEMENT_3D ( 'NONE', #26369, #20416, #44648 ) ;
#65716=LINE ( 'NONE', #16630, #7686 ) ;
#65726=CARTESIAN_POINT ( 'NONE',  ( 69.92761780597730592, 4.000000000000015099, 4.898587196589422689E-16 ) ) ;
#65767=CARTESIAN_POINT ( 'NONE',  ( 75.30000000000001137, 0.000000000000000000, 0.000000000000000000 ) ) ;
#65772=EDGE_CURVE ( 'NONE', #12412, #59786, #32732, .T. ) ;
#65780=AXIS2_PLACEMENT_3D ( 'NONE', #17675, #74818, #9555 ) ;
#65796=ORIENTED_EDGE ( 'NONE', *, *, #86440, .F. ) ;
#65806=VECTOR ( 'NONE', #97865, 1000.000000000000000 ) ;
#65810=DIRECTION ( 'NONE',  ( 0.000000000000000000, -1.000000000000000000, 0.000000000000000000 ) ) ;
#65820=( NAMED_UNIT ( * ) PLANE_ANGLE_UNIT ( ) SI_UNIT ( $, .RADIAN. ) );
#65903=EDGE_CURVE ( 'NONE', #6434, #102890, #39025, .T. ) ;
#65975=CARTESIAN_POINT ( 'NONE',  ( 5.299999999999999822, 7.960204194457794491E-16, -6.499999999999999112 ) ) ;
#65990=DIRECTION ( 'NONE',  ( -1.000000000000000000, -1.224606353822377258E-16, -0.000000000000000000 ) ) ;
#66007=ORIENTED_EDGE ( 'NONE', *, *, #63924, .T. ) ;
#66029=EDGE_CURVE ( 'NONE', #40289, #32311, #106103, .T. ) ;
#66069=VECTOR ( 'NONE', #95440, 1000.000000000000000 ) ;
#66175=( GEOMETRIC_REPRESENTATION_CONTEXT ( 3 ) GLOBAL_UNCERTAINTY_ASSIGNED_CONTEXT ( ( #73703 ) ) GLOBAL_UNIT_ASSIGNED_CONTEXT ( ( #40480, #39962, #71774 ) ) REPRESENTATION_CONTEXT ( 'NONE', 'WORKASPACE' ) );
#66184=DIRECTION ( 'NONE',  ( 0.000000000000000000, -1.000000000000000000, 0.000000000000000000 ) ) ;
#66208=CIRCLE ( 'NONE', #61072, 4.000000000000007105 ) ;
#66209=DIRECTION ( 'NONE',  ( 0.000000000000000000, -1.000000000000000000, 0.000000000000000000 ) ) ;
#66242=PRODUCT_DEFINITION_FORMATION_WITH_SPECIFIED_SOURCE ( 'ANY', '', #19209, .NOT_KNOWN. ) ;
#66339=VERTEX_POINT ( 'NONE', #96857 ) ;
#66352=VECTOR ( 'NONE', #88422, 1000.000000000000000 ) ;
#66429=AXIS2_PLACEMENT_3D ( 'NONE', #50895, #27214, #84881 ) ;
#66451=AXIS2_PLACEMENT_3D ( 'NONE', #88638, #104822, #14730 ) ;
#66454=EDGE_CURVE ( 'NONE', #29354, #33265, #40765, .T. ) ;
#66496=CIRCLE ( 'NONE', #26968, 3.309500000000007880 ) ;
#66517=VERTEX_POINT ( 'NONE', #76807 ) ;
#66543=VERTEX_POINT ( 'NONE', #91422 ) ;
#66550=CARTESIAN_POINT ( 'NONE',  ( 54.03872891708841308, 6.856755485862130937E-15, 0.000000000000000000 ) ) ;
#66576=DIRECTION ( 'NONE',  ( 0.5735764363510440500, 0.8191520442889932418, 0.000000000000000000 ) ) ;
#66585=EDGE_LOOP ( 'NONE', ( #96660, #10460, #42726, #103843 ) ) ;
#66648=ADVANCED_FACE ( 'NONE', ( #28304 ), #90753, .T. ) ;
#66658=AXIS2_PLACEMENT_3D ( 'NONE', #21577, #46874, #71154 ) ;
#66666=DIRECTION ( 'NONE',  ( 0.000000000000000000, 0.000000000000000000, -1.000000000000000000 ) ) ;
#66694=DIRECTION ( 'NONE',  ( -0.5735764363510494901, -0.8191520442889894671, 0.000000000000000000 ) ) ;
#66737=DIRECTION ( 'NONE',  ( -1.000000000000000000, -1.224606353822377258E-16, -0.000000000000000000 ) ) ;
#66745=CIRCLE ( 'NONE', #15059, 6.499999999999999112 ) ;
#66797=CARTESIAN_POINT ( 'NONE',  ( 55.26095113931063452, 6.856755485862130937E-15, 0.000000000000000000 ) ) ;
#66802=ORIENTED_EDGE ( 'NONE', *, *, #58467, .F. ) ;
#66806=LINE ( 'NONE', #50078, #62189 ) ;
#66818=DIRECTION ( 'NONE',  ( -1.000000000000000000, -0.000000000000000000, -0.000000000000000000 ) ) ;
#66825=AXIS2_PLACEMENT_3D ( 'NONE', #10454, #83288, #43371 ) ;
#66850=CARTESIAN_POINT ( 'NONE',  ( 59.89460441624491693, -1.232595164407830946E-29, 4.000000000000007105 ) ) ;
#66862=FACE_OUTER_BOUND ( 'NONE', #45646, .T. ) ;
#66875=LINE ( 'NONE', #32932, #105347 ) ;
#66920=FACE_OUTER_BOUND ( 'NONE', #23304, .T. ) ;
#66940=DIRECTION ( 'NONE',  ( 0.000000000000000000, -1.000000000000000000, 0.000000000000000000 ) ) ;
#66953=CARTESIAN_POINT ( 'NONE',  ( 72.11682663846713126, 4.898587196589294500E-16, -4.000000000000007105 ) ) ;
#66955=ORIENTED_EDGE ( 'NONE', *, *, #65903, .F. ) ;
#66971=DIRECTION ( 'NONE',  ( 0.5735764363510442720, -0.8191520442889930198, 1.003171929053526349E-16 ) ) ;
#66996=DIRECTION ( 'NONE',  ( 1.000000000000000000, 1.224606353822377258E-16, 0.000000000000000000 ) ) ;
#66999=ADVANCED_FACE ( 'NONE', ( #67544 ), #84249, .T. ) ;
#67018=EDGE_CURVE ( 'NONE', #4022, #59703, #61049, .T. ) ;
#67054=DIRECTION ( 'NONE',  ( 0.000000000000000000, 0.000000000000000000, -1.000000000000000000 ) ) ;
#67081=ORIENTED_EDGE ( 'NONE', *, *, #94297, .T. ) ;
#67087=DIRECTION ( 'NONE',  ( -1.000000000000000000, -0.000000000000000000, -0.000000000000000000 ) ) ;
#67125=DIRECTION ( 'NONE',  ( 0.000000000000000000, -1.000000000000000000, 0.000000000000000000 ) ) ;
#67144=EDGE_CURVE ( 'NONE', #3167, #93228, #32809, .T. ) ;
#67157=CARTESIAN_POINT ( 'NONE',  ( 58.67238219402268840, 6.975173280561618775E-15, 0.000000000000000000 ) ) ;
#67212=PLANE ( 'NONE',  #87781 ) ;
#67318=AXIS2_PLACEMENT_3D ( 'NONE', #76795, #8873, #59577 ) ;
#67376=AXIS2_PLACEMENT_3D ( 'NONE', #86233, #103449, #12306 ) ;
#67382=FACE_OUTER_BOUND ( 'NONE', #80246, .T. ) ;
#67387=ORIENTED_EDGE ( 'NONE', *, *, #44202, .F. ) ;
#67394=CARTESIAN_POINT ( 'NONE',  ( 0.000000000000000000, 0.000000000000000000, 4.000000000000000000 ) ) ;
#67450=ORIENTED_EDGE ( 'NONE', *, *, #58280, .F. ) ;
#67469=ORIENTED_EDGE ( 'NONE', *, *, #101045, .T. ) ;
#67494=EDGE_CURVE ( 'NONE', #4517, #104615, #104412, .T. ) ;
#67501=CARTESIAN_POINT ( 'NONE',  ( 0.000000000000000000, 0.000000000000000000, 4.000000000000000000 ) ) ;
#67531=EDGE_CURVE ( 'NONE', #35344, #40074, #70270, .T. ) ;
#67541=EDGE_CURVE ( 'NONE', #54844, #99696, #88248, .T. ) ;
#67544=FACE_OUTER_BOUND ( 'NONE', #68646, .T. ) ;
#67584=CIRCLE ( 'NONE', #53783, 4.000000000000007105 ) ;
#67634=ORIENTED_EDGE ( 'NONE', *, *, #78576, .T. ) ;
#67642=FACE_OUTER_BOUND ( 'NONE', #89488, .T. ) ;
#67747=CARTESIAN_POINT ( 'NONE',  ( 0.000000000000000000, 0.000000000000000000, 0.000000000000000000 ) ) ;
#67779=ORIENTED_EDGE ( 'NONE', *, *, #101045, .F. ) ;
#67783=CARTESIAN_POINT ( 'NONE',  ( 70.89460441624491693, 6.975173280561618775E-15, 0.000000000000000000 ) ) ;
#67832=CARTESIAN_POINT ( 'NONE',  ( 0.2578475836320727188, -6.890627091270376425, -1.065083781909170302 ) ) ;
#67859=EDGE_LOOP ( 'NONE', ( #44127, #8885, #7156, #12977, #100955 ) ) ;
#67860=EDGE_CURVE ( 'NONE', #41106, #59573, #20434, .T. ) ;
#67871=DIRECTION ( 'NONE',  ( -0.5735764363510497121, 0.8191520442889892450, 1.003171929053521665E-16 ) ) ;
#67934=EDGE_LOOP ( 'NONE', ( #1069, #15667, #204, #17378, #11866 ) ) ;
#67939=ORIENTED_EDGE ( 'NONE', *, *, #37892, .F. ) ;
#67971=EDGE_LOOP ( 'NONE', ( #98541, #85041, #106270, #56622, #94707, #28542 ) ) ;
#67981=DIRECTION ( 'NONE',  ( -1.000000000000000000, -1.224606353822377258E-16, -0.000000000000000000 ) ) ;
#68001=CARTESIAN_POINT ( 'NONE',  ( 68.70539558375507738, -4.000000000000000000, 0.000000000000000000 ) ) ;
#68017=CARTESIAN_POINT ( 'NONE',  ( 63.07777777777777573, 6.915964383211875250E-15, 0.000000000000000000 ) ) ;
#68042=CARTESIAN_POINT ( 'NONE',  ( 0.2573354458087829810, 4.368923434677195239, 5.432802636760776238 ) ) ;
#68056=CIRCLE ( 'NONE', #30128, 4.000000000000007105 ) ;
#68080=DIRECTION ( 'NONE',  ( -0.5735764363510494901, -0.8191520442889894671, 0.000000000000000000 ) ) ;
#68118=AXIS2_PLACEMENT_3D ( 'NONE', #10052, #76370, #848 ) ;
#68203=EDGE_CURVE ( 'NONE', #85895, #101318, #37661, .T. ) ;
#68263=DIRECTION ( 'NONE',  ( 0.000000000000000000, 1.000000000000000000, 0.000000000000000000 ) ) ;
#68267=DIRECTION ( 'NONE',  ( -1.000000000000000000, -1.224606353822377258E-16, -0.000000000000000000 ) ) ;
#68311=CONICAL_SURFACE ( 'NONE', #7995, 4.000000000000007105, 0.9599310885968835860 ) ;
#68331=CARTESIAN_POINT ( 'NONE',  ( 67.22793774957824553, -4.000000000000000888, 4.898587196589422689E-16 ) ) ;
#68359=CARTESIAN_POINT ( 'NONE',  ( 74.56127108291157413, 4.000000000000013323, 0.000000000000000000 ) ) ;
#68360=EDGE_CURVE ( 'NONE', #76274, #76519, #58678, .T. ) ;
#68378=CONICAL_SURFACE ( 'NONE', #57961, 4.000000000000007105, 0.9599310885968835860 ) ;
#68382=ORIENTED_EDGE ( 'NONE', *, *, #76027, .F. ) ;
#68399=CARTESIAN_POINT ( 'NONE',  ( 62.59428447264396311, -4.000000000000000000, 0.000000000000000000 ) ) ;
#68513=ORIENTED_EDGE ( 'NONE', *, *, #43518, .T. ) ;
#68520=DIRECTION ( 'NONE',  ( 0.000000000000000000, -1.000000000000000000, -2.311253228826400140E-16 ) ) ;
#68522=CARTESIAN_POINT ( 'NONE',  ( 0.000000000000000000, 0.000000000000000000, 0.000000000000000000 ) ) ;
#68537=EDGE_LOOP ( 'NONE', ( #34345, #6619, #18179, #89559, #83458, #46537 ) ) ;
#68547=CARTESIAN_POINT ( 'NONE',  ( 62.33904886068935980, 6.975173280561618775E-15, 0.000000000000000000 ) ) ;
#68635=CARTESIAN_POINT ( 'NONE',  ( 65.52222222222222570, -3.309500000000000774, 0.000000000000000000 ) ) ;
#68646=EDGE_LOOP ( 'NONE', ( #70837, #59256, #1732, #63510, #60370, #32394 ) ) ;
#68656=EDGE_CURVE ( 'NONE', #39378, #70947, #41170, .T. ) ;
#68662=DIRECTION ( 'NONE',  ( -1.000000000000000000, -1.224606353822377258E-16, -0.000000000000000000 ) ) ;
#68697=DIRECTION ( 'NONE',  ( -1.000000000000000000, -1.224606353822377258E-16, -0.000000000000000000 ) ) ;
#68757=EDGE_CURVE ( 'NONE', #35102, #105955, #97970, .T. ) ;
#68771=CARTESIAN_POINT ( 'NONE',  ( 0.000000000000000000, 4.898587196589412829E-16, -4.000000000000000000 ) ) ;
#68772=CARTESIAN_POINT ( 'NONE',  ( 61.85555555555556140, 3.309500000000014541, 4.052968581778174646E-16 ) ) ;
#68806=DIRECTION ( 'NONE',  ( 0.000000000000000000, -1.000000000000000000, 0.000000000000000000 ) ) ;
#68809=AXIS2_PLACEMENT_3D ( 'NONE', #47697, #95741, #61807 ) ;
#68825=ORIENTED_EDGE ( 'NONE', *, *, #72528, .T. ) ;
#68850=ORIENTED_EDGE ( 'NONE', *, *, #81930, .T. ) ;
#68880=VERTEX_POINT ( 'NONE', #100989 ) ;
#68888=AXIS2_PLACEMENT_3D ( 'NONE', #46585, #6650, #78951 ) ;
#68927=CIRCLE ( 'NONE', #36239, 4.000000000000007105 ) ;
#68929=FACE_OUTER_BOUND ( 'NONE', #15224, .T. ) ;
#68935=VERTEX_POINT ( 'NONE', #92895 ) ;
#68969=ORIENTED_EDGE ( 'NONE', *, *, #6746, .F. ) ;
#68985=DIRECTION ( 'NONE',  ( -1.000000000000000000, -0.000000000000000000, -0.000000000000000000 ) ) ;
#69015=CYLINDRICAL_SURFACE ( 'NONE', #51907, 4.000000000000000000 ) ;
#69022=CONICAL_SURFACE ( 'NONE', #67318, 4.000000000000007105, 0.9599310885968835860 ) ;
#69029=AXIS2_PLACEMENT_3D ( 'NONE', #104978, #29023, #103385 ) ;
#69053=AXIS2_PLACEMENT_3D ( 'NONE', #85950, #102641, #12021 ) ;
#69083=EDGE_CURVE ( 'NONE', #53314, #63428, #104925, .T. ) ;
#69100=DIRECTION ( 'NONE',  ( -1.000000000000000000, -1.224606353822377258E-16, -0.000000000000000000 ) ) ;
#69104=CIRCLE ( 'NONE', #19251, 4.000000000000007105 ) ;
#69111=FACE_OUTER_BOUND ( 'NONE', #21859, .T. ) ;
#69128=ORIENTED_EDGE ( 'NONE', *, *, #80508, .T. ) ;
#69231=DIRECTION ( 'NONE',  ( 0.5735764363510440500, 0.8191520442889932418, 0.000000000000000000 ) ) ;
#69245=CARTESIAN_POINT ( 'NONE',  ( 64.29999999999999716, 3.309500000000014541, 0.000000000000000000 ) ) ;
#69261=ORIENTED_EDGE ( 'NONE', *, *, #88867, .T. ) ;
#69264=ORIENTED_EDGE ( 'NONE', *, *, #79096, .T. ) ;
#69278=DIRECTION ( 'NONE',  ( 0.000000000000000000, 1.000000000000000000, 0.000000000000000000 ) ) ;
#69301=SHAPE_DEFINITION_REPRESENTATION ( #2784, #77771 ) ;
#69354=EDGE_CURVE ( 'NONE', #101359, #87625, #30958, .T. ) ;
#69357=LINE ( 'NONE', #18692, #76013 ) ;
#69370=CONICAL_SURFACE ( 'NONE', #62513, 6.499999999999999112, 1.047197551196600296 ) ;
#69374=ORIENTED_EDGE ( 'NONE', *, *, #89531, .T. ) ;
#69471=PRESENTATION_STYLE_ASSIGNMENT (( #36606 ) ) ;
#69473=FACE_OUTER_BOUND ( 'NONE', #105042, .T. ) ;
#69510=ORIENTED_EDGE ( 'NONE', *, *, #20921, .T. ) ;
#69524=ADVANCED_FACE ( 'NONE', ( #18257 ), #60836, .T. ) ;
#69541=EDGE_CURVE ( 'NONE', #9016, #51147, #18808, .T. ) ;
#69546=CARTESIAN_POINT ( 'NONE',  ( 55.26095113931063452, -4.000000000000000000, 0.000000000000000000 ) ) ;
#69571=DIRECTION ( 'NONE',  ( 0.000000000000000000, 1.000000000000000000, 0.000000000000000000 ) ) ;
#69600=VERTEX_POINT ( 'NONE', #86185 ) ;
#69704=VERTEX_POINT ( 'NONE', #6818 ) ;
#69741=CARTESIAN_POINT ( 'NONE',  ( 58.92761780597729881, 6.856755485862130937E-15, 0.000000000000000000 ) ) ;
#69806=EDGE_CURVE ( 'NONE', #87625, #101359, #61978, .T. ) ;
#69878=FACE_OUTER_BOUND ( 'NONE', #34090, .T. ) ;
#69880=EDGE_CURVE ( 'NONE', #30792, #99128, #104986, .T. ) ;
#69975=EDGE_CURVE ( 'NONE', #11751, #84900, #41299, .T. ) ;
#69989=CIRCLE ( 'NONE', #23526, 3.309500000000007880 ) ;
#70028=DIRECTION ( 'NONE',  ( 0.000000000000000000, -1.000000000000000000, 0.000000000000000000 ) ) ;
#70079=CARTESIAN_POINT ( 'NONE',  ( 58.67238219402268840, 4.000000000000014211, 0.000000000000000000 ) ) ;
#70203=AXIS2_PLACEMENT_3D ( 'NONE', #27849, #100082, #52591 ) ;
#70245=EDGE_CURVE ( 'NONE', #105730, #58641, #91295, .T. ) ;
#70270=CIRCLE ( 'NONE', #56466, 4.000000000000007105 ) ;
#70310=FACE_OUTER_BOUND ( 'NONE', #55711, .T. ) ;
#70316=LINE ( 'NONE', #103734, #39126 ) ;
#70335=EDGE_LOOP ( 'NONE', ( #73955, #43489, #90513, #86936, #37599 ) ) ;
#70361=CONICAL_SURFACE ( 'NONE', #84134, 3.309500000000007880, 0.9599310885968770357 ) ;
#70382=LINE ( 'NONE', #45058, #89166 ) ;
#70385=CARTESIAN_POINT ( 'NONE',  ( 65.52222222222222570, 6.915964383211875250E-15, 0.000000000000000000 ) ) ;
#70397=DIRECTION ( 'NONE',  ( 1.000000000000000000, 1.224606353822377258E-16, 0.000000000000000000 ) ) ;
#70403=CARTESIAN_POINT ( 'NONE',  ( 58.67238219402268840, 6.975173280561618775E-15, 0.000000000000000000 ) ) ;
#70434=FACE_OUTER_BOUND ( 'NONE', #33923, .T. ) ;
#70440=PLANE ( 'NONE',  #72588 ) ;
#70474=DIRECTION ( 'NONE',  ( -0.5735764363510497121, 0.8191520442889892450, 1.003171929053521665E-16 ) ) ;
#70479=AXIS2_PLACEMENT_3D ( 'NONE', #54194, #87133, #13207 ) ;
#70504=EDGE_LOOP ( 'NONE', ( #2907, #21760, #22273, #9589, #73396, #30655 ) ) ;
#70543=DIRECTION ( 'NONE',  ( 0.000000000000000000, -1.000000000000000000, 0.000000000000000000 ) ) ;
#70549=DIRECTION ( 'NONE',  ( 0.000000000000000000, 1.000000000000000000, 0.000000000000000000 ) ) ;
#70551=VECTOR ( 'NONE', #13077, 1000.000000000000000 ) ;
#70592=CARTESIAN_POINT ( 'NONE',  ( 0.1061556211655303172, -4.836380039389409191, 4.623144047065555817 ) ) ;
#70597=CARTESIAN_POINT ( 'NONE',  ( 4.699999999999999289, 0.000000000000000000, 0.000000000000000000 ) ) ;
#70609=CIRCLE ( 'NONE', #51652, 4.000000000000007105 ) ;
#70621=EDGE_CURVE ( 'NONE', #9016, #21775, #20812, .T. ) ;
#70638=DIRECTION ( 'NONE',  ( -1.000000000000000000, -1.224606353822377258E-16, -0.000000000000000000 ) ) ;
#70642=DIRECTION ( 'NONE',  ( 0.000000000000000000, -1.000000000000000000, 0.000000000000000000 ) ) ;
#70658=CYLINDRICAL_SURFACE ( 'NONE', #102988, 4.000000000000000000 ) ;
#70672=ORIENTED_EDGE ( 'NONE', *, *, #1136, .F. ) ;
#70741=CARTESIAN_POINT ( 'NONE',  ( 72.11682663846713126, -4.000000000000000000, 4.898587196589421703E-16 ) ) ;
#70750=EDGE_CURVE ( 'NONE', #16756, #93278, #6953, .T. ) ;
#70788=ORIENTED_EDGE ( 'NONE', *, *, #95989, .T. ) ;
#70791=VERTEX_POINT ( 'NONE', #45714 ) ;
#70820=ORIENTED_EDGE ( 'NONE', *, *, #67144, .F. ) ;
#70822=VECTOR ( 'NONE', #96854, 1000.000000000000000 ) ;
#70837=ORIENTED_EDGE ( 'NONE', *, *, #79000, .T. ) ;
#70858=EDGE_LOOP ( 'NONE', ( #27523, #34985, #34662, #28966, #74130 ) ) ;
#70859=AXIS2_PLACEMENT_3D ( 'NONE', #53743, #11136, #36015 ) ;
#70918=DIRECTION ( 'NONE',  ( 0.5735764363510442720, -0.8191520442889930198, 1.003171929053526349E-16 ) ) ;
#70944=ORIENTED_EDGE ( 'NONE', *, *, #98738, .T. ) ;
#70947=VERTEX_POINT ( 'NONE', #77433 ) ;
#71022=DIRECTION ( 'NONE',  ( 0.000000000000000000, 1.000000000000000000, 0.000000000000000000 ) ) ;
#71025=CARTESIAN_POINT ( 'NONE',  ( 73.33904886068935980, -4.000000000000000888, 4.898587196589422689E-16 ) ) ;
#71081=EDGE_CURVE ( 'NONE', #30721, #18822, #32634, .T. ) ;
#71113=CARTESIAN_POINT ( 'NONE',  ( 0.4037800551813686689, -4.058962678540087410, 5.969670414742687115 ) ) ;
#71115=VECTOR ( 'NONE', #43250, 1000.000000000000000 ) ;
#71118=EDGE_LOOP ( 'NONE', ( #21274, #31232, #954, #42612, #34374 ) ) ;
#71146=VECTOR ( 'NONE', #98469, 1000.000000000000000 ) ;
#71150=ORIENTED_EDGE ( 'NONE', *, *, #74158, .F. ) ;
#71154=DIRECTION ( 'NONE',  ( 0.000000000000000000, -1.000000000000000000, 0.000000000000000000 ) ) ;
#71172=ADVANCED_FACE ( 'NONE', ( #73561 ), #17486, .F. ) ;
#71174=DIRECTION ( 'NONE',  ( -1.000000000000000000, -0.000000000000000000, -0.000000000000000000 ) ) ;
#71220=EDGE_CURVE ( 'NONE', #52615, #37041, #77304, .T. ) ;
#71235=VECTOR ( 'NONE', #10995, 1000.000000000000000 ) ;
#71254=SURFACE_STYLE_USAGE ( .BOTH. , #32419 ) ;
#71297=CARTESIAN_POINT ( 'NONE',  ( 62.33904886068935980, 6.975173280561618775E-15, 0.000000000000000000 ) ) ;
#71349=CARTESIAN_POINT ( 'NONE',  ( 63.56127108291158123, 6.975173280561618775E-15, 0.000000000000000000 ) ) ;
#71360=LINE ( 'NONE', #15253, #53608 ) ;
#71363=AXIS2_PLACEMENT_3D ( 'NONE', #51999, #92453, #43918 ) ;
#71379=CARTESIAN_POINT ( 'NONE',  ( 72.11682663846713126, 6.975173280561618775E-15, 0.000000000000000000 ) ) ;
#71393=EDGE_CURVE ( 'NONE', #71455, #93427, #96598, .T. ) ;
#71394=DIRECTION ( 'NONE',  ( -1.000000000000000000, -0.000000000000000000, -0.000000000000000000 ) ) ;
#71406=CARTESIAN_POINT ( 'NONE',  ( 4.699999999999999289, 5.629165124598849879, 3.250000000000002665 ) ) ;
#71455=VERTEX_POINT ( 'NONE', #77838 ) ;
#71482=FACE_BOUND ( 'NONE', #99287, .T. ) ;
#71483=DIRECTION ( 'NONE',  ( 0.000000000000000000, -1.000000000000000000, 0.000000000000000000 ) ) ;
#71522=CARTESIAN_POINT ( 'NONE',  ( -6.082437715114721581E-15, 5.469921996229787808, -3.525817189091417170 ) ) ;
#71526=DIRECTION ( 'NONE',  ( -1.000000000000000000, -0.000000000000000000, -0.000000000000000000 ) ) ;
#71530=CARTESIAN_POINT ( 'NONE',  ( 70.89460441624491693, -4.000000000000000000, 4.898587196589421703E-16 ) ) ;
#71553=EDGE_LOOP ( 'NONE', ( #84850, #10057, #100125, #104457, #8337, #82897 ) ) ;
#71619=DIRECTION ( 'NONE',  ( -1.000000000000000000, -1.224606353822377258E-16, -0.000000000000000000 ) ) ;
#71642=DIRECTION ( 'NONE',  ( 0.000000000000000000, -1.000000000000000000, 0.000000000000000000 ) ) ;
#71682=VERTEX_POINT ( 'NONE', #28131 ) ;
#71771=DIRECTION ( 'NONE',  ( 0.000000000000000000, 0.000000000000000000, 1.000000000000000000 ) ) ;
#71774=( NAMED_UNIT ( * ) SI_UNIT ( $, .STERADIAN. ) SOLID_ANGLE_UNIT ( ) );
#71777=CARTESIAN_POINT ( 'NONE',  ( 71.63333333333333997, 3.309500000000014541, 4.052968581778174646E-16 ) ) ;
#71799=EDGE_CURVE ( 'NONE', #3167, #94772, #72327, .T. ) ;
#71815=CARTESIAN_POINT ( 'NONE',  ( 71.63333333333333997, 3.309500000000014541, 0.000000000000000000 ) ) ;
#71835=ORIENTED_EDGE ( 'NONE', *, *, #68656, .F. ) ;
#71841=DIRECTION ( 'NONE',  ( 0.000000000000000000, 0.000000000000000000, 1.000000000000000000 ) ) ;
#71866=AXIS2_PLACEMENT_3D ( 'NONE', #11899, #102517, #61546 ) ;
#71869=ORIENTED_EDGE ( 'NONE', *, *, #54468, .T. ) ;
#71889=CARTESIAN_POINT ( 'NONE',  ( 72.85555555555556850, 6.915964383211875250E-15, 0.000000000000000000 ) ) ;
#71916=ORIENTED_EDGE ( 'NONE', *, *, #43854, .F. ) ;
#71959=ORIENTED_EDGE ( 'NONE', *, *, #42428, .F. ) ;
#71992=CARTESIAN_POINT ( 'NONE',  ( 67.22793774957824553, 6.975173280561618775E-15, 0.000000000000000000 ) ) ;
#72034=CIRCLE ( 'NONE', #53007, 4.000000000000007105 ) ;
#72154=AXIS2_PLACEMENT_3D ( 'NONE', #30984, #12623, #62280 ) ;
#72249=VECTOR ( 'NONE', #69231, 1000.000000000000000 ) ;
#72271=CARTESIAN_POINT ( 'NONE',  ( 70.41111111111112564, 6.915964383211875250E-15, 0.000000000000000000 ) ) ;
#72276=ORIENTED_EDGE ( 'NONE', *, *, #57156, .T. ) ;
#72290=EDGE_CURVE ( 'NONE', #105955, #71682, #43153, .T. ) ;
#72302=CIRCLE ( 'NONE', #106782, 4.000000000000007105 ) ;
#72319=EDGE_CURVE ( 'NONE', #79502, #70791, #53476, .T. ) ;
#72327=CIRCLE ( 'NONE', #34491, 3.309500000000007880 ) ;
#72378=ORIENTED_EDGE ( 'NONE', *, *, #60766, .T. ) ;
#72417=DIRECTION ( 'NONE',  ( -1.000000000000000000, -0.000000000000000000, -0.000000000000000000 ) ) ;
#72462=TOROIDAL_SURFACE ( 'NONE', #22532, 4.400000000000000355, 0.4000000000000000222 ) ;
#72503=DIRECTION ( 'NONE',  ( 0.000000000000000000, -1.000000000000000000, 0.000000000000000000 ) ) ;
#72507=LINE ( 'NONE', #47162, #33929 ) ;
#72508=ORIENTED_EDGE ( 'NONE', *, *, #26494, .F. ) ;
#72528=EDGE_CURVE ( 'NONE', #4022, #49330, #29863, .T. ) ;
#72544=AXIS2_PLACEMENT_3D ( 'NONE', #98600, #23692, #41964 ) ;
#72546=ORIENTED_EDGE ( 'NONE', *, *, #9014, .T. ) ;
#72555=EDGE_LOOP ( 'NONE', ( #50605, #101705, #106450, #81867, #345 ) ) ;
#72588=AXIS2_PLACEMENT_3D ( 'NONE', #29481, #62357, #87158 ) ;
#72592=DIRECTION ( 'NONE',  ( -1.000000000000000000, -1.224606353822377258E-16, -0.000000000000000000 ) ) ;
#72598=CARTESIAN_POINT ( 'NONE',  ( 59.89460441624491693, 4.898587196589294500E-16, -4.000000000000007105 ) ) ;
#72604=EDGE_LOOP ( 'NONE', ( #58584, #6871, #11100, #58657, #57093 ) ) ;
#72671=ORIENTED_EDGE ( 'NONE', *, *, #88027, .T. ) ;
#72687=CARTESIAN_POINT ( 'NONE',  ( 64.78349330513380266, -4.000000000000000000, 4.898587196589421703E-16 ) ) ;
#72691=DIRECTION ( 'NONE',  ( 1.000000000000000000, 1.224606353822377258E-16, 0.000000000000000000 ) ) ;
#72721=DIRECTION ( 'NONE',  ( 0.000000000000000000, -1.000000000000000000, 0.000000000000000000 ) ) ;
#72733=ORIENTED_EDGE ( 'NONE', *, *, #34407, .T. ) ;
#72747=VERTEX_POINT ( 'NONE', #73255 ) ;
#72752=DIRECTION ( 'NONE',  ( -1.000000000000000000, -1.224606353822377258E-16, -0.000000000000000000 ) ) ;
#72754=DIRECTION ( 'NONE',  ( -1.000000000000000000, -1.224606353822377258E-16, -0.000000000000000000 ) ) ;
#72781=CARTESIAN_POINT ( 'NONE',  ( 54.03872891708841308, -4.000000000000000000, 0.000000000000000000 ) ) ;
#72784=ORIENTED_EDGE ( 'NONE', *, *, #55028, .T. ) ;
#72791=ORIENTED_EDGE ( 'NONE', *, *, #3398, .T. ) ;
#72805=ADVANCED_FACE ( 'NONE', ( #17713 ), #50573, .T. ) ;
#72832=CYLINDRICAL_SURFACE ( 'NONE', #78386, 4.000000000000000000 ) ;
#72852=CARTESIAN_POINT ( 'NONE',  ( 61.37206225042174879, 6.856755485862130937E-15, 0.000000000000000000 ) ) ;
#72856=DIRECTION ( 'NONE',  ( 1.000000000000000000, 0.000000000000000000, 0.000000000000000000 ) ) ;
#72893=ORIENTED_EDGE ( 'NONE', *, *, #66454, .T. ) ;
#72946=EDGE_CURVE ( 'NONE', #58641, #105730, #22480, .T. ) ;
#72989=CARTESIAN_POINT ( 'NONE',  ( 59.41111111111111143, 6.915964383211875250E-15, 0.000000000000000000 ) ) ;
#72999=FACE_OUTER_BOUND ( 'NONE', #106477, .T. ) ;
#73017=DIRECTION ( 'NONE',  ( -0.5735764363510494901, -0.8191520442889894671, 0.000000000000000000 ) ) ;
#73050=CARTESIAN_POINT ( 'NONE',  ( 60.14984002819952025, 4.898587196589294500E-16, -4.000000000000007105 ) ) ;
#73086=CARTESIAN_POINT ( 'NONE',  ( 60.14984002819952025, -4.000000000000000000, 0.000000000000000000 ) ) ;
#73095=AXIS2_PLACEMENT_3D ( 'NONE', #104248, #72417, #38486 ) ;
#73120=CARTESIAN_POINT ( 'NONE',  ( 0.000000000000000000, 0.000000000000000000, 0.000000000000000000 ) ) ;
#73123=ORIENTED_EDGE ( 'NONE', *, *, #92736, .T. ) ;
#73126=DIRECTION ( 'NONE',  ( -1.000000000000000000, -1.224606353822377258E-16, -0.000000000000000000 ) ) ;
#73141=EDGE_LOOP ( 'NONE', ( #106666, #67779, #78627, #53715, #14981 ) ) ;
#73146=AXIS2_PLACEMENT_3D ( 'NONE', #67157, #100042, #101111 ) ;
#73148=( LENGTH_UNIT ( ) NAMED_UNIT ( * ) SI_UNIT ( .MILLI., .METRE. ) );
#73192=ORIENTED_EDGE ( 'NONE', *, *, #61290, .T. ) ;
#73244=ORIENTED_EDGE ( 'NONE', *, *, #2521, .T. ) ;
#73255=CARTESIAN_POINT ( 'NONE',  ( 61.11682663846713837, -4.000000000000000888, 4.898587196589422689E-16 ) ) ;
#73278=ORIENTED_EDGE ( 'NONE', *, *, #44946, .T. ) ;
#73352=ORIENTED_EDGE ( 'NONE', *, *, #106466, .T. ) ;
#73384=FACE_OUTER_BOUND ( 'NONE', #90481, .T. ) ;
#73387=DIRECTION ( 'NONE',  ( 0.000000000000000000, 0.000000000000000000, 1.000000000000000000 ) ) ;
#73396=ORIENTED_EDGE ( 'NONE', *, *, #32651, .F. ) ;
#73401=EDGE_CURVE ( 'NONE', #48389, #27209, #58707, .T. ) ;
#73428=EDGE_CURVE ( 'NONE', #63624, #96955, #96593, .T. ) ;
#73503=DIRECTION ( 'NONE',  ( 1.000000000000000000, 0.000000000000000000, -0.000000000000000000 ) ) ;
#73530=AXIS2_PLACEMENT_3D ( 'NONE', #30123, #39276, #46292 ) ;
#73546=ORIENTED_EDGE ( 'NONE', *, *, #6680, .F. ) ;
#73555=VECTOR ( 'NONE', #81839, 1000.000000000000000 ) ;
#73556=DIRECTION ( 'NONE',  ( -1.000000000000000000, -1.224606353822377258E-16, -0.000000000000000000 ) ) ;
#73561=FACE_OUTER_BOUND ( 'NONE', #44743, .T. ) ;
#73568=CIRCLE ( 'NONE', #20383, 4.000000000000007105 ) ;
#73640=ADVANCED_FACE ( 'NONE', ( #79209 ), #69015, .T. ) ;
#73675=FACE_OUTER_BOUND ( 'NONE', #67971, .T. ) ;
#73688=EDGE_CURVE ( 'NONE', #103417, #53703, #48440, .T. ) ;
#73703=UNCERTAINTY_MEASURE_WITH_UNIT (LENGTH_MEASURE( 1.000000000000000082E-05 ), #40480, 'distance_accuracy_value', 'NONE');
#73743=AXIS2_PLACEMENT_3D ( 'NONE', #39437, #12469, #105217 ) ;
#73822=EDGE_LOOP ( 'NONE', ( #32788, #104449, #16945, #73244, #7867 ) ) ;
#73892=EDGE_CURVE ( 'NONE', #53703, #55070, #92610, .T. ) ;
#73945=FACE_OUTER_BOUND ( 'NONE', #72555, .T. ) ;
#73946=DIRECTION ( 'NONE',  ( 0.5735764363510442720, -0.8191520442889930198, 1.003171929053526349E-16 ) ) ;
#73950=CARTESIAN_POINT ( 'NONE',  ( 73.33904886068935980, -1.232595164407830946E-29, 4.000000000000007105 ) ) ;
#73955=ORIENTED_EDGE ( 'NONE', *, *, #91027, .T. ) ;
#73982=DIRECTION ( 'NONE',  ( 0.000000000000000000, -1.000000000000000000, 0.000000000000000000 ) ) ;
#73986=EDGE_CURVE ( 'NONE', #57259, #40695, #20952, .T. ) ;
#74003=EDGE_CURVE ( 'NONE', #66339, #70791, #10098, .T. ) ;
#74017=CIRCLE ( 'NONE', #77505, 4.000000000000007105 ) ;
#74021=EDGE_CURVE ( 'NONE', #38361, #98861, #94987, .T. ) ;
#74034=EDGE_LOOP ( 'NONE', ( #32679, #22764, #59522, #89703 ) ) ;
#74047=DIRECTION ( 'NONE',  ( -1.000000000000000000, -0.000000000000000000, -0.000000000000000000 ) ) ;
#74050=AXIS2_PLACEMENT_3D ( 'NONE', #46266, #61940, #70543 ) ;
#74077=EDGE_CURVE ( 'NONE', #85895, #3882, #85608, .T. ) ;
#74091=DIRECTION ( 'NONE',  ( 0.000000000000000000, -1.000000000000000000, 0.000000000000000000 ) ) ;
#74130=ORIENTED_EDGE ( 'NONE', *, *, #20778, .F. ) ;
#74158=EDGE_CURVE ( 'NONE', #84731, #38550, #44616, .T. ) ;
#74183=DIRECTION ( 'NONE',  ( -1.000000000000000000, -1.224606353822377258E-16, -0.000000000000000000 ) ) ;
#74218=AXIS2_PLACEMENT_3D ( 'NONE', #91333, #49787, #17448 ) ;
#74221=ORIENTED_EDGE ( 'NONE', *, *, #50537, .F. ) ;
#74241=EDGE_CURVE ( 'NONE', #31918, #82092, #96690, .T. ) ;
#74255=DIRECTION ( 'NONE',  ( 0.000000000000000000, -1.000000000000000000, 0.000000000000000000 ) ) ;
#74264=CARTESIAN_POINT ( 'NONE',  ( 54.52222222222221859, 6.915964383211875250E-15, 0.000000000000000000 ) ) ;
#74281=CARTESIAN_POINT ( 'NONE',  ( 59.89460441624491693, 6.975173280561618775E-15, 0.000000000000000000 ) ) ;
#74291=CARTESIAN_POINT ( 'NONE',  ( 60.14984002819952025, 6.856755485862130937E-15, 0.000000000000000000 ) ) ;
#74422=CARTESIAN_POINT ( 'NONE',  ( 5.299999999999999822, -3.752776749732578132, -6.500000000000000888 ) ) ;
#74438=ORIENTED_EDGE ( 'NONE', *, *, #2495, .T. ) ;
#74443=FACE_OUTER_BOUND ( 'NONE', #87160, .T. ) ;
#74450=VECTOR ( 'NONE', #77716, 1000.000000000000000 ) ;
#74604=AXIS2_PLACEMENT_3D ( 'NONE', #49595, #474, #8605 ) ;
#74623=DIRECTION ( 'NONE',  ( 0.000000000000000000, 0.000000000000000000, 1.000000000000000000 ) ) ;
#74632=AXIS2_PLACEMENT_3D ( 'NONE', #97792, #23956, #88652 ) ;
#74640=LINE ( 'NONE', #83275, #102966 ) ;
#74641=ORIENTED_EDGE ( 'NONE', *, *, #64124, .T. ) ;
#74704=ORIENTED_EDGE ( 'NONE', *, *, #43376, .T. ) ;
#74757=ORIENTED_EDGE ( 'NONE', *, *, #94422, .T. ) ;
#74763=CARTESIAN_POINT ( 'NONE',  ( 74.56127108291157413, 6.975173280561618775E-15, 0.000000000000000000 ) ) ;
#74774=DIRECTION ( 'NONE',  ( 0.000000000000000000, -1.000000000000000000, 0.000000000000000000 ) ) ;
#74779=CIRCLE ( 'NONE', #28324, 3.309500000000007880 ) ;
#74796=ORIENTED_EDGE ( 'NONE', *, *, #70621, .F. ) ;
#74797=DIRECTION ( 'NONE',  ( 0.000000000000000000, -1.000000000000000000, 0.000000000000000000 ) ) ;
#74808=EDGE_LOOP ( 'NONE', ( #41631, #38773, #106618 ) ) ;
#74812=CARTESIAN_POINT ( 'NONE',  ( 0.000000000000000000, 0.000000000000000000, 0.000000000000000000 ) ) ;
#74817=CIRCLE ( 'NONE', #42099, 6.499999999999999112 ) ;
#74818=DIRECTION ( 'NONE',  ( -1.000000000000000000, -1.224606353822377258E-16, -0.000000000000000000 ) ) ;
#74870=CONICAL_SURFACE ( 'NONE', #76576, 3.309500000000007880, 0.9599310885968770357 ) ;
#74880=EDGE_CURVE ( 'NONE', #35260, #105857, #62402, .T. ) ;
#74969=CONICAL_SURFACE ( 'NONE', #23363, 4.000000000000007105, 0.9599310885968835860 ) ;
#75000=DIRECTION ( 'NONE',  ( 0.000000000000000000, -1.000000000000000000, 0.000000000000000000 ) ) ;
#75011=DIRECTION ( 'NONE',  ( 1.000000000000000000, 0.000000000000000000, -0.000000000000000000 ) ) ;
#75046=VECTOR ( 'NONE', #36776, 1000.000000000000000 ) ;
#75093=EDGE_CURVE ( 'NONE', #81361, #103201, #97929, .T. ) ;
#75115=CONICAL_SURFACE ( 'NONE', #106069, 3.309500000000007880, 0.9599310885968770357 ) ;
#75117=LINE ( 'NONE', #84827, #21125 ) ;
#75153=DIRECTION ( 'NONE',  ( -1.000000000000000000, -0.000000000000000000, -0.000000000000000000 ) ) ;
#75190=FACE_OUTER_BOUND ( 'NONE', #67859, .T. ) ;
#75206=AXIS2_PLACEMENT_3D ( 'NONE', #88034, #88559, #47548 ) ;
#75248=CARTESIAN_POINT ( 'NONE',  ( 54.03872891708841308, 6.856755485862130937E-15, 0.000000000000000000 ) ) ;
#75269=DIRECTION ( 'NONE',  ( -1.000000000000000000, -0.000000000000000000, -0.000000000000000000 ) ) ;
#75286=EDGE_LOOP ( 'NONE', ( #85181, #6005, #82318, #8571, #46635 ) ) ;
#75303=DIRECTION ( 'NONE',  ( -1.000000000000000000, -0.000000000000000000, -0.000000000000000000 ) ) ;
#75305=ORIENTED_EDGE ( 'NONE', *, *, #34964, .T. ) ;
#75314=EDGE_LOOP ( 'NONE', ( #9539, #58897, #45956, #63505, #71916, #106758 ) ) ;
#75318=DIRECTION ( 'NONE',  ( 0.000000000000000000, -1.000000000000000000, 0.000000000000000000 ) ) ;
#75334=CARTESIAN_POINT ( 'NONE',  ( 65.03872891708842019, 6.856755485862130937E-15, 0.000000000000000000 ) ) ;
#75390=CIRCLE ( 'NONE', #32306, 4.000000000000007105 ) ;
#75396=ORIENTED_EDGE ( 'NONE', *, *, #97127, .T. ) ;
#75414=EDGE_CURVE ( 'NONE', #99696, #69600, #102976, .T. ) ;
#75420=VERTEX_POINT ( 'NONE', #36961 ) ;
#75435=ORIENTED_EDGE ( 'NONE', *, *, #14263, .T. ) ;
#75443=CARTESIAN_POINT ( 'NONE',  ( 64.78349330513380266, 6.975173280561618775E-15, 0.000000000000000000 ) ) ;
#75445=LINE ( 'NONE', #99176, #30710 ) ;
#75454=DIRECTION ( 'NONE',  ( 0.000000000000000000, -1.000000000000000000, 0.000000000000000000 ) ) ;
#75459=CONICAL_SURFACE ( 'NONE', #29025, 6.499999999999999112, 1.047197551196600296 ) ;
#75472=ORIENTED_EDGE ( 'NONE', *, *, #87507, .F. ) ;
#75475=DIRECTION ( 'NONE',  ( -1.000000000000000000, -1.224606353822377258E-16, -0.000000000000000000 ) ) ;
#75516=CYLINDRICAL_SURFACE ( 'NONE', #82299, 4.000000000000000000 ) ;
#75526=AXIS2_PLACEMENT_3D ( 'NONE', #7504, #88982, #63662 ) ;
#75606=AXIS2_PLACEMENT_3D ( 'NONE', #28622, #86318, #21582 ) ;
#75622=ORIENTED_EDGE ( 'NONE', *, *, #37880, .T. ) ;
#75659=CARTESIAN_POINT ( 'NONE',  ( 55.00571552735602410, 6.975173280561618775E-15, 0.000000000000000000 ) ) ;
#75690=AXIS2_PLACEMENT_3D ( 'NONE', #65767, #80336, #98126 ) ;
#75720=DIRECTION ( 'NONE',  ( -1.000000000000000000, -1.224606353822377258E-16, -0.000000000000000000 ) ) ;
#75746=ORIENTED_EDGE ( 'NONE', *, *, #84299, .F. ) ;
#75804=VERTEX_POINT ( 'NONE', #77257 ) ;
#75824=ORIENTED_EDGE ( 'NONE', *, *, #28158, .F. ) ;
#75852=EDGE_CURVE ( 'NONE', #19599, #57235, #63427, .T. ) ;
#75872=VERTEX_POINT ( 'NONE', #89595 ) ;
#75921=CARTESIAN_POINT ( 'NONE',  ( 0.1061556211655365900, -6.421950209808287013, -1.876855952934446847 ) ) ;
#75957=DIRECTION ( 'NONE',  ( 0.5735764363510440500, 0.8191520442889932418, 0.000000000000000000 ) ) ;
#76013=VECTOR ( 'NONE', #103310, 1000.000000000000000 ) ;
#76020=ORIENTED_EDGE ( 'NONE', *, *, #8222, .T. ) ;
#76027=EDGE_CURVE ( 'NONE', #35260, #99128, #23285, .T. ) ;
#76043=DIRECTION ( 'NONE',  ( 0.000000000000000000, 0.000000000000000000, 1.000000000000000000 ) ) ;
#76071=CARTESIAN_POINT ( 'NONE',  ( 68.45015997180047407, 4.898587196589294500E-16, -4.000000000000007105 ) ) ;
#76073=B_SPLINE_CURVE_WITH_KNOTS ( 'NONE', 3,
 ( #47835, #16017, #7916, #48896, #81790, #90442 ),
 .UNSPECIFIED., .F., .F.,
 ( 4, 2, 4 ),
 ( 2.380733003145476372E-07, 0.001898835937927386775, 0.003797433802554458452 ),
 .UNSPECIFIED. ) ;
#76149=FACE_OUTER_BOUND ( 'NONE', #65249, .T. ) ;
#76171=CARTESIAN_POINT ( 'NONE',  ( 4.699999999999999289, -3.752776749732579020, -6.500000000000000888 ) ) ;
#76216=CONICAL_SURFACE ( 'NONE', #12708, 4.000000000000007105, 0.9599310885968835860 ) ;
#76230=DIRECTION ( 'NONE',  ( -0.5735764363510494901, -0.8191520442889894671, 0.000000000000000000 ) ) ;
#76247=DIRECTION ( 'NONE',  ( 0.000000000000000000, -1.000000000000000000, 0.000000000000000000 ) ) ;
#76265=DIRECTION ( 'NONE',  ( -1.000000000000000000, -1.224606353822377258E-16, -0.000000000000000000 ) ) ;
#76271=DIRECTION ( 'NONE',  ( 0.000000000000000000, -1.000000000000000000, 0.000000000000000000 ) ) ;
#76274=VERTEX_POINT ( 'NONE', #28084 ) ;
#76277=CIRCLE ( 'NONE', #29810, 3.309500000000007880 ) ;
#76324=AXIS2_PLACEMENT_3D ( 'NONE', #58499, #740, #9381 ) ;
#76370=DIRECTION ( 'NONE',  ( 1.000000000000000000, 1.224606353822377258E-16, 0.000000000000000000 ) ) ;
#76378=AXIS2_PLACEMENT_3D ( 'NONE', #2411, #53102, #86025 ) ;
#76379=CARTESIAN_POINT ( 'NONE',  ( 66.74444444444444002, -3.309500000000000774, 4.475777889183797681E-16 ) ) ;
#76383=ORIENTED_EDGE ( 'NONE', *, *, #94623, .T. ) ;
#76396=DIRECTION ( 'NONE',  ( -1.000000000000000000, -1.224606353822377258E-16, -0.000000000000000000 ) ) ;
#76408=EDGE_CURVE ( 'NONE', #42218, #102336, #77163, .T. ) ;
#76443=ADVANCED_FACE ( 'NONE', ( #81216 ), #40243, .T. ) ;
#76472=CIRCLE ( 'NONE', #81612, 3.309500000000007880 ) ;
#76494=ORIENTED_EDGE ( 'NONE', *, *, #99492, .T. ) ;
#76519=VERTEX_POINT ( 'NONE', #98307 ) ;
#76576=AXIS2_PLACEMENT_3D ( 'NONE', #72271, #45884, #64204 ) ;
#76588=CONICAL_SURFACE ( 'NONE', #30131, 3.309500000000007880, 0.9599310885968770357 ) ;
#76590=AXIS2_PLACEMENT_3D ( 'NONE', #76727, #9864, #35792 ) ;
#76610=CARTESIAN_POINT ( 'NONE',  ( 66.26095113931063452, -1.232595164407830946E-29, 4.000000000000007105 ) ) ;
#76643=DIRECTION ( 'NONE',  ( 0.000000000000000000, 1.000000000000000000, 0.000000000000000000 ) ) ;
#76684=DIRECTION ( 'NONE',  ( -1.000000000000000000, -0.000000000000000000, -0.000000000000000000 ) ) ;
#76687=CARTESIAN_POINT ( 'NONE',  ( 69.18888888888888289, 3.309500000000014541, 0.000000000000000000 ) ) ;
#76719=CARTESIAN_POINT ( 'NONE',  ( 56.96666666666666856, 3.309500000000014541, 0.000000000000000000 ) ) ;
#76721=AXIS2_PLACEMENT_3D ( 'NONE', #19720, #94095, #28880 ) ;
#76727=CARTESIAN_POINT ( 'NONE',  ( 0.000000000000000000, 0.000000000000000000, 0.000000000000000000 ) ) ;
#76795=CARTESIAN_POINT ( 'NONE',  ( 59.89460441624491693, 6.975173280561618775E-15, 0.000000000000000000 ) ) ;
#76805=CARTESIAN_POINT ( 'NONE',  ( 56.22793774957824553, 6.975173280561618775E-15, 0.000000000000000000 ) ) ;
#76807=CARTESIAN_POINT ( 'NONE',  ( 72.85555555555556850, -3.309500000000000774, 4.475777889183797681E-16 ) ) ;
#76817=CIRCLE ( 'NONE', #97504, 4.000000000000007105 ) ;
#76819=DIRECTION ( 'NONE',  ( 0.000000000000000000, -1.000000000000000000, 0.000000000000000000 ) ) ;
#76824=CONICAL_SURFACE ( 'NONE', #95792, 6.499999999999999112, 1.047197551196600296 ) ;
#76828=CIRCLE ( 'NONE', #90619, 4.000000000000007105 ) ;
#76831=DIRECTION ( 'NONE',  ( -1.000000000000000000, -0.000000000000000000, -0.000000000000000000 ) ) ;
#76834=FACE_OUTER_BOUND ( 'NONE', #88237, .T. ) ;
#76878=APPLICATION_CONTEXT ( 'automotive_design' ) ;
#76888=DIRECTION ( 'NONE',  ( 0.000000000000000000, 0.000000000000000000, -1.000000000000000000 ) ) ;
#76890=EDGE_CURVE ( 'NONE', #48389, #16756, #79338, .T. ) ;
#76935=CARTESIAN_POINT ( 'NONE',  ( 55.26095113931063452, 6.856755485862130937E-15, 0.000000000000000000 ) ) ;
#76941=DIRECTION ( 'NONE',  ( 1.000000000000000000, 1.224606353822377258E-16, 0.000000000000000000 ) ) ;
#76977=EDGE_CURVE ( 'NONE', #86973, #82907, #41152, .T. ) ;
#76993=CONICAL_SURFACE ( 'NONE', #27072, 3.309500000000007880, 0.9599310885968770357 ) ;
#76995=DIRECTION ( 'NONE',  ( 0.000000000000000000, 0.000000000000000000, 1.000000000000000000 ) ) ;
#77001=DIRECTION ( 'NONE',  ( -1.000000000000000000, -1.224606353822377258E-16, -0.000000000000000000 ) ) ;
#77007=DIRECTION ( 'NONE',  ( 0.000000000000000000, -1.000000000000000000, 0.000000000000000000 ) ) ;
#77084=AXIS2_PLACEMENT_3D ( 'NONE', #53588, #78388, #4505 ) ;
#77113=ORIENTED_EDGE ( 'NONE', *, *, #103584, .T. ) ;
#77134=AXIS2_PLACEMENT_3D ( 'NONE', #93198, #35528, #102348 ) ;
#77140=ORIENTED_EDGE ( 'NONE', *, *, #11871, .T. ) ;
#77163=B_SPLINE_CURVE_WITH_KNOTS ( 'NONE', 3,
 ( #24099, #37768, #29675, #56941, #33239, #45828 ),
 .UNSPECIFIED., .F., .F.,
 ( 4, 2, 4 ),
 ( 2.380733003139562229E-07, 0.001898835937927378101, 0.003797433802554441972 ),
 .UNSPECIFIED. ) ;
#77166=ORIENTED_EDGE ( 'NONE', *, *, #61304, .T. ) ;
#77197=CARTESIAN_POINT ( 'NONE',  ( 0.4053525175236797340, 3.145852061456238413, -6.500000000000000000 ) ) ;
#77245=LINE ( 'NONE', #70741, #102518 ) ;
#77257=CARTESIAN_POINT ( 'NONE',  ( 4.699999999999999289, 7.505553499465139389, 0.000000000000000000 ) ) ;
#77259=CIRCLE ( 'NONE', #25562, 4.000000000000007105 ) ;
#77268=DIRECTION ( 'NONE',  ( 0.000000000000000000, 1.000000000000000000, 0.000000000000000000 ) ) ;
#77274=ORIENTED_EDGE ( 'NONE', *, *, #72946, .F. ) ;
#77304=LINE ( 'NONE', #2333, #72249 ) ;
#77324=CARTESIAN_POINT ( 'NONE',  ( 73.33904886068935980, 6.975173280561618775E-15, 0.000000000000000000 ) ) ;
#77327=CARTESIAN_POINT ( 'NONE',  ( 61.11682663846713837, 4.000000000000014211, 0.000000000000000000 ) ) ;
#77340=AXIS2_PLACEMENT_3D ( 'NONE', #73120, #106025, #32170 ) ;
#77347=CARTESIAN_POINT ( 'NONE',  ( 62.59428447264396311, 6.856755485862130937E-15, 0.000000000000000000 ) ) ;
#77362=ORIENTED_EDGE ( 'NONE', *, *, #57360, .F. ) ;
#77398=EDGE_LOOP ( 'NONE', ( #89471, #79118, #63677, #85350, #84275 ) ) ;
#77433=CARTESIAN_POINT ( 'NONE',  ( 63.56127108291158123, -1.232595164407830946E-29, 4.000000000000007105 ) ) ;
#77453=AXIS2_PLACEMENT_3D ( 'NONE', #91676, #75475, #50641 ) ;
#77490=ORIENTED_EDGE ( 'NONE', *, *, #97127, .F. ) ;
#77499=FACE_OUTER_BOUND ( 'NONE', #89793, .T. ) ;
#77505=AXIS2_PLACEMENT_3D ( 'NONE', #60108, #1274, #100524 ) ;
#77521=CARTESIAN_POINT ( 'NONE',  ( 74.60950000000003968, 0.000000000000000000, 4.000000000000000000 ) ) ;
#77550=AXIS2_PLACEMENT_3D ( 'NONE', #67783, #60773, #11654 ) ;
#77590=ORIENTED_EDGE ( 'NONE', *, *, #56497, .T. ) ;
#77594=FACE_OUTER_BOUND ( 'NONE', #101718, .T. ) ;
#77596=CARTESIAN_POINT ( 'NONE',  ( 0.000000000000000000, 0.000000000000000000, 0.000000000000000000 ) ) ;
#77635=AXIS2_PLACEMENT_3D ( 'NONE', #874, #33851, #43515 ) ;
#77636=EDGE_CURVE ( 'NONE', #20792, #91765, #15500, .T. ) ;
#77638=VECTOR ( 'NONE', #41290, 1000.000000000000114 ) ;
#77660=DIRECTION ( 'NONE',  ( 1.000000000000000000, 1.224606353822377258E-16, 0.000000000000000000 ) ) ;
#77672=DIRECTION ( 'NONE',  ( -1.000000000000000000, -1.224606353822377258E-16, -0.000000000000000000 ) ) ;
#77702=ORIENTED_EDGE ( 'NONE', *, *, #16330, .F. ) ;
#77716=DIRECTION ( 'NONE',  ( -1.000000000000000000, -0.000000000000000000, -0.000000000000000000 ) ) ;
#77769=AXIS2_PLACEMENT_3D ( 'NONE', #4110, #54220, #38614 ) ;
#77771=SHAPE_REPRESENTATION ( 'hex bolt gradeab_din_DIN EN 24014 - M8 x 70 x 22-S', ( #10728 ), #66175 ) ;
#77773=DIRECTION ( 'NONE',  ( 0.000000000000000000, 0.000000000000000000, -1.000000000000000000 ) ) ;
#77790=EDGE_CURVE ( 'NONE', #37936, #98735, #1708, .T. ) ;
#77838=CARTESIAN_POINT ( 'NONE',  ( 61.85555555555556140, 3.309500000000014541, 0.000000000000000000 ) ) ;
#77854=DIRECTION ( 'NONE',  ( -1.000000000000000000, -1.224606353822377258E-16, -0.000000000000000000 ) ) ;
#77883=VERTEX_POINT ( 'NONE', #56239 ) ;
#77981=CIRCLE ( 'NONE', #15989, 4.000000000000007105 ) ;
#77989=CARTESIAN_POINT ( 'NONE',  ( 57.70539558375507738, 6.856755485862130937E-15, 0.000000000000000000 ) ) ;
#78019=CIRCLE ( 'NONE', #31532, 6.499999999999999112 ) ;
#78022=ORIENTED_EDGE ( 'NONE', *, *, #100420, .T. ) ;
#78050=FACE_OUTER_BOUND ( 'NONE', #95991, .T. ) ;
#78073=ORIENTED_EDGE ( 'NONE', *, *, #65903, .T. ) ;
#78082=CYLINDRICAL_SURFACE ( 'NONE', #65116, 6.499999999999999112 ) ;
#78109=EDGE_CURVE ( 'NONE', #90738, #98861, #51357, .T. ) ;
#78120=ORIENTED_EDGE ( 'NONE', *, *, #63735, .F. ) ;
#78157=AXIS2_PLACEMENT_3D ( 'NONE', #16388, #89232, #32610 ) ;
#78175=DIRECTION ( 'NONE',  ( 0.000000000000000000, 0.000000000000000000, 1.000000000000000000 ) ) ;
#78193=CARTESIAN_POINT ( 'NONE',  ( 63.81650669486618455, -4.000000000000000000, 0.000000000000000000 ) ) ;
#78237=LINE ( 'NONE', #52361, #32376 ) ;
#78346=DIRECTION ( 'NONE',  ( -1.000000000000000000, -0.000000000000000000, -0.000000000000000000 ) ) ;
#78347=EDGE_LOOP ( 'NONE', ( #56937, #77113, #89782, #47617, #10788 ) ) ;
#78349=CARTESIAN_POINT ( 'NONE',  ( 66.00571552735603120, 4.898587196589294500E-16, -4.000000000000007105 ) ) ;
#78386=AXIS2_PLACEMENT_3D ( 'NONE', #23259, #57180, #71771 ) ;
#78388=DIRECTION ( 'NONE',  ( 1.000000000000000000, 0.000000000000000000, 0.000000000000000000 ) ) ;
#78515=FACE_OUTER_BOUND ( 'NONE', #11469, .T. ) ;
#78529=CIRCLE ( 'NONE', #106067, 4.000000000000007105 ) ;
#78545=CYLINDRICAL_SURFACE ( 'NONE', #45078, 4.000000000000000000 ) ;
#78552=DIRECTION ( 'NONE',  ( -0.5735764363510497121, 0.8191520442889892450, 1.003171929053521665E-16 ) ) ;
#78576=EDGE_CURVE ( 'NONE', #76274, #5888, #23141, .T. ) ;
#78586=DIRECTION ( 'NONE',  ( -1.000000000000000000, -1.224606353822377258E-16, -0.000000000000000000 ) ) ;
#78598=CARTESIAN_POINT ( 'NONE',  ( 69.67238219402268840, 6.975173280561618775E-15, 0.000000000000000000 ) ) ;
#78627=ORIENTED_EDGE ( 'NONE', *, *, #20778, .T. ) ;
#78702=EDGE_CURVE ( 'NONE', #79305, #60384, #12107, .T. ) ;
#78711=DIRECTION ( 'NONE',  ( -1.000000000000000000, -1.224606353822377258E-16, -0.000000000000000000 ) ) ;
#78726=DIRECTION ( 'NONE',  ( 1.000000000000000000, 1.224606353822377258E-16, 0.000000000000000000 ) ) ;
#78740=AXIS2_PLACEMENT_3D ( 'NONE', #102102, #85402, #2870 ) ;
#78741=CARTESIAN_POINT ( 'NONE',  ( 4.699999999999999289, -7.505553499465137612, 3.546421054897781431E-16 ) ) ;
#78745=CARTESIAN_POINT ( 'NONE',  ( 68.70539558375507738, 4.000000000000015099, 4.898587196589422689E-16 ) ) ;
#78797=CARTESIAN_POINT ( 'NONE',  ( 67.96666666666666856, 3.309500000000014541, 4.052968581778174646E-16 ) ) ;
#78849=DIRECTION ( 'NONE',  ( 0.000000000000000000, 0.000000000000000000, 1.000000000000000000 ) ) ;
#78877=FACE_OUTER_BOUND ( 'NONE', #37954, .T. ) ;
#78882=FACE_OUTER_BOUND ( 'NONE', #99316, .T. ) ;
#78894=DIRECTION ( 'NONE',  ( 0.000000000000000000, -1.000000000000000000, 0.000000000000000000 ) ) ;
#78929=CARTESIAN_POINT ( 'NONE',  ( 52.81650669486619165, 4.000000000000015099, 4.898587196589422689E-16 ) ) ;
#78951=DIRECTION ( 'NONE',  ( 0.000000000000000000, -1.000000000000000000, 0.000000000000000000 ) ) ;
#78969=CONICAL_SURFACE ( 'NONE', #53112, 4.000000000000007105, 0.9599310885968835860 ) ;
#78995=DIRECTION ( 'NONE',  ( 0.000000000000000000, -1.000000000000000000, 0.000000000000000000 ) ) ;
#79000=EDGE_CURVE ( 'NONE', #40074, #95890, #44927, .T. ) ;
#79026=CARTESIAN_POINT ( 'NONE',  ( 5.299999999999999822, 3.752776749732553263, -6.499999999999999112 ) ) ;
#79029=EDGE_LOOP ( 'NONE', ( #26388, #95386, #38755, #29594, #60624 ) ) ;
#79084=CARTESIAN_POINT ( 'NONE',  ( 71.14984002819953446, 6.856755485862130937E-15, 0.000000000000000000 ) ) ;
#79096=EDGE_CURVE ( 'NONE', #11751, #6495, #82276, .T. ) ;
#79102=EDGE_CURVE ( 'NONE', #55070, #103417, #40230, .T. ) ;
#79103=ADVANCED_FACE ( 'NONE', ( #80676 ), #62183, .T. ) ;
#79118=ORIENTED_EDGE ( 'NONE', *, *, #74880, .T. ) ;
#79155=DIRECTION ( 'NONE',  ( 1.000000000000000000, 1.224606353822377258E-16, 0.000000000000000000 ) ) ;
#79172=VECTOR ( 'NONE', #36299, 1000.000000000000000 ) ;
#79179=ORIENTED_EDGE ( 'NONE', *, *, #100161, .T. ) ;
#79209=FACE_OUTER_BOUND ( 'NONE', #88161, .T. ) ;
#79220=CONICAL_SURFACE ( 'NONE', #74050, 3.309500000000007880, 0.9599310885968770357 ) ;
#79247=AXIS2_PLACEMENT_3D ( 'NONE', #9590, #42503, #34459 ) ;
#79255=CARTESIAN_POINT ( 'NONE',  ( 54.52222222222221859, 6.915964383211875250E-15, 0.000000000000000000 ) ) ;
#79299=ORIENTED_EDGE ( 'NONE', *, *, #61966, .F. ) ;
#79305=VERTEX_POINT ( 'NONE', #63201 ) ;
#79338=LINE ( 'NONE', #95528, #3269 ) ;
#79341=CARTESIAN_POINT ( 'NONE',  ( 5.299999999999999822, 0.000000000000000000, 0.000000000000000000 ) ) ;
#79371=ORIENTED_EDGE ( 'NONE', *, *, #32936, .T. ) ;
#79454=DIRECTION ( 'NONE',  ( 0.000000000000000000, -1.000000000000000000, 0.000000000000000000 ) ) ;
#79502=VERTEX_POINT ( 'NONE', #83603 ) ;
#79549=CARTESIAN_POINT ( 'NONE',  ( 0.000000000000000000, 0.000000000000000000, 0.000000000000000000 ) ) ;
#79573=CARTESIAN_POINT ( 'NONE',  ( 62.33904886068935980, 4.000000000000013323, 0.000000000000000000 ) ) ;
#79590=ORIENTED_EDGE ( 'NONE', *, *, #43399, .T. ) ;
#79618=CARTESIAN_POINT ( 'NONE',  ( 0.1061556211655305393, 4.836380039389409191, -4.623144047065556705 ) ) ;
#79637=DIRECTION ( 'NONE',  ( 0.000000000000000000, -1.000000000000000000, 0.000000000000000000 ) ) ;
#79644=DIRECTION ( 'NONE',  ( -1.000000000000000000, -1.224606353822377258E-16, -0.000000000000000000 ) ) ;
#79667=ORIENTED_EDGE ( 'NONE', *, *, #14441, .T. ) ;
#79669=DIRECTION ( 'NONE',  ( 0.000000000000000000, -1.000000000000000000, 0.000000000000000000 ) ) ;
#79686=CIRCLE ( 'NONE', #15939, 4.000000000000007105 ) ;
#79737=VECTOR ( 'NONE', #52371, 1000.000000000000000 ) ;
#79788=VECTOR ( 'NONE', #15400, 1000.000000000000000 ) ;
#79798=DIRECTION ( 'NONE',  ( 0.000000000000000000, -1.000000000000000000, 0.000000000000000000 ) ) ;
#79841=EDGE_CURVE ( 'NONE', #103962, #32281, #34705, .T. ) ;
#79849=ORIENTED_EDGE ( 'NONE', *, *, #100752, .F. ) ;
#79961=CARTESIAN_POINT ( 'NONE',  ( 62.59428447264396311, 4.000000000000015099, 4.898587196589422689E-16 ) ) ;
#79962=LINE ( 'NONE', #4497, #27402 ) ;
#79969=CARTESIAN_POINT ( 'NONE',  ( 59.41111111111111143, 3.309500000000014541, 0.000000000000000000 ) ) ;
#79971=ORIENTED_EDGE ( 'NONE', *, *, #7846, .T. ) ;
#79990=EDGE_CURVE ( 'NONE', #58295, #53379, #94981, .T. ) ;
#80037=DIRECTION ( 'NONE',  ( 0.5735764363510440500, 0.8191520442889932418, 0.000000000000000000 ) ) ;
#80038=ADVANCED_FACE ( 'NONE', ( #2030 ), #100732, .T. ) ;
#80039=CIRCLE ( 'NONE', #86937, 4.000000000000007105 ) ;
#80062=DIRECTION ( 'NONE',  ( -1.000000000000000000, -0.000000000000000000, -0.000000000000000000 ) ) ;
#80078=DIRECTION ( 'NONE',  ( 0.000000000000000000, -1.000000000000000000, 0.000000000000000000 ) ) ;
#80130=CIRCLE ( 'NONE', #99060, 3.309500000000007880 ) ;
#80138=CIRCLE ( 'NONE', #30195, 4.000000000000000000 ) ;
#80213=ORIENTED_EDGE ( 'NONE', *, *, #44161, .F. ) ;
#80246=EDGE_LOOP ( 'NONE', ( #9375, #75824, #76383, #34471, #48810, #85681 ) ) ;
#80272=DIRECTION ( 'NONE',  ( 0.5735764363510440500, 0.8191520442889932418, 0.000000000000000000 ) ) ;
#80289=ORIENTED_EDGE ( 'NONE', *, *, #37992, .F. ) ;
#80309=DIRECTION ( 'NONE',  ( -0.5735764363510497121, 0.8191520442889892450, 1.003171929053521665E-16 ) ) ;
#80312=CYLINDRICAL_SURFACE ( 'NONE', #83986, 4.000000000000000000 ) ;
#80323=CARTESIAN_POINT ( 'NONE',  ( 4.699999999999999289, -5.629165124598843661, 3.250000000000010658 ) ) ;
#80334=CARTESIAN_POINT ( 'NONE',  ( 63.07777777777777573, 6.915964383211875250E-15, 0.000000000000000000 ) ) ;
#80336=DIRECTION ( 'NONE',  ( -1.000000000000000000, -0.000000000000000000, -0.000000000000000000 ) ) ;
#80398=ORIENTED_EDGE ( 'NONE', *, *, #93956, .T. ) ;
#80431=DIRECTION ( 'NONE',  ( -1.000000000000000000, -1.224606353822377258E-16, -0.000000000000000000 ) ) ;
#80506=DIRECTION ( 'NONE',  ( 0.5735764363510440500, 0.8191520442889932418, 0.000000000000000000 ) ) ;
#80508=EDGE_CURVE ( 'NONE', #28791, #13515, #17281, .T. ) ;
#80512=CIRCLE ( 'NONE', #1269, 4.000000000000007105 ) ;
#80556=FACE_OUTER_BOUND ( 'NONE', #55488, .T. ) ;
#80565=ORIENTED_EDGE ( 'NONE', *, *, #30719, .T. ) ;
#80567=ADVANCED_FACE ( 'NONE', ( #102812 ), #72462, .F. ) ;
#80656=CARTESIAN_POINT ( 'NONE',  ( 67.96666666666666856, -3.309500000000000774, 0.000000000000000000 ) ) ;
#80676=FACE_OUTER_BOUND ( 'NONE', #851, .T. ) ;
#80696=VERTEX_POINT ( 'NONE', #96324 ) ;
#80704=CARTESIAN_POINT ( 'NONE',  ( 53.78349330513380266, -1.232595164407830946E-29, 4.000000000000007105 ) ) ;
#80716=EDGE_LOOP ( 'NONE', ( #22154, #35866, #104993, #60711, #197, #81610 ) ) ;
#80738=DIRECTION ( 'NONE',  ( -1.000000000000000000, -1.224606353822377258E-16, -0.000000000000000000 ) ) ;
#80740=CARTESIAN_POINT ( 'NONE',  ( 61.11682663846713837, -1.232595164407830946E-29, 4.000000000000007105 ) ) ;
#80797=DIRECTION ( 'NONE',  ( 0.000000000000000000, -1.000000000000000000, 0.000000000000000000 ) ) ;
#80817=VECTOR ( 'NONE', #57862, 1000.000000000000000 ) ;
#80819=LINE ( 'NONE', #6930, #41550 ) ;
#80887=ORIENTED_EDGE ( 'NONE', *, *, #56013, .T. ) ;
#80903=ORIENTED_EDGE ( 'NONE', *, *, #23770, .F. ) ;
#80943=CARTESIAN_POINT ( 'NONE',  ( 57.45015997180046696, -1.232595164407830946E-29, 4.000000000000007105 ) ) ;
#80968=ADVANCED_FACE ( 'NONE', ( #50915 ), #69022, .T. ) ;
#80995=AXIS2_PLACEMENT_3D ( 'NONE', #41777, #58505, #49864 ) ;
#80996=EDGE_CURVE ( 'NONE', #95890, #8224, #82786, .T. ) ;
#80999=CARTESIAN_POINT ( 'NONE',  ( 53.78349330513380266, 4.000000000000013323, 0.000000000000000000 ) ) ;
#81058=VERTEX_POINT ( 'NONE', #16306 ) ;
#81106=CARTESIAN_POINT ( 'NONE',  ( 63.81650669486618455, 4.000000000000015099, 4.898587196589422689E-16 ) ) ;
#81117=AXIS2_PLACEMENT_3D ( 'NONE', #9005, #76396, #41911 ) ;
#81146=LINE ( 'NONE', #56329, #62160 ) ;
#81155=VECTOR ( 'NONE', #39679, 1000.000000000000000 ) ;
#81172=AXIS2_PLACEMENT_3D ( 'NONE', #42463, #83453, #66209 ) ;
#81216=FACE_OUTER_BOUND ( 'NONE', #39545, .T. ) ;
#81244=ADVANCED_FACE ( 'NONE', ( #18467 ), #96642, .T. ) ;
#81268=CARTESIAN_POINT ( 'NONE',  ( 62.59428447264396311, 4.898587196589294500E-16, -4.000000000000007105 ) ) ;
#81355=DIRECTION ( 'NONE',  ( -1.000000000000000000, -1.224606353822377258E-16, -0.000000000000000000 ) ) ;
#81361=VERTEX_POINT ( 'NONE', #11391 ) ;
#81369=ORIENTED_EDGE ( 'NONE', *, *, #47700, .F. ) ;
#81453=EDGE_CURVE ( 'NONE', #101318, #41106, #29239, .T. ) ;
#81459=ORIENTED_EDGE ( 'NONE', *, *, #60626, .F. ) ;
#81482=ORIENTED_EDGE ( 'NONE', *, *, #97534, .T. ) ;
#81490=CARTESIAN_POINT ( 'NONE',  ( 55.00571552735602410, 4.000000000000013323, 0.000000000000000000 ) ) ;
#81520=CIRCLE ( 'NONE', #57433, 4.000000000000007105 ) ;
#81593=CARTESIAN_POINT ( 'NONE',  ( 66.26095113931063452, -4.000000000000000000, 0.000000000000000000 ) ) ;
#81609=AXIS2_PLACEMENT_3D ( 'NONE', #18620, #25114, #51481 ) ;
#81610=ORIENTED_EDGE ( 'NONE', *, *, #28438, .F. ) ;
#81612=AXIS2_PLACEMENT_3D ( 'NONE', #22593, #87299, #21012 ) ;
#81636=CARTESIAN_POINT ( 'NONE',  ( 72.85555555555556850, -3.309500000000000774, 0.000000000000000000 ) ) ;
#81658=ORIENTED_EDGE ( 'NONE', *, *, #74077, .T. ) ;
#81674=LINE ( 'NONE', #90862, #30604 ) ;
#81776=DIRECTION ( 'NONE',  ( -1.000000000000000000, -0.000000000000000000, -0.000000000000000000 ) ) ;
#81790=CARTESIAN_POINT ( 'NONE',  ( -6.010545793716514417E-15, 5.948846446048893455, -2.696295709017758391 ) ) ;
#81839=DIRECTION ( 'NONE',  ( 0.5735764363510440500, 0.8191520442889932418, 0.000000000000000000 ) ) ;
#81867=ORIENTED_EDGE ( 'NONE', *, *, #29467, .F. ) ;
#81886=ORIENTED_EDGE ( 'NONE', *, *, #37992, .T. ) ;
#81893=DIRECTION ( 'NONE',  ( 0.5735764363510442720, -0.8191520442889930198, 1.003171929053526349E-16 ) ) ;
#81896=AXIS2_PLACEMENT_3D ( 'NONE', #102799, #18722, #12177 ) ;
#81922=LINE ( 'NONE', #40953, #11483 ) ;
#81924=CARTESIAN_POINT ( 'NONE',  ( 63.56127108291158123, 4.000000000000013323, 0.000000000000000000 ) ) ;
#81930=EDGE_CURVE ( 'NONE', #87882, #58831, #51894, .T. ) ;
#82053=CARTESIAN_POINT ( 'NONE',  ( 73.59428447264397732, -1.232595164407830946E-29, 4.000000000000007105 ) ) ;
#82092=VERTEX_POINT ( 'NONE', #21533 ) ;
#82127=AXIS2_PLACEMENT_3D ( 'NONE', #28292, #94053, #79454 ) ;
#82176=ORIENTED_EDGE ( 'NONE', *, *, #10088, .F. ) ;
#82249=ADVANCED_FACE ( 'NONE', ( #77499 ), #78545, .T. ) ;
#82259=CARTESIAN_POINT ( 'NONE',  ( 0.4037800551813748862, 7.199367570657604354, 0.5303295852573147728 ) ) ;
#82276=LINE ( 'NONE', #64520, #3582 ) ;
#82283=CIRCLE ( 'NONE', #77134, 4.000000000000007105 ) ;
#82299=AXIS2_PLACEMENT_3D ( 'NONE', #100853, #43161, #76043 ) ;
#82318=ORIENTED_EDGE ( 'NONE', *, *, #101224, .T. ) ;
#82323=EDGE_CURVE ( 'NONE', #93278, #30721, #39901, .T. ) ;
#82342=DIRECTION ( 'NONE',  ( 0.000000000000000000, -1.000000000000000000, 0.000000000000000000 ) ) ;
#82434=CIRCLE ( 'NONE', #96239, 4.000000000000007105 ) ;
#82442=DIRECTION ( 'NONE',  ( -1.000000000000000000, -1.224606353822377258E-16, -0.000000000000000000 ) ) ;
#82447=VERTEX_POINT ( 'NONE', #105865 ) ;
#82465=CARTESIAN_POINT ( 'NONE',  ( 74.60950000000003968, 4.898587196589412829E-16, -4.000000000000000000 ) ) ;
#82476=DIRECTION ( 'NONE',  ( -0.5735764363510494901, -0.8191520442889894671, 0.000000000000000000 ) ) ;
#82529=VERTEX_POINT ( 'NONE', #19575 ) ;
#82537=CARTESIAN_POINT ( 'NONE',  ( 74.07777777777778283, 6.915964383211875250E-15, 0.000000000000000000 ) ) ;
#82547=CIRCLE ( 'NONE', #53231, 6.499999999999999112 ) ;
#82559=EDGE_LOOP ( 'NONE', ( #72791, #81658, #48917, #77362, #82176 ) ) ;
#82574=ORIENTED_EDGE ( 'NONE', *, *, #4983, .F. ) ;
#82602=CARTESIAN_POINT ( 'NONE',  ( 0.000000000000000000, 0.000000000000000000, 4.000000000000000000 ) ) ;
#82654=VERTEX_POINT ( 'NONE', #76687 ) ;
#82658=ORIENTED_EDGE ( 'NONE', *, *, #28103, .T. ) ;
#82678=ORIENTED_EDGE ( 'NONE', *, *, #61085, .T. ) ;
#82680=ADVANCED_FACE ( 'NONE', ( #8764 ), #41669, .T. ) ;
#82681=CARTESIAN_POINT ( 'NONE',  ( 0.000000000000000000, 0.000000000000000000, 0.000000000000000000 ) ) ;
#82690=VECTOR ( 'NONE', #39192, 1000.000000000000227 ) ;
#82712=CARTESIAN_POINT ( 'NONE',  ( 66.00571552735603120, 6.975173280561618775E-15, 0.000000000000000000 ) ) ;
#82714=CARTESIAN_POINT ( 'NONE',  ( 69.92761780597730592, -4.000000000000000000, 0.000000000000000000 ) ) ;
#82717=VECTOR ( 'NONE', #95633, 1000.000000000000000 ) ;
#82749=FACE_OUTER_BOUND ( 'NONE', #99595, .T. ) ;
#82759=DIRECTION ( 'NONE',  ( 0.5735764363510442720, -0.8191520442889930198, 1.003171929053526349E-16 ) ) ;
#82786=CIRCLE ( 'NONE', #80995, 4.000000000000007105 ) ;
#82827=ORIENTED_EDGE ( 'NONE', *, *, #88383, .T. ) ;
#82842=DIRECTION ( 'NONE',  ( 0.000000000000000000, 0.000000000000000000, 1.000000000000000000 ) ) ;
#82845=CARTESIAN_POINT ( 'NONE',  ( 4.699999999999999289, 6.499999999999999112, 0.000000000000000000 ) ) ;
#82849=EDGE_CURVE ( 'NONE', #72747, #21935, #105487, .T. ) ;
#82872=LINE ( 'NONE', #42406, #38001 ) ;
#82897=ORIENTED_EDGE ( 'NONE', *, *, #98895, .F. ) ;
#82904=FACE_OUTER_BOUND ( 'NONE', #77398, .T. ) ;
#82907=VERTEX_POINT ( 'NONE', #40474 ) ;
#82912=DIRECTION ( 'NONE',  ( 0.5735764363510442720, -0.8191520442889930198, 1.003171929053526349E-16 ) ) ;
#82989=LINE ( 'NONE', #57625, #106369 ) ;
#83025=DIRECTION ( 'NONE',  ( -1.000000000000000000, -1.224606353822377258E-16, -0.000000000000000000 ) ) ;
#83028=ORIENTED_EDGE ( 'NONE', *, *, #21689, .T. ) ;
#83101=ORIENTED_EDGE ( 'NONE', *, *, #37880, .F. ) ;
#83109=CARTESIAN_POINT ( 'NONE',  ( 58.18888888888888999, 6.915964383211875250E-15, 0.000000000000000000 ) ) ;
#83140=LINE ( 'NONE', #57782, #101954 ) ;
#83141=ADVANCED_FACE ( 'NONE', ( #7432 ), #5556, .T. ) ;
#83160=CARTESIAN_POINT ( 'NONE',  ( 0.5805565836007582359, 3.752776749732553263, -6.499999999999999112 ) ) ;
#83167=CARTESIAN_POINT ( 'NONE',  ( 63.07777777777777573, 3.309500000000014541, 0.000000000000000000 ) ) ;
#83173=DIRECTION ( 'NONE',  ( -1.000000000000000000, -1.224606353822377258E-16, -0.000000000000000000 ) ) ;
#83187=DIRECTION ( 'NONE',  ( 0.000000000000000000, 0.000000000000000000, 1.000000000000000000 ) ) ;
#83275=CARTESIAN_POINT ( 'NONE',  ( 66.00571552735603120, 4.000000000000014211, 0.000000000000000000 ) ) ;
#83288=DIRECTION ( 'NONE',  ( -1.000000000000000000, -1.224606353822377258E-16, -0.000000000000000000 ) ) ;
#83291=ORIENTED_EDGE ( 'NONE', *, *, #67531, .F. ) ;
#83292=FACE_OUTER_BOUND ( 'NONE', #73822, .T. ) ;
#83343=EDGE_CURVE ( 'NONE', #35284, #98286, #12542, .T. ) ;
#83366=CARTESIAN_POINT ( 'NONE',  ( 53.29999999999999716, 6.915964383211875250E-15, 0.000000000000000000 ) ) ;
#83426=CARTESIAN_POINT ( 'NONE',  ( 0.000000000000000000, 0.000000000000000000, 4.000000000000000000 ) ) ;
#83450=CARTESIAN_POINT ( 'NONE',  ( 63.56127108291158123, 4.000000000000014211, 0.000000000000000000 ) ) ;
#83453=DIRECTION ( 'NONE',  ( -1.000000000000000000, -1.224606353822377258E-16, -0.000000000000000000 ) ) ;
#83458=ORIENTED_EDGE ( 'NONE', *, *, #82849, .F. ) ;
#83467=CARTESIAN_POINT ( 'NONE',  ( 58.18888888888888999, 3.309500000000014541, 4.052968581778174646E-16 ) ) ;
#83479=ORIENTED_EDGE ( 'NONE', *, *, #3266, .T. ) ;
#83508=AXIS2_PLACEMENT_3D ( 'NONE', #10830, #43751, #76643 ) ;
#83603=CARTESIAN_POINT ( 'NONE',  ( 52.81650669486619165, 4.898587196589294500E-16, -4.000000000000007105 ) ) ;
#83631=DIRECTION ( 'NONE',  ( 0.000000000000000000, -1.000000000000000000, 0.000000000000000000 ) ) ;
#83726=VERTEX_POINT ( 'NONE', #101654 ) ;
#83728=LINE ( 'NONE', #1745, #11851 ) ;
#83751=VECTOR ( 'NONE', #103631, 1000.000000000000000 ) ;
#83760=DIRECTION ( 'NONE',  ( 1.000000000000000000, 1.224606353822377258E-16, 0.000000000000000000 ) ) ;
#83799=ADVANCED_FACE ( 'NONE', ( #76834 ), #20255, .T. ) ;
#83815=EDGE_CURVE ( 'NONE', #93278, #77883, #27813, .T. ) ;
#83817=CARTESIAN_POINT ( 'NONE',  ( 57.70539558375507738, 6.856755485862130937E-15, 0.000000000000000000 ) ) ;
#83838=VECTOR ( 'NONE', #104564, 1000.000000000000227 ) ;
#83860=AXIS2_PLACEMENT_3D ( 'NONE', #25049, #26138, #74091 ) ;
#83881=CARTESIAN_POINT ( 'NONE',  ( 60.14984002819952025, 4.000000000000015099, 4.898587196589422689E-16 ) ) ;
#83934=CARTESIAN_POINT ( 'NONE',  ( 0.000000000000000000, 4.898587196589412829E-16, -4.000000000000000000 ) ) ;
#83973=VECTOR ( 'NONE', #103097, 1000.000000000000000 ) ;
#83975=DIRECTION ( 'NONE',  ( 0.000000000000000000, -1.000000000000000000, 0.000000000000000000 ) ) ;
#83986=AXIS2_PLACEMENT_3D ( 'NONE', #63096, #6963, #64170 ) ;
#83992=DIRECTION ( 'NONE',  ( -0.5735764363510494901, -0.8191520442889894671, 0.000000000000000000 ) ) ;
#84016=CARTESIAN_POINT ( 'NONE',  ( 4.449746416242592429E-16, -5.788408252967910173, -2.974182810908588603 ) ) ;
#84024=DIRECTION ( 'NONE',  ( 0.000000000000000000, -1.000000000000000000, 0.000000000000000000 ) ) ;
#84048=LINE ( 'NONE', #10671, #45670 ) ;
#84100=AXIS2_PLACEMENT_3D ( 'NONE', #60890, #100264, #59292 ) ;
#84134=AXIS2_PLACEMENT_3D ( 'NONE', #56854, #64447, #97320 ) ;
#84147=EDGE_LOOP ( 'NONE', ( #103808, #27635, #39162, #23449, #77490, #106592 ) ) ;
#84159=EDGE_CURVE ( 'NONE', #103417, #43619, #15170, .T. ) ;
#84163=DIRECTION ( 'NONE',  ( 0.000000000000000000, -1.000000000000000000, 0.000000000000000000 ) ) ;
#84247=CARTESIAN_POINT ( 'NONE',  ( 65.52222222222222570, 6.915964383211875250E-15, 0.000000000000000000 ) ) ;
#84248=CONICAL_SURFACE ( 'NONE', #92860, 3.309499999999999886, 0.7853981633974710386 ) ;
#84249=CYLINDRICAL_SURFACE ( 'NONE', #99421, 4.000000000000000000 ) ;
#84250=EDGE_LOOP ( 'NONE', ( #43063, #28335, #87773, #72546, #61728 ) ) ;
#84275=ORIENTED_EDGE ( 'NONE', *, *, #100836, .F. ) ;
#84286=EDGE_CURVE ( 'NONE', #93427, #71455, #17807, .T. ) ;
#84299=EDGE_CURVE ( 'NONE', #84731, #4022, #103935, .T. ) ;
#84326=ORIENTED_EDGE ( 'NONE', *, *, #92223, .F. ) ;
#84358=LINE ( 'NONE', #77327, #33223 ) ;
#84378=CIRCLE ( 'NONE', #37897, 4.000000000000007105 ) ;
#84395=VERTEX_POINT ( 'NONE', #78193 ) ;
#84397=VECTOR ( 'NONE', #59611, 1000.000000000000000 ) ;
#84404=CARTESIAN_POINT ( 'NONE',  ( 68.70539558375507738, -1.232595164407830946E-29, 4.000000000000007105 ) ) ;
#84447=DIRECTION ( 'NONE',  ( 1.000000000000000000, 1.224606353822377258E-16, 0.000000000000000000 ) ) ;
#84567=EDGE_CURVE ( 'NONE', #93427, #19599, #4307, .T. ) ;
#84569=CONICAL_SURFACE ( 'NONE', #77635, 3.309500000000007880, 0.9599310885968770357 ) ;
#84592=CARTESIAN_POINT ( 'NONE',  ( 0.000000000000000000, 0.000000000000000000, 0.000000000000000000 ) ) ;
#84603=AXIS2_PLACEMENT_3D ( 'NONE', #9530, #17655, #74797 ) ;
#84604=ORIENTED_EDGE ( 'NONE', *, *, #40202, .T. ) ;
#84610=EDGE_LOOP ( 'NONE', ( #98394, #60703, #24283, #51161, #65056, #105 ) ) ;
#84625=VERTEX_POINT ( 'NONE', #38809 ) ;
#84637=LINE ( 'NONE', #35051, #95691 ) ;
#84689=EDGE_CURVE ( 'NONE', #106204, #99028, #12704, .T. ) ;
#84728=DIRECTION ( 'NONE',  ( 0.000000000000000000, -1.000000000000000000, 0.000000000000000000 ) ) ;
#84731=VERTEX_POINT ( 'NONE', #413 ) ;
#84785=PLANE ( 'NONE',  #28269 ) ;
#84788=CARTESIAN_POINT ( 'NONE',  ( 65.03872891708842019, 4.898587196589294500E-16, -4.000000000000007105 ) ) ;
#84789=EDGE_CURVE ( 'NONE', #105857, #37936, #10912, .T. ) ;
#84826=DIRECTION ( 'NONE',  ( 0.000000000000000000, -1.000000000000000000, 0.000000000000000000 ) ) ;
#84827=CARTESIAN_POINT ( 'NONE',  ( 62.33904886068935980, -4.000000000000000000, 4.898587196589421703E-16 ) ) ;
#84850=ORIENTED_EDGE ( 'NONE', *, *, #83815, .F. ) ;
#84881=DIRECTION ( 'NONE',  ( 0.000000000000000000, 1.000000000000000000, 0.000000000000000000 ) ) ;
#84884=CARTESIAN_POINT ( 'NONE',  ( 4.699999999999999289, -3.752776749732553707, 6.499999999999998224 ) ) ;
#84900=VERTEX_POINT ( 'NONE', #68399 ) ;
#84906=CIRCLE ( 'NONE', #90046, 4.000000000000007105 ) ;
#84908=DIRECTION ( 'NONE',  ( -1.000000000000000000, -1.224606353822377258E-16, -0.000000000000000000 ) ) ;
#84967=ORIENTED_EDGE ( 'NONE', *, *, #29080, .T. ) ;
#84990=CARTESIAN_POINT ( 'NONE',  ( 55.74444444444444713, -3.309500000000000774, 4.475777889183797681E-16 ) ) ;
#85026=EDGE_CURVE ( 'NONE', #40074, #28791, #15448, .T. ) ;
#85041=ORIENTED_EDGE ( 'NONE', *, *, #19266, .T. ) ;
#85056=ORIENTED_EDGE ( 'NONE', *, *, #19724, .T. ) ;
#85060=DIRECTION ( 'NONE',  ( 1.000000000000000000, 0.000000000000000000, -0.000000000000000000 ) ) ;
#85096=CARTESIAN_POINT ( 'NONE',  ( 0.000000000000000000, 0.000000000000000000, 4.000000000000000000 ) ) ;
#85104=CARTESIAN_POINT ( 'NONE',  ( 56.48317336153285595, 6.856755485862130937E-15, 0.000000000000000000 ) ) ;
#85181=ORIENTED_EDGE ( 'NONE', *, *, #94297, .F. ) ;
#85188=CARTESIAN_POINT ( 'NONE',  ( 0.5805565836007648972, -7.505553499465138501, -1.190388518514737689E-16 ) ) ;
#85194=CIRCLE ( 'NONE', #57601, 4.000000000000007105 ) ;
#85220=CARTESIAN_POINT ( 'NONE',  ( 53.29999999999999716, 6.915964383211875250E-15, 0.000000000000000000 ) ) ;
#85261=ORIENTED_EDGE ( 'NONE', *, *, #25660, .F. ) ;
#85318=CONICAL_SURFACE ( 'NONE', #49096, 3.309500000000007880, 0.9599310885968770357 ) ;
#85340=ORIENTED_EDGE ( 'NONE', *, *, #105016, .T. ) ;
#85350=ORIENTED_EDGE ( 'NONE', *, *, #94422, .F. ) ;
#85366=EDGE_CURVE ( 'NONE', #7404, #57904, #100628, .T. ) ;
#85388=AXIS2_PLACEMENT_3D ( 'NONE', #87250, #27985, #85660 ) ;
#85402=DIRECTION ( 'NONE',  ( -1.000000000000000000, -1.224606353822377258E-16, -0.000000000000000000 ) ) ;
#85417=CARTESIAN_POINT ( 'NONE',  ( 0.000000000000000000, 4.898587196589412829E-16, -4.000000000000000000 ) ) ;
#85433=EDGE_LOOP ( 'NONE', ( #41003, #32862, #89878 ) ) ;
#85434=DIRECTION ( 'NONE',  ( 0.000000000000000000, -1.000000000000000000, 0.000000000000000000 ) ) ;
#85447=DIRECTION ( 'NONE',  ( 1.000000000000000000, 1.224606353822377258E-16, 0.000000000000000000 ) ) ;
#85457=EDGE_CURVE ( 'NONE', #83726, #68935, #21523, .T. ) ;
#85509=VERTEX_POINT ( 'NONE', #64325 ) ;
#85557=AXIS2_PLACEMENT_3D ( 'NONE', #55940, #23104, #64609 ) ;
#85569=DIRECTION ( 'NONE',  ( 0.000000000000000000, -1.000000000000000000, 0.000000000000000000 ) ) ;
#85575=ORIENTED_EDGE ( 'NONE', *, *, #11698, .T. ) ;
#85604=CARTESIAN_POINT ( 'NONE',  ( 0.2595206531158521512, 2.531175536751809396, 6.499999999999995559 ) ) ;
#85608=LINE ( 'NONE', #86678, #17531 ) ;
#85623=DIRECTION ( 'NONE',  ( 0.000000000000000000, 0.000000000000000000, 1.000000000000000000 ) ) ;
#85657=AXIS2_PLACEMENT_3D ( 'NONE', #30664, #64086, #23098 ) ;
#85658=ORIENTED_EDGE ( 'NONE', *, *, #28865, .F. ) ;
#85660=DIRECTION ( 'NONE',  ( 0.000000000000000000, 1.000000000000000000, 0.000000000000000000 ) ) ;
#85681=ORIENTED_EDGE ( 'NONE', *, *, #92646, .F. ) ;
#85691=ORIENTED_EDGE ( 'NONE', *, *, #35361, .F. ) ;
#85759=CARTESIAN_POINT ( 'NONE',  ( 67.22793774957824553, -4.000000000000000000, 4.898587196589421703E-16 ) ) ;
#85776=EDGE_CURVE ( 'NONE', #106205, #82529, #65716, .T. ) ;
#85777=ADVANCED_FACE ( 'NONE', ( #50565 ), #90389, .T. ) ;
#85781=ORIENTED_EDGE ( 'NONE', *, *, #46140, .T. ) ;
#85832=AXIS2_PLACEMENT_3D ( 'NONE', #72852, #30314, #6004 ) ;
#85890=DIRECTION ( 'NONE',  ( 0.5735764363510442720, -0.8191520442889930198, 1.003171929053526349E-16 ) ) ;
#85895=VERTEX_POINT ( 'NONE', #4863 ) ;
#85911=DIRECTION ( 'NONE',  ( 0.000000000000000000, -1.000000000000000000, 0.000000000000000000 ) ) ;
#85918=EDGE_CURVE ( 'NONE', #53703, #54493, #104162, .T. ) ;
#85950=CARTESIAN_POINT ( 'NONE',  ( 69.92761780597730592, 6.856755485862130937E-15, 0.000000000000000000 ) ) ;
#85954=CARTESIAN_POINT ( 'NONE',  ( 55.26095113931063452, 4.898587196589294500E-16, -4.000000000000007105 ) ) ;
#85972=DIRECTION ( 'NONE',  ( 0.000000000000000000, -1.000000000000000000, 0.000000000000000000 ) ) ;
#86023=DIRECTION ( 'NONE',  ( -1.000000000000000000, -1.224606353822377258E-16, -0.000000000000000000 ) ) ;
#86025=DIRECTION ( 'NONE',  ( 0.000000000000000000, 0.000000000000000000, 1.000000000000000000 ) ) ;
#86099=VECTOR ( 'NONE', #95002, 1000.000000000000000 ) ;
#86156=B_SPLINE_CURVE_WITH_KNOTS ( 'NONE', 3,
 ( #96361, #71522, #7843, #106004, #79618, #55844, #105492, #6791 ),
 .UNSPECIFIED., .F., .F.,
 ( 4, 2, 2, 4 ),
 ( 0.003797433802554458452, 0.004743183970586253503, 0.005688934138618048121, 0.007580434474681637357 ),
 .UNSPECIFIED. ) ;
#86165=CIRCLE ( 'NONE', #46564, 3.309500000000007880 ) ;
#86185=CARTESIAN_POINT ( 'NONE',  ( 67.22793774957824553, 4.898587196589294500E-16, -4.000000000000007105 ) ) ;
#86186=ADVANCED_FACE ( 'NONE', ( #47441 ), #85318, .T. ) ;
#86208=AXIS2_PLACEMENT_3D ( 'NONE', #64639, #15544, #65163 ) ;
#86215=FACE_OUTER_BOUND ( 'NONE', #93454, .T. ) ;
#86226=ORIENTED_EDGE ( 'NONE', *, *, #99492, .F. ) ;
#86233=CARTESIAN_POINT ( 'NONE',  ( 70.89460441624491693, 6.975173280561618775E-15, 0.000000000000000000 ) ) ;
#86236=ORIENTED_EDGE ( 'NONE', *, *, #74077, .F. ) ;
#86254=ORIENTED_EDGE ( 'NONE', *, *, #106466, .F. ) ;
#86293=LINE ( 'NONE', #30171, #83838 ) ;
#86309=VERTEX_POINT ( 'NONE', #57649 ) ;
#86310=CIRCLE ( 'NONE', #22577, 6.499999999999999112 ) ;
#86318=DIRECTION ( 'NONE',  ( -1.000000000000000000, -1.224606353822377258E-16, -0.000000000000000000 ) ) ;
#86325=ORIENTED_EDGE ( 'NONE', *, *, #23958, .T. ) ;
#86388=ORIENTED_EDGE ( 'NONE', *, *, #83815, .T. ) ;
#86395=AXIS2_PLACEMENT_3D ( 'NONE', #37941, #14135, #13607 ) ;
#86407=ORIENTED_EDGE ( 'NONE', *, *, #98895, .T. ) ;
#86440=EDGE_CURVE ( 'NONE', #52615, #102808, #4314, .T. ) ;
#86449=CARTESIAN_POINT ( 'NONE',  ( 53.78349330513380266, 6.975173280561618775E-15, 0.000000000000000000 ) ) ;
#86451=FACE_OUTER_BOUND ( 'NONE', #75314, .T. ) ;
#86505=DIRECTION ( 'NONE',  ( -1.000000000000000000, -0.000000000000000000, -0.000000000000000000 ) ) ;
#86550=AXIS2_PLACEMENT_3D ( 'NONE', #86449, #21712, #85911 ) ;
#86586=DIRECTION ( 'NONE',  ( 1.000000000000000000, 0.000000000000000000, -0.000000000000000000 ) ) ;
#86588=PLANE ( 'NONE',  #794 ) ;
#86590=CARTESIAN_POINT ( 'NONE',  ( 0.000000000000000000, 0.000000000000000000, 0.000000000000000000 ) ) ;
#86616=EDGE_CURVE ( 'NONE', #84900, #1105, #59536, .T. ) ;
#86621=ORIENTED_EDGE ( 'NONE', *, *, #92736, .F. ) ;
#86641=DIRECTION ( 'NONE',  ( -1.000000000000000000, -1.224606353822377258E-16, -0.000000000000000000 ) ) ;
#86646=EDGE_LOOP ( 'NONE', ( #75472, #11453, #31831, #12126, #17529 ) ) ;
#86649=DIRECTION ( 'NONE',  ( 0.000000000000000000, 0.000000000000000000, -1.000000000000000000 ) ) ;
#86653=DIRECTION ( 'NONE',  ( -1.000000000000000000, -1.224606353822377258E-16, -0.000000000000000000 ) ) ;
#86678=CARTESIAN_POINT ( 'NONE',  ( 74.07777777777778283, 3.309500000000014541, 4.052968581778174646E-16 ) ) ;
#86721=EDGE_LOOP ( 'NONE', ( #76020, #105514, #74796, #87733, #106455 ) ) ;
#86774=CARTESIAN_POINT ( 'NONE',  ( 0.2565376335216161818, -2.516992571280038504, -6.500000000000001776 ) ) ;
#86814=EDGE_CURVE ( 'NONE', #103201, #26677, #86866, .T. ) ;
#86834=CARTESIAN_POINT ( 'NONE',  ( 66.00571552735603120, 4.000000000000013323, 0.000000000000000000 ) ) ;
#86835=DIRECTION ( 'NONE',  ( -1.000000000000000000, -0.000000000000000000, -0.000000000000000000 ) ) ;
#86842=FACE_OUTER_BOUND ( 'NONE', #36544, .T. ) ;
#86866=CIRCLE ( 'NONE', #102564, 4.000000000000007105 ) ;
#86895=LINE ( 'NONE', #53456, #75046 ) ;
#86919=ADVANCED_FACE ( 'NONE', ( #19303 ), #74969, .T. ) ;
#86926=DIRECTION ( 'NONE',  ( 0.000000000000000000, -1.000000000000000000, 0.000000000000000000 ) ) ;
#86936=ORIENTED_EDGE ( 'NONE', *, *, #18926, .F. ) ;
#86937=AXIS2_PLACEMENT_3D ( 'NONE', #94318, #20480, #70028 ) ;
#86952=ORIENTED_EDGE ( 'NONE', *, *, #31867, .T. ) ;
#86973=VERTEX_POINT ( 'NONE', #68331 ) ;
#87006=CARTESIAN_POINT ( 'NONE',  ( 0.000000000000000000, 4.898587196589412829E-16, -4.000000000000000000 ) ) ;
#87028=AXIS2_PLACEMENT_3D ( 'NONE', #48201, #39082, #13712 ) ;
#87031=ORIENTED_EDGE ( 'NONE', *, *, #103584, .F. ) ;
#87101=CONICAL_SURFACE ( 'NONE', #49189, 4.000000000000007105, 0.9599310885968835860 ) ;
#87133=DIRECTION ( 'NONE',  ( -1.000000000000000000, -1.224606353822377258E-16, -0.000000000000000000 ) ) ;
#87153=VECTOR ( 'NONE', #56956, 1000.000000000000000 ) ;
#87158=DIRECTION ( 'NONE',  ( 0.000000000000000000, 0.000000000000000000, -1.000000000000000000 ) ) ;
#87160=EDGE_LOOP ( 'NONE', ( #22133, #27037, #11526, #80565, #21013 ) ) ;
#87164=DIRECTION ( 'NONE',  ( 1.000000000000000000, 0.000000000000000000, -0.000000000000000000 ) ) ;
#87189=CARTESIAN_POINT ( 'NONE',  ( 0.000000000000000000, 1.502314598737161398E-15, 6.499999999999999112 ) ) ;
#87206=CIRCLE ( 'NONE', #20105, 3.309500000000007880 ) ;
#87229=CONICAL_SURFACE ( 'NONE', #56395, 6.499999999999999112, 1.047197551196600296 ) ;
#87246=EDGE_CURVE ( 'NONE', #51147, #55118, #104080, .T. ) ;
#87250=CARTESIAN_POINT ( 'NONE',  ( 61.11682663846713837, 6.975173280561618775E-15, 0.000000000000000000 ) ) ;
#87287=CARTESIAN_POINT ( 'NONE',  ( 64.29999999999999716, -3.309500000000000774, 0.000000000000000000 ) ) ;
#87299=DIRECTION ( 'NONE',  ( -1.000000000000000000, -1.224606353822377258E-16, -0.000000000000000000 ) ) ;
#87303=DIRECTION ( 'NONE',  ( -1.000000000000000000, -1.224606353822377258E-16, -0.000000000000000000 ) ) ;
#87358=CARTESIAN_POINT ( 'NONE',  ( 73.59428447264397732, 4.898587196589294500E-16, -4.000000000000007105 ) ) ;
#87411=EDGE_CURVE ( 'NONE', #36600, #47158, #68056, .T. ) ;
#87414=EDGE_LOOP ( 'NONE', ( #49143, #46830, #69264, #59384, #24974, #7416 ) ) ;
#87421=CIRCLE ( 'NONE', #54655, 4.000000000000007105 ) ;
#87496=CARTESIAN_POINT ( 'NONE',  ( 4.699999999999999289, 0.000000000000000000, 0.000000000000000000 ) ) ;
#87497=ORIENTED_EDGE ( 'NONE', *, *, #32524, .T. ) ;
#87507=EDGE_CURVE ( 'NONE', #101359, #20792, #9735, .T. ) ;
#87562=ORIENTED_EDGE ( 'NONE', *, *, #69975, .T. ) ;
#87572=AXIS2_PLACEMENT_3D ( 'NONE', #38223, #53838, #55415 ) ;
#87586=VECTOR ( 'NONE', #89062, 1000.000000000000000 ) ;
#87589=AXIS2_PLACEMENT_3D ( 'NONE', #77989, #28410, #85569 ) ;
#87625=VERTEX_POINT ( 'NONE', #76719 ) ;
#87642=AXIS2_PLACEMENT_3D ( 'NONE', #54138, #33100, #48176 ) ;
#87688=ORIENTED_EDGE ( 'NONE', *, *, #3704, .F. ) ;
#87733=ORIENTED_EDGE ( 'NONE', *, *, #9395, .F. ) ;
#87773=ORIENTED_EDGE ( 'NONE', *, *, #33990, .T. ) ;
#87774=VERTEX_POINT ( 'NONE', #71815 ) ;
#87781=AXIS2_PLACEMENT_3D ( 'NONE', #82845, #820, #66666 ) ;
#87791=ADVANCED_FACE ( 'NONE', ( #86451 ), #4976, .F. ) ;
#87803=ORIENTED_EDGE ( 'NONE', *, *, #29467, .T. ) ;
#87809=AXIS2_PLACEMENT_3D ( 'NONE', #29081, #36624, #11757 ) ;
#87882=VERTEX_POINT ( 'NONE', #95983 ) ;
#87897=ORIENTED_EDGE ( 'NONE', *, *, #60293, .F. ) ;
#87970=LINE ( 'NONE', #38887, #54070 ) ;
#87975=ORIENTED_EDGE ( 'NONE', *, *, #105179, .T. ) ;
#88003=DIRECTION ( 'NONE',  ( -1.000000000000000000, -1.224606353822377258E-16, -0.000000000000000000 ) ) ;
#88027=EDGE_CURVE ( 'NONE', #94772, #84900, #49535, .T. ) ;
#88034=CARTESIAN_POINT ( 'NONE',  ( 67.48317336153286305, 6.856755485862130937E-15, 0.000000000000000000 ) ) ;
#88118=EDGE_CURVE ( 'NONE', #92331, #68935, #15577, .T. ) ;
#88159=CARTESIAN_POINT ( 'NONE',  ( 67.48317336153286305, 4.000000000000015099, 4.898587196589422689E-16 ) ) ;
#88161=EDGE_LOOP ( 'NONE', ( #93882, #66007, #36509, #49078, #14498, #47084 ) ) ;
#88176=ORIENTED_EDGE ( 'NONE', *, *, #17416, .F. ) ;
#88191=DIRECTION ( 'NONE',  ( -1.000000000000000000, -1.224606353822377258E-16, -0.000000000000000000 ) ) ;
#88212=EDGE_CURVE ( 'NONE', #62199, #106204, #13056, .T. ) ;
#88237=EDGE_LOOP ( 'NONE', ( #64260, #102132, #49949, #1242, #31261, #63407 ) ) ;
#88248=LINE ( 'NONE', #30029, #18631 ) ;
#88320=ADVANCED_FACE ( 'NONE', ( #12790 ), #76824, .T. ) ;
#88332=ORIENTED_EDGE ( 'NONE', *, *, #96676, .F. ) ;
#88336=DIRECTION ( 'NONE',  ( 0.000000000000000000, -1.000000000000000000, 0.000000000000000000 ) ) ;
#88361=DIRECTION ( 'NONE',  ( 0.000000000000000000, -1.000000000000000000, 0.000000000000000000 ) ) ;
#88383=EDGE_CURVE ( 'NONE', #41303, #22977, #78529, .T. ) ;
#88413=CIRCLE ( 'NONE', #103880, 4.400000000000000355 ) ;
#88422=DIRECTION ( 'NONE',  ( -0.5735764363510494901, -0.8191520442889894671, 0.000000000000000000 ) ) ;
#88433=ORIENTED_EDGE ( 'NONE', *, *, #28634, .F. ) ;
#88436=CARTESIAN_POINT ( 'NONE',  ( 0.000000000000000000, 4.898587196589412829E-16, -4.000000000000000000 ) ) ;
#88441=DIRECTION ( 'NONE',  ( 0.000000000000000000, 1.000000000000000000, 0.000000000000000000 ) ) ;
#88452=DIRECTION ( 'NONE',  ( 0.000000000000000000, -0.5000000000000016653, -0.8660254037844375974 ) ) ;
#88559=DIRECTION ( 'NONE',  ( -1.000000000000000000, -1.224606353822377258E-16, -0.000000000000000000 ) ) ;
#88638=CARTESIAN_POINT ( 'NONE',  ( 73.33904886068935980, 6.975173280561618775E-15, 0.000000000000000000 ) ) ;
#88652=DIRECTION ( 'NONE',  ( 0.000000000000000000, -1.000000000000000000, 0.000000000000000000 ) ) ;
#88676=ORIENTED_EDGE ( 'NONE', *, *, #55462, .T. ) ;
#88748=CARTESIAN_POINT ( 'NONE',  ( 72.85555555555556850, 3.309500000000014541, 4.052968581778174646E-16 ) ) ;
#88753=CARTESIAN_POINT ( 'NONE',  ( 66.74444444444444002, 3.309500000000014541, 4.052968581778174646E-16 ) ) ;
#88790=DIRECTION ( 'NONE',  ( -1.000000000000000000, -0.000000000000000000, -0.000000000000000000 ) ) ;
#88830=CIRCLE ( 'NONE', #59506, 3.309500000000007880 ) ;
#88862=CONICAL_SURFACE ( 'NONE', #56103, 3.309500000000007880, 0.9599310885968770357 ) ;
#88867=EDGE_CURVE ( 'NONE', #75420, #105857, #13139, .T. ) ;
#88906=CARTESIAN_POINT ( 'NONE',  ( 55.00571552735602410, 6.975173280561618775E-15, 0.000000000000000000 ) ) ;
#88941=ORIENTED_EDGE ( 'NONE', *, *, #94898, .T. ) ;
#88946=CARTESIAN_POINT ( 'NONE',  ( 60.14984002819952025, 6.856755485862130937E-15, 0.000000000000000000 ) ) ;
#88982=DIRECTION ( 'NONE',  ( -1.000000000000000000, -1.224606353822377258E-16, -0.000000000000000000 ) ) ;
#89043=EDGE_CURVE ( 'NONE', #87774, #58295, #30810, .T. ) ;
#89062=DIRECTION ( 'NONE',  ( 0.5735764363510440500, 0.8191520442889932418, 0.000000000000000000 ) ) ;
#89075=CONICAL_SURFACE ( 'NONE', #42567, 4.000000000000007105, 0.9599310885968835860 ) ;
#89099=EDGE_LOOP ( 'NONE', ( #50958, #61293, #81886, #3232, #29566 ) ) ;
#89166=VECTOR ( 'NONE', #29427, 1000.000000000000227 ) ;
#89206=CARTESIAN_POINT ( 'NONE',  ( 58.67238219402268840, 6.975173280561618775E-15, 0.000000000000000000 ) ) ;
#89232=DIRECTION ( 'NONE',  ( -1.000000000000000000, -1.224606353822377258E-16, -0.000000000000000000 ) ) ;
#89236=DIRECTION ( 'NONE',  ( 0.000000000000000000, -1.000000000000000000, 0.000000000000000000 ) ) ;
#89258=DIRECTION ( 'NONE',  ( -1.000000000000000000, -0.000000000000000000, -0.000000000000000000 ) ) ;
#89260=FACE_OUTER_BOUND ( 'NONE', #75286, .T. ) ;
#89288=ORIENTED_EDGE ( 'NONE', *, *, #26452, .F. ) ;
#89304=LINE ( 'NONE', #80656, #79788 ) ;
#89367=DIRECTION ( 'NONE',  ( 0.000000000000000000, -1.000000000000000000, 0.000000000000000000 ) ) ;
#89372=ADVANCED_FACE ( 'NONE', ( #60909 ), #10073, .T. ) ;
#89425=CARTESIAN_POINT ( 'NONE',  ( 65.03872891708842019, -4.000000000000000000, 0.000000000000000000 ) ) ;
#89471=ORIENTED_EDGE ( 'NONE', *, *, #63735, .T. ) ;
#89479=CARTESIAN_POINT ( 'NONE',  ( 4.699999999999999289, 6.499999999999999112, 0.000000000000000000 ) ) ;
#89488=EDGE_LOOP ( 'NONE', ( #98536, #52174, #106319, #43449, #60974, #46724 ) ) ;
#89505=DIRECTION ( 'NONE',  ( -1.000000000000000000, -0.000000000000000000, -0.000000000000000000 ) ) ;
#89509=AXIS2_PLACEMENT_3D ( 'NONE', #19355, #27437, #43049 ) ;
#89531=EDGE_CURVE ( 'NONE', #93228, #87882, #58516, .T. ) ;
#89543=CARTESIAN_POINT ( 'NONE',  ( 61.85555555555556140, 6.915964383211875250E-15, 0.000000000000000000 ) ) ;
#89559=ORIENTED_EDGE ( 'NONE', *, *, #93477, .T. ) ;
#89561=CARTESIAN_POINT ( 'NONE',  ( 67.22793774957824553, 6.975173280561618775E-15, 0.000000000000000000 ) ) ;
#89574=FILL_AREA_STYLE_COLOUR ( '', #102293 ) ;
#89595=CARTESIAN_POINT ( 'NONE',  ( 73.59428447264397732, -4.000000000000000000, 0.000000000000000000 ) ) ;
#89691=EDGE_LOOP ( 'NONE', ( #40297, #77166, #77590 ) ) ;
#89703=ORIENTED_EDGE ( 'NONE', *, *, #61379, .F. ) ;
#89729=ORIENTED_EDGE ( 'NONE', *, *, #90120, .T. ) ;
#89782=ORIENTED_EDGE ( 'NONE', *, *, #23958, .F. ) ;
#89793=EDGE_LOOP ( 'NONE', ( #88176, #30897, #96423, #64143, #26200, #81369 ) ) ;
#89878=ORIENTED_EDGE ( 'NONE', *, *, #73688, .T. ) ;
#89899=PRODUCT_DEFINITION_CONTEXT ( 'detailed design', #63831, 'design' ) ;
#89907=DIRECTION ( 'NONE',  ( -1.000000000000000000, -0.000000000000000000, -0.000000000000000000 ) ) ;
#89956=EDGE_CURVE ( 'NONE', #102890, #99463, #91555, .T. ) ;
#89960=EDGE_CURVE ( 'NONE', #34382, #84395, #20529, .T. ) ;
#89984=DIRECTION ( 'NONE',  ( -1.000000000000000000, 0.000000000000000000, -0.000000000000000000 ) ) ;
#90037=VECTOR ( 'NONE', #63586, 1000.000000000000000 ) ;
#90046=AXIS2_PLACEMENT_3D ( 'NONE', #61849, #12728, #21924 ) ;
#90118=CIRCLE ( 'NONE', #41930, 4.000000000000007105 ) ;
#90120=EDGE_CURVE ( 'NONE', #2681, #6495, #8443, .T. ) ;
#90126=DIRECTION ( 'NONE',  ( -1.000000000000000000, -0.000000000000000000, -0.000000000000000000 ) ) ;
#90143=CARTESIAN_POINT ( 'NONE',  ( 57.45015997180046696, -4.000000000000000000, 4.898587196589421703E-16 ) ) ;
#90156=AXIS2_PLACEMENT_3D ( 'NONE', #37955, #91328, #78175 ) ;
#90240=AXIS2_PLACEMENT_3D ( 'NONE', #106162, #81355, #7466 ) ;
#90257=FACE_OUTER_BOUND ( 'NONE', #23346, .T. ) ;
#90288=CARTESIAN_POINT ( 'NONE',  ( 55.00571552735602410, 6.975173280561618775E-15, 0.000000000000000000 ) ) ;
#90306=EDGE_CURVE ( 'NONE', #86309, #45881, #10356, .T. ) ;
#90359=CARTESIAN_POINT ( 'NONE',  ( 0.000000000000000000, 5.629165124598848990, 3.250000000000002220 ) ) ;
#90389=CONICAL_SURFACE ( 'NONE', #43893, 3.309500000000007880, 0.9599310885968770357 ) ;
#90411=ORIENTED_EDGE ( 'NONE', *, *, #25850, .F. ) ;
#90442=CARTESIAN_POINT ( 'NONE',  ( 0.000000000000000000, 5.629165124598842773, -3.250000000000011990 ) ) ;
#90472=AXIS2_PLACEMENT_3D ( 'NONE', #50325, #65990, #91861 ) ;
#90481=EDGE_LOOP ( 'NONE', ( #85056, #42755, #92037 ) ) ;
#90513=ORIENTED_EDGE ( 'NONE', *, *, #99726, .F. ) ;
#90522=AXIS2_PLACEMENT_3D ( 'NONE', #89543, #99750, #99202 ) ;
#90532=DIRECTION ( 'NONE',  ( 1.000000000000000000, 0.000000000000000000, 0.000000000000000000 ) ) ;
#90619=AXIS2_PLACEMENT_3D ( 'NONE', #572, #99293, #8174 ) ;
#90634=DIRECTION ( 'NONE',  ( -1.000000000000000000, -1.224606353822377258E-16, -0.000000000000000000 ) ) ;
#90668=ORIENTED_EDGE ( 'NONE', *, *, #80996, .F. ) ;
#90679=CARTESIAN_POINT ( 'NONE',  ( 57.45015997180046696, 6.975173280561618775E-15, 0.000000000000000000 ) ) ;
#90686=EDGE_CURVE ( 'NONE', #66543, #20623, #84378, .T. ) ;
#90703=VECTOR ( 'NONE', #28198, 1000.000000000000000 ) ;
#90738=VERTEX_POINT ( 'NONE', #61334 ) ;
#90753=CONICAL_SURFACE ( 'NONE', #63194, 3.309499999999999886, 0.7853981633974710386 ) ;
#90782=ORIENTED_EDGE ( 'NONE', *, *, #77636, .T. ) ;
#90787=CARTESIAN_POINT ( 'NONE',  ( 0.000000000000000000, 0.000000000000000000, 4.000000000000000000 ) ) ;
#90844=VERTEX_POINT ( 'NONE', #31106 ) ;
#90862=CARTESIAN_POINT ( 'NONE',  ( 61.11682663846713837, -4.000000000000000000, 4.898587196589421703E-16 ) ) ;
#90890=CONICAL_SURFACE ( 'NONE', #104652, 3.309500000000007880, 0.9599310885968770357 ) ;
#90896=CONICAL_SURFACE ( 'NONE', #71866, 3.309500000000007880, 0.9599310885968770357 ) ;
#90958=EDGE_CURVE ( 'NONE', #39308, #47158, #50946, .T. ) ;
#90996=DIRECTION ( 'NONE',  ( 0.000000000000000000, -1.000000000000000000, 0.000000000000000000 ) ) ;
#91027=EDGE_CURVE ( 'NONE', #63428, #53314, #86165, .T. ) ;
#91041=CARTESIAN_POINT ( 'NONE',  ( 4.699999999999999289, -7.505553499465137612, 3.546421054897781431E-16 ) ) ;
#91046=ORIENTED_EDGE ( 'NONE', *, *, #52159, .T. ) ;
#91076=ORIENTED_EDGE ( 'NONE', *, *, #89043, .F. ) ;
#91100=CARTESIAN_POINT ( 'NONE',  ( 4.699999999999999289, 3.752776749732553263, -6.499999999999999112 ) ) ;
#91166=DIRECTION ( 'NONE',  ( -1.000000000000000000, -0.000000000000000000, -0.000000000000000000 ) ) ;
#91208=AXIS2_PLACEMENT_3D ( 'NONE', #14137, #3950, #45483 ) ;
#91217=EDGE_CURVE ( 'NONE', #50622, #20770, #103384, .T. ) ;
#91283=EDGE_CURVE ( 'NONE', #17325, #50186, #55081, .T. ) ;
#91286=DIRECTION ( 'NONE',  ( 0.000000000000000000, 1.000000000000000000, 0.000000000000000000 ) ) ;
#91295=CIRCLE ( 'NONE', #24180, 3.309500000000007880 ) ;
#91306=ORIENTED_EDGE ( 'NONE', *, *, #51329, .F. ) ;
#91317=CARTESIAN_POINT ( 'NONE',  ( 65.52222222222222570, 6.915964383211875250E-15, 0.000000000000000000 ) ) ;
#91325=CARTESIAN_POINT ( 'NONE',  ( 73.33904886068935980, 6.975173280561618775E-15, 0.000000000000000000 ) ) ;
#91328=DIRECTION ( 'NONE',  ( -1.000000000000000000, -0.000000000000000000, -0.000000000000000000 ) ) ;
#91333=CARTESIAN_POINT ( 'NONE',  ( 5.299999999999999822, 7.505553499465139389, 0.000000000000000000 ) ) ;
#91422=CARTESIAN_POINT ( 'NONE',  ( 67.48317336153286305, 4.898587196589294500E-16, -4.000000000000007105 ) ) ;
#91451=AXIS2_PLACEMENT_3D ( 'NONE', #10908, #59499, #2288 ) ;
#91491=CARTESIAN_POINT ( 'NONE',  ( 70.89460441624491693, 6.975173280561618775E-15, 0.000000000000000000 ) ) ;
#91552=ORIENTED_EDGE ( 'NONE', *, *, #58467, .T. ) ;
#91555=LINE ( 'NONE', #33866, #99678 ) ;
#91563=CARTESIAN_POINT ( 'NONE',  ( 56.48317336153285595, -4.000000000000000000, 0.000000000000000000 ) ) ;
#91595=DIRECTION ( 'NONE',  ( -1.000000000000000000, -0.000000000000000000, -0.000000000000000000 ) ) ;
#91618=ORIENTED_EDGE ( 'NONE', *, *, #5674, .F. ) ;
#91626=DIRECTION ( 'NONE',  ( -0.000000000000000000, 0.5000000000000018874, 0.8660254037844375974 ) ) ;
#91676=CARTESIAN_POINT ( 'NONE',  ( 65.52222222222222570, 6.915964383211875250E-15, 0.000000000000000000 ) ) ;
#91686=CIRCLE ( 'NONE', #86550, 4.000000000000007105 ) ;
#91711=ORIENTED_EDGE ( 'NONE', *, *, #67541, .F. ) ;
#91738=CARTESIAN_POINT ( 'NONE',  ( 54.52222222222221859, 3.309500000000014541, 0.000000000000000000 ) ) ;
#91745=DIRECTION ( 'NONE',  ( -1.000000000000000000, -1.224606353822377258E-16, -0.000000000000000000 ) ) ;
#91765=VERTEX_POINT ( 'NONE', #80943 ) ;
#91842=ORIENTED_EDGE ( 'NONE', *, *, #84567, .F. ) ;
#91846=CARTESIAN_POINT ( 'NONE',  ( 70.41111111111112564, -3.309500000000000774, 0.000000000000000000 ) ) ;
#91853=DIRECTION ( 'NONE',  ( 1.000000000000000000, 1.224606353822377258E-16, 0.000000000000000000 ) ) ;
#91861=DIRECTION ( 'NONE',  ( 0.000000000000000000, -1.000000000000000000, 0.000000000000000000 ) ) ;
#91922=EDGE_LOOP ( 'NONE', ( #19236, #56540, #62115, #10891, #69510 ) ) ;
#91925=CARTESIAN_POINT ( 'NONE',  ( 57.45015997180046696, 6.975173280561618775E-15, 0.000000000000000000 ) ) ;
#91967=MECHANICAL_DESIGN_GEOMETRIC_PRESENTATION_REPRESENTATION('',(#50592),#4139);
#92037=ORIENTED_EDGE ( 'NONE', *, *, #85918, .T. ) ;
#92108=DIRECTION ( 'NONE',  ( -1.000000000000000000, -1.224606353822377258E-16, -0.000000000000000000 ) ) ;
#92122=CARTESIAN_POINT ( 'NONE',  ( 68.70539558375507738, 6.856755485862130937E-15, 0.000000000000000000 ) ) ;
#92129=DIRECTION ( 'NONE',  ( -1.000000000000000000, -0.000000000000000000, -0.000000000000000000 ) ) ;
#92154=DIRECTION ( 'NONE',  ( 0.000000000000000000, -1.000000000000000000, 0.000000000000000000 ) ) ;
#92178=CARTESIAN_POINT ( 'NONE',  ( 70.41111111111112564, -3.309500000000000774, 4.475777889183797681E-16 ) ) ;
#92191=CARTESIAN_POINT ( 'NONE',  ( 65.03872891708842019, 6.856755485862130937E-15, 0.000000000000000000 ) ) ;
#92223=EDGE_CURVE ( 'NONE', #2515, #86973, #3228, .T. ) ;
#92244=DIRECTION ( 'NONE',  ( -1.000000000000000000, -1.224606353822377258E-16, -0.000000000000000000 ) ) ;
#92247=ORIENTED_EDGE ( 'NONE', *, *, #91283, .F. ) ;
#92270=ORIENTED_EDGE ( 'NONE', *, *, #74158, .T. ) ;
#92331=VERTEX_POINT ( 'NONE', #84990 ) ;
#92412=DIRECTION ( 'NONE',  ( -1.000000000000000000, -1.224606353822377258E-16, -0.000000000000000000 ) ) ;
#92446=CARTESIAN_POINT ( 'NONE',  ( 66.74444444444444002, 6.915964383211875250E-15, 0.000000000000000000 ) ) ;
#92453=DIRECTION ( 'NONE',  ( -0.000000000000000000, 1.000000000000000000, -1.224646799147353207E-16 ) ) ;
#92522=CARTESIAN_POINT ( 'NONE',  ( 0.000000000000000000, 0.000000000000000000, 0.000000000000000000 ) ) ;
#92542=AXIS2_PLACEMENT_3D ( 'NONE', #61404, #79155, #70549 ) ;
#92567=EDGE_LOOP ( 'NONE', ( #14087, #25490, #11728, #92247, #13617, #103294 ) ) ;
#92591=DIRECTION ( 'NONE',  ( 0.000000000000000000, 1.000000000000000000, 0.000000000000000000 ) ) ;
#92595=ORIENTED_EDGE ( 'NONE', *, *, #21344, .T. ) ;
#92610=LINE ( 'NONE', #91041, #63964 ) ;
#92634=CARTESIAN_POINT ( 'NONE',  ( 72.11682663846713126, 4.000000000000013323, 0.000000000000000000 ) ) ;
#92646=EDGE_CURVE ( 'NONE', #11977, #103417, #86310, .T. ) ;
#92688=VECTOR ( 'NONE', #59055, 1000.000000000000000 ) ;
#92699=ORIENTED_EDGE ( 'NONE', *, *, #19266, .F. ) ;
#92736=EDGE_CURVE ( 'NONE', #47738, #105869, #3615, .T. ) ;
#92772=CIRCLE ( 'NONE', #63545, 4.000000000000007105 ) ;
#92779=CARTESIAN_POINT ( 'NONE',  ( 67.96666666666666856, 6.915964383211875250E-15, 0.000000000000000000 ) ) ;
#92796=CARTESIAN_POINT ( 'NONE',  ( 66.74444444444444002, 6.915964383211875250E-15, 0.000000000000000000 ) ) ;
#92813=AXIS2_PLACEMENT_3D ( 'NONE', #91325, #106413, #16900 ) ;
#92860=AXIS2_PLACEMENT_3D ( 'NONE', #46136, #96290, #22415 ) ;
#92876=ORIENTED_EDGE ( 'NONE', *, *, #89960, .T. ) ;
#92882=ADVANCED_FACE ( 'NONE', ( #78882 ), #26124, .T. ) ;
#92895=CARTESIAN_POINT ( 'NONE',  ( 56.22793774957824553, -4.000000000000000888, 4.898587196589422689E-16 ) ) ;
#92924=EDGE_CURVE ( 'NONE', #54950, #106205, #30360, .T. ) ;
#92972=CARTESIAN_POINT ( 'NONE',  ( 57.45015997180046696, -4.000000000000000888, 4.898587196589422689E-16 ) ) ;
#92994=DIRECTION ( 'NONE',  ( -1.000000000000000000, -1.224606353822377258E-16, -0.000000000000000000 ) ) ;
#93070=EDGE_LOOP ( 'NONE', ( #86236, #24566, #4646, #5094, #29151 ) ) ;
#93119=CARTESIAN_POINT ( 'NONE',  ( 64.78349330513380266, 4.000000000000013323, 0.000000000000000000 ) ) ;
#93198=CARTESIAN_POINT ( 'NONE',  ( 63.81650669486618455, 6.856755485862130937E-15, 0.000000000000000000 ) ) ;
#93206=SURFACE_STYLE_FILL_AREA ( #45206 ) ;
#93211=AXIS2_PLACEMENT_3D ( 'NONE', #83366, #42376, #105520 ) ;
#93224=ORIENTED_EDGE ( 'NONE', *, *, #50779, .F. ) ;
#93228=VERTEX_POINT ( 'NONE', #81924 ) ;
#93277=DIRECTION ( 'NONE',  ( -1.000000000000000000, -1.224606353822377258E-16, -0.000000000000000000 ) ) ;
#93278=VERTEX_POINT ( 'NONE', #24271 ) ;
#93291=CIRCLE ( 'NONE', #45115, 4.000000000000007105 ) ;
#93299=CONICAL_SURFACE ( 'NONE', #101909, 4.000000000000007105, 0.9599310885968835860 ) ;
#93418=CYLINDRICAL_SURFACE ( 'NONE', #6604, 4.000000000000000000 ) ;
#93427=VERTEX_POINT ( 'NONE', #60356 ) ;
#93454=EDGE_LOOP ( 'NONE', ( #59407, #61821, #103980, #1333, #87897 ) ) ;
#93469=EDGE_CURVE ( 'NONE', #80696, #23441, #311, .T. ) ;
#93477=EDGE_CURVE ( 'NONE', #57235, #21935, #23484, .T. ) ;
#93489=VECTOR ( 'NONE', #89505, 1000.000000000000000 ) ;
#93530=VERTEX_POINT ( 'NONE', #19924 ) ;
#93592=AXIS2_PLACEMENT_3D ( 'NONE', #91925, #76265, #67125 ) ;
#93605=EDGE_CURVE ( 'NONE', #59016, #11977, #17504, .T. ) ;
#93639=ORIENTED_EDGE ( 'NONE', *, *, #91283, .T. ) ;
#93658=ORIENTED_EDGE ( 'NONE', *, *, #15452, .T. ) ;
#93744=CYLINDRICAL_SURFACE ( 'NONE', #97826, 4.000000000000000000 ) ;
#93782=CARTESIAN_POINT ( 'NONE',  ( 0.000000000000000000, 1.502314598737160017E-15, -6.500000000000000000 ) ) ;
#93818=ADVANCED_FACE ( 'NONE', ( #60628 ), #51438, .T. ) ;
#93834=ORIENTED_EDGE ( 'NONE', *, *, #45544, .F. ) ;
#93866=ADVANCED_FACE ( 'NONE', ( #67642 ), #59553, .T. ) ;
#93882=ORIENTED_EDGE ( 'NONE', *, *, #5622, .F. ) ;
#93924=ORIENTED_EDGE ( 'NONE', *, *, #92924, .F. ) ;
#93946=DIRECTION ( 'NONE',  ( -1.000000000000000000, -1.224606353822377258E-16, -0.000000000000000000 ) ) ;
#93947=ORIENTED_EDGE ( 'NONE', *, *, #78702, .F. ) ;
#93956=EDGE_CURVE ( 'NONE', #81058, #25843, #5029, .T. ) ;
#94053=DIRECTION ( 'NONE',  ( -1.000000000000000000, -1.224606353822377258E-16, -0.000000000000000000 ) ) ;
#94054=DIRECTION ( 'NONE',  ( -1.000000000000000000, -1.224606353822377258E-16, -0.000000000000000000 ) ) ;
#94095=DIRECTION ( 'NONE',  ( 1.000000000000000000, 1.224606353822377258E-16, 0.000000000000000000 ) ) ;
#94151=CYLINDRICAL_SURFACE ( 'NONE', #104161, 4.000000000000000000 ) ;
#94163=ORIENTED_EDGE ( 'NONE', *, *, #36130, .T. ) ;
#94259=ORIENTED_EDGE ( 'NONE', *, *, #106628, .T. ) ;
#94297=EDGE_CURVE ( 'NONE', #22931, #59650, #10318, .T. ) ;
#94318=CARTESIAN_POINT ( 'NONE',  ( 56.48317336153285595, 6.856755485862130937E-15, 0.000000000000000000 ) ) ;
#94358=CARTESIAN_POINT ( 'NONE',  ( 59.89460441624491693, 4.000000000000013323, 0.000000000000000000 ) ) ;
#94411=ORIENTED_EDGE ( 'NONE', *, *, #17302, .F. ) ;
#94418=DIRECTION ( 'NONE',  ( -1.000000000000000000, -0.000000000000000000, -0.000000000000000000 ) ) ;
#94422=EDGE_CURVE ( 'NONE', #98735, #75420, #84906, .T. ) ;
#94488=DIRECTION ( 'NONE',  ( 0.000000000000000000, -2.311253228826402606E-16, -1.000000000000000000 ) ) ;
#94506=CIRCLE ( 'NONE', #75526, 4.000000000000007105 ) ;
#94515=CARTESIAN_POINT ( 'NONE',  ( 54.03872891708841308, 4.898587196589294500E-16, -4.000000000000007105 ) ) ;
#94579=ORIENTED_EDGE ( 'NONE', *, *, #78109, .T. ) ;
#94603=ORIENTED_EDGE ( 'NONE', *, *, #57748, .F. ) ;
#94623=EDGE_CURVE ( 'NONE', #103960, #54493, #20627, .T. ) ;
#94701=FACE_OUTER_BOUND ( 'NONE', #45845, .T. ) ;
#94703=ADVANCED_FACE ( 'NONE', ( #31345 ), #460, .T. ) ;
#94705=DIRECTION ( 'NONE',  ( 0.000000000000000000, 0.000000000000000000, 1.000000000000000000 ) ) ;
#94707=ORIENTED_EDGE ( 'NONE', *, *, #86814, .F. ) ;
#94740=CARTESIAN_POINT ( 'NONE',  ( 64.78349330513380266, 6.975173280561618775E-15, 0.000000000000000000 ) ) ;
#94760=AXIS2_PLACEMENT_3D ( 'NONE', #2933, #103238, #101647 ) ;
#94772=VERTEX_POINT ( 'NONE', #9137 ) ;
#94898=EDGE_CURVE ( 'NONE', #104615, #38361, #90118, .T. ) ;
#94908=AXIS2_PLACEMENT_3D ( 'NONE', #26983, #93277, #10218 ) ;
#94927=VECTOR ( 'NONE', #4289, 1000.000000000000227 ) ;
#94930=FACE_OUTER_BOUND ( 'NONE', #2602, .T. ) ;
#94981=CIRCLE ( 'NONE', #65698, 4.000000000000007105 ) ;
#94987=CIRCLE ( 'NONE', #65780, 4.000000000000007105 ) ;
#95002=DIRECTION ( 'NONE',  ( 0.5735764363510440500, 0.8191520442889932418, 0.000000000000000000 ) ) ;
#95026=CARTESIAN_POINT ( 'NONE',  ( 69.67238219402268840, 6.975173280561618775E-15, 0.000000000000000000 ) ) ;
#95112=DIRECTION ( 'NONE',  ( -0.5735764363510494901, -0.8191520442889894671, 0.000000000000000000 ) ) ;
#95165=ORIENTED_EDGE ( 'NONE', *, *, #5066, .T. ) ;
#95273=ORIENTED_EDGE ( 'NONE', *, *, #2438, .F. ) ;
#95332=DIRECTION ( 'NONE',  ( -1.000000000000000000, -1.224606353822377258E-16, -0.000000000000000000 ) ) ;
#95358=VECTOR ( 'NONE', #27930, 1000.000000000000000 ) ;
#95386=ORIENTED_EDGE ( 'NONE', *, *, #96075, .T. ) ;
#95388=VECTOR ( 'NONE', #62717, 1000.000000000000000 ) ;
#95440=DIRECTION ( 'NONE',  ( -0.5735764363510494901, -0.8191520442889894671, 0.000000000000000000 ) ) ;
#95445=ORIENTED_EDGE ( 'NONE', *, *, #17416, .T. ) ;
#95455=CARTESIAN_POINT ( 'NONE',  ( 61.11682663846713837, 6.975173280561618775E-15, 0.000000000000000000 ) ) ;
#95459=CARTESIAN_POINT ( 'NONE',  ( 0.000000000000000000, 0.000000000000000000, 0.000000000000000000 ) ) ;
#95487=ADVANCED_FACE ( 'NONE', ( #19033 ), #24780, .T. ) ;
#95528=CARTESIAN_POINT ( 'NONE',  ( 59.41111111111111143, 3.309500000000014541, 4.052968581778174646E-16 ) ) ;
#95533=CARTESIAN_POINT ( 'NONE',  ( 62.33904886068935980, -1.232595164407830946E-29, 4.000000000000007105 ) ) ;
#95556=ORIENTED_EDGE ( 'NONE', *, *, #74241, .F. ) ;
#95563=ADVANCED_FACE ( 'NONE', ( #61593 ), #84785, .F. ) ;
#95585=DIRECTION ( 'NONE',  ( -1.000000000000000000, -1.224606353822377258E-16, -0.000000000000000000 ) ) ;
#95602=ORIENTED_EDGE ( 'NONE', *, *, #33990, .F. ) ;
#95633=DIRECTION ( 'NONE',  ( 0.5735764363510440500, 0.8191520442889932418, 0.000000000000000000 ) ) ;
#95637=VECTOR ( 'NONE', #80037, 1000.000000000000000 ) ;
#95639=CARTESIAN_POINT ( 'NONE',  ( 66.00571552735603120, 6.975173280561618775E-15, 0.000000000000000000 ) ) ;
#95691=VECTOR ( 'NONE', #10201, 1000.000000000000000 ) ;
#95696=CIRCLE ( 'NONE', #49167, 4.000000000000007105 ) ;
#95715=CARTESIAN_POINT ( 'NONE',  ( 71.14984002819953446, -4.000000000000000000, 0.000000000000000000 ) ) ;
#95741=DIRECTION ( 'NONE',  ( -1.000000000000000000, -1.224606353822377258E-16, -0.000000000000000000 ) ) ;
#95745=DIRECTION ( 'NONE',  ( 0.000000000000000000, -1.000000000000000000, 0.000000000000000000 ) ) ;
#95792=AXIS2_PLACEMENT_3D ( 'NONE', #60844, #21985, #13851 ) ;
#95817=CIRCLE ( 'NONE', #2792, 4.000000000000007105 ) ;
#95890=VERTEX_POINT ( 'NONE', #36679 ) ;
#95892=EDGE_LOOP ( 'NONE', ( #17111, #47838, #104807, #104592, #85691 ) ) ;
#95961=CARTESIAN_POINT ( 'NONE',  ( 59.89460441624491693, -4.000000000000000888, 4.898587196589422689E-16 ) ) ;
#95983=CARTESIAN_POINT ( 'NONE',  ( 63.56127108291158123, 4.898587196589294500E-16, -4.000000000000007105 ) ) ;
#95989=EDGE_CURVE ( 'NONE', #68935, #30792, #40079, .T. ) ;
#95991=EDGE_LOOP ( 'NONE', ( #94603, #51649, #79179, #102398, #85340 ) ) ;
#96075=EDGE_CURVE ( 'NONE', #52615, #22977, #5847, .T. ) ;
#96099=CARTESIAN_POINT ( 'NONE',  ( 4.699999999999999289, -7.505553499465138501, 0.000000000000000000 ) ) ;
#96108=DIRECTION ( 'NONE',  ( 0.000000000000000000, 0.8660254037844377084, -0.5000000000000017764 ) ) ;
#96117=B_SPLINE_CURVE_WITH_KNOTS ( 'NONE', 3,
 ( #87189, #13268, #46190, #85604, #36016, #28998 ),
 .UNSPECIFIED., .F., .F.,
 ( 4, 2, 4 ),
 ( 0.01067228061038543591, 0.01257272967564228294, 0.01447317874089912824 ),
 .UNSPECIFIED. ) ;
#96125=CIRCLE ( 'NONE', #87589, 4.000000000000007105 ) ;
#96129=ORIENTED_EDGE ( 'NONE', *, *, #12202, .F. ) ;
#96139=DIRECTION ( 'NONE',  ( 0.000000000000000000, -1.000000000000000000, 0.000000000000000000 ) ) ;
#96144=DIRECTION ( 'NONE',  ( 0.000000000000000000, -0.5000000000000004441, 0.8660254037844383745 ) ) ;
#96158=AXIS2_PLACEMENT_3D ( 'NONE', #95455, #72752, #46377 ) ;
#96169=DIRECTION ( 'NONE',  ( 0.000000000000000000, 0.000000000000000000, 1.000000000000000000 ) ) ;
#96239=AXIS2_PLACEMENT_3D ( 'NONE', #53685, #103311, #95745 ) ;
#96264=DIRECTION ( 'NONE',  ( -1.000000000000000000, -1.224606353822377258E-16, -0.000000000000000000 ) ) ;
#96290=DIRECTION ( 'NONE',  ( -1.000000000000000000, -0.000000000000000000, -0.000000000000000000 ) ) ;
#96324=CARTESIAN_POINT ( 'NONE',  ( 64.78349330513380266, -1.232595164407830946E-29, 4.000000000000007105 ) ) ;
#96326=AXIS2_PLACEMENT_3D ( 'NONE', #4670, #54784, #29510 ) ;
#96361=CARTESIAN_POINT ( 'NONE',  ( 0.000000000000000000, 5.629165124598842773, -3.250000000000011990 ) ) ;
#96365=EDGE_CURVE ( 'NONE', #8358, #61384, #48750, .T. ) ;
#96387=CARTESIAN_POINT ( 'NONE',  ( 0.000000000000000000, 0.000000000000000000, 4.000000000000000000 ) ) ;
#96406=ORIENTED_EDGE ( 'NONE', *, *, #19204, .F. ) ;
#96423=ORIENTED_EDGE ( 'NONE', *, *, #73428, .T. ) ;
#96458=CARTESIAN_POINT ( 'NONE',  ( 58.18888888888888999, -3.309500000000000774, 4.475777889183797681E-16 ) ) ;
#96467=DIRECTION ( 'NONE',  ( 0.000000000000000000, -1.000000000000000000, 0.000000000000000000 ) ) ;
#96472=ORIENTED_EDGE ( 'NONE', *, *, #69354, .F. ) ;
#96483=CARTESIAN_POINT ( 'NONE',  ( 58.67238219402268840, 4.000000000000013323, 0.000000000000000000 ) ) ;
#96495=DIRECTION ( 'NONE',  ( -0.000000000000000000, 0.000000000000000000, 1.000000000000000000 ) ) ;
#96541=ORIENTED_EDGE ( 'NONE', *, *, #44063, .F. ) ;
#96543=LINE ( 'NONE', #78741, #8173 ) ;
#96593=CIRCLE ( 'NONE', #41442, 4.000000000000007105 ) ;
#96596=ORIENTED_EDGE ( 'NONE', *, *, #79096, .F. ) ;
#96598=CIRCLE ( 'NONE', #91208, 3.309500000000007880 ) ;
#96602=CARTESIAN_POINT ( 'NONE',  ( 63.81650669486618455, -1.232595164407830946E-29, 4.000000000000007105 ) ) ;
#96617=EDGE_LOOP ( 'NONE', ( #35635, #61914, #4113, #12464, #904, #71835 ) ) ;
#96642=CONICAL_SURFACE ( 'NONE', #34698, 3.309500000000007880, 0.9599310885968770357 ) ;
#96660=ORIENTED_EDGE ( 'NONE', *, *, #35280, .F. ) ;
#96676=EDGE_CURVE ( 'NONE', #90844, #86309, #105589, .T. ) ;
#96690=B_SPLINE_CURVE_WITH_KNOTS ( 'NONE', 3,
 ( #90359, #8372, #1320, #43414, #16470, #41801, #82259, #33209 ),
 .UNSPECIFIED., .F., .F.,
 ( 4, 2, 2, 4 ),
 ( 0.003797433802554435033, 0.004743183970586232687, 0.005688934138618029906, 0.007580434474681625213 ),
 .UNSPECIFIED. ) ;
#96702=CARTESIAN_POINT ( 'NONE',  ( 0.000000000000000000, 1.502314598737161398E-15, 6.499999999999999112 ) ) ;
#96792=ORIENTED_EDGE ( 'NONE', *, *, #101942, .T. ) ;
#96810=DIRECTION ( 'NONE',  ( 0.000000000000000000, 1.000000000000000000, 0.000000000000000000 ) ) ;
#96812=ORIENTED_EDGE ( 'NONE', *, *, #50019, .F. ) ;
#96819=VECTOR ( 'NONE', #29021, 1000.000000000000000 ) ;
#96854=DIRECTION ( 'NONE',  ( -0.5735764363510497121, 0.8191520442889892450, 1.003171929053521665E-16 ) ) ;
#96857=CARTESIAN_POINT ( 'NONE',  ( 53.29999999999999716, -3.309500000000000774, 4.475777889183797681E-16 ) ) ;
#96860=ADVANCED_FACE ( 'NONE', ( #83292 ), #19577, .T. ) ;
#96875=CIRCLE ( 'NONE', #3878, 4.000000000000007105 ) ;
#96889=DIRECTION ( 'NONE',  ( -1.000000000000000000, -1.224606353822377258E-16, -0.000000000000000000 ) ) ;
#96935=ORIENTED_EDGE ( 'NONE', *, *, #23903, .T. ) ;
#96951=AXIS2_PLACEMENT_3D ( 'NONE', #21970, #53774, #71022 ) ;
#96955=VERTEX_POINT ( 'NONE', #26174 ) ;
#96976=ORIENTED_EDGE ( 'NONE', *, *, #38528, .F. ) ;
#97052=ORIENTED_EDGE ( 'NONE', *, *, #100243, .T. ) ;
#97089=AXIS2_PLACEMENT_3D ( 'NONE', #66797, #82442, #18265 ) ;
#97127=EDGE_CURVE ( 'NONE', #91765, #36600, #23011, .T. ) ;
#97180=AXIS2_PLACEMENT_3D ( 'NONE', #88906, #47373, #64634 ) ;
#97206=DIRECTION ( 'NONE',  ( 0.000000000000000000, -1.000000000000000000, 0.000000000000000000 ) ) ;
#97230=ADVANCED_FACE ( 'NONE', ( #75190 ), #52302, .T. ) ;
#97262=FACE_OUTER_BOUND ( 'NONE', #98309, .T. ) ;
#97271=DIRECTION ( 'NONE',  ( -1.000000000000000000, -0.000000000000000000, -0.000000000000000000 ) ) ;
#97320=DIRECTION ( 'NONE',  ( 0.000000000000000000, -1.000000000000000000, 0.000000000000000000 ) ) ;
#97342=ORIENTED_EDGE ( 'NONE', *, *, #58280, .T. ) ;
#97388=DIRECTION ( 'NONE',  ( 0.000000000000000000, -1.000000000000000000, 0.000000000000000000 ) ) ;
#97391=CARTESIAN_POINT ( 'NONE',  ( 56.96666666666666856, 3.309500000000014541, 4.052968581778174646E-16 ) ) ;
#97409=CARTESIAN_POINT ( 'NONE',  ( 56.22793774957824553, 6.975173280561618775E-15, 0.000000000000000000 ) ) ;
#97493=DIRECTION ( 'NONE',  ( 0.000000000000000000, -1.000000000000000000, 0.000000000000000000 ) ) ;
#97496=ORIENTED_EDGE ( 'NONE', *, *, #101283, .T. ) ;
#97504=AXIS2_PLACEMENT_3D ( 'NONE', #102831, #13264, #53216 ) ;
#97524=VERTEX_POINT ( 'NONE', #96458 ) ;
#97533=ORIENTED_EDGE ( 'NONE', *, *, #18926, .T. ) ;
#97534=EDGE_CURVE ( 'NONE', #43629, #66517, #76472, .T. ) ;
#97551=DIRECTION ( 'NONE',  ( 0.000000000000000000, -1.000000000000000000, 0.000000000000000000 ) ) ;
#97554=EDGE_LOOP ( 'NONE', ( #34264, #28558, #40274, #82658, #44109 ) ) ;
#97609=ADVANCED_FACE ( 'NONE', ( #888 ), #102291, .T. ) ;
#97664=FACE_OUTER_BOUND ( 'NONE', #85433, .T. ) ;
#97671=DIRECTION ( 'NONE',  ( 0.000000000000000000, 0.4999999999999991673, -0.8660254037844390407 ) ) ;
#97734=DIRECTION ( 'NONE',  ( 0.000000000000000000, -1.000000000000000000, 0.000000000000000000 ) ) ;
#97792=CARTESIAN_POINT ( 'NONE',  ( 69.92761780597730592, 6.856755485862130937E-15, 0.000000000000000000 ) ) ;
#97804=CARTESIAN_POINT ( 'NONE',  ( 0.5805565836007648972, -7.505553499465138501, -1.190388518514737689E-16 ) ) ;
#97807=DIRECTION ( 'NONE',  ( -1.000000000000000000, -1.224606353822377258E-16, -0.000000000000000000 ) ) ;
#97826=AXIS2_PLACEMENT_3D ( 'NONE', #84592, #35002, #36608 ) ;
#97846=DIRECTION ( 'NONE',  ( -1.000000000000000000, -1.224606353822377258E-16, -0.000000000000000000 ) ) ;
#97865=DIRECTION ( 'NONE',  ( -1.000000000000000000, -0.000000000000000000, -0.000000000000000000 ) ) ;
#97928=CIRCLE ( 'NONE', #51427, 4.000000000000007105 ) ;
#97929=LINE ( 'NONE', #16486, #57202 ) ;
#97962=CARTESIAN_POINT ( 'NONE',  ( 5.299999999999999822, -3.752776749732553263, 6.499999999999999112 ) ) ;
#97970=CIRCLE ( 'NONE', #92813, 4.000000000000007105 ) ;
#97995=VECTOR ( 'NONE', #40471, 1000.000000000000000 ) ;
#98043=CLOSED_SHELL ( 'NONE', ( #69524, #66648, #94703, #96860, #83799, #21406, #14116, #99493, #62498, #64748, #66999, #27714, #47389, #40942, #1752, #13602, #505, #55549, #62227, #104882, #14426, #27464, #61509, #6877, #37327, #62768, #56566, #3189, #13303, #30595, #35311, #13769, #63372, #11836, #27063, #103015, #26337, #34035, #81244, #97609, #58944, #102245, #15267, #57278, #95487, #26422, #60693, #50060, #104004, #43296, #27509, #18188, #8247, #105709, #10749, #80567, #27111, #22048, #10102, #44656, #45138, #47896, #45528, #8060, #55224, #21279, #30697, #55875, #24968, #25068, #42835, #10532, #48288, #88320, #55302, #71172, #87791, #95563, #7806, #41848, #103487, #58396, #85777, #93866, #15421, #4149, #41812, #14742, #47052, #93818, #53083, #59212, #46011, #86919, #97230, #101262, #80968, #83141, #39227, #56710, #57246, #80038, #454, #79103, #82680, #42027, #86186, #59562, #8864, #22477, #82249, #33781, #89372, #72805, #39313, #13221, #25923, #53735, #15472, #76443, #39383, #46236, #43525, #52078, #62258, #44106, #13910, #92882, #43248, #9275, #26173, #73640, #46477, #65497, #44233, #31709, #31854 ) ) ;
#98060=CARTESIAN_POINT ( 'NONE',  ( 59.89460441624491693, 4.000000000000014211, 0.000000000000000000 ) ) ;
#98115=CARTESIAN_POINT ( 'NONE',  ( 68.45015997180047407, 6.975173280561618775E-15, 0.000000000000000000 ) ) ;
#98126=DIRECTION ( 'NONE',  ( 0.000000000000000000, 0.000000000000000000, 1.000000000000000000 ) ) ;
#98188=AXIS2_PLACEMENT_3D ( 'NONE', #27217, #75720, #85972 ) ;
#98285=CARTESIAN_POINT ( 'NONE',  ( 64.78349330513380266, 6.975173280561618775E-15, 0.000000000000000000 ) ) ;
#98286=VERTEX_POINT ( 'NONE', #95533 ) ;
#98307=CARTESIAN_POINT ( 'NONE',  ( 57.70539558375507738, 4.000000000000015099, 4.898587196589422689E-16 ) ) ;
#98309=EDGE_LOOP ( 'NONE', ( #62132, #20476, #85261, #12555, #14276 ) ) ;
#98348=CARTESIAN_POINT ( 'NONE',  ( 63.56127108291158123, -4.000000000000000888, 4.898587196589422689E-16 ) ) ;
#98381=DIRECTION ( 'NONE',  ( 0.000000000000000000, -0.4999999999999991673, 0.8660254037844390407 ) ) ;
#98394=ORIENTED_EDGE ( 'NONE', *, *, #32172, .F. ) ;
#98414=EDGE_LOOP ( 'NONE', ( #69261, #33750, #4469, #58511, #46413, #96812 ) ) ;
#98416=CARTESIAN_POINT ( 'NONE',  ( 0.000000000000000000, 4.898587196589412829E-16, -4.000000000000000000 ) ) ;
#98469=DIRECTION ( 'NONE',  ( -0.000000000000000000, 1.000000000000000000, 2.311253228826400140E-16 ) ) ;
#98526=DIRECTION ( 'NONE',  ( -1.000000000000000000, -1.224606353822377258E-16, -0.000000000000000000 ) ) ;
#98536=ORIENTED_EDGE ( 'NONE', *, *, #23260, .F. ) ;
#98541=ORIENTED_EDGE ( 'NONE', *, *, #99726, .T. ) ;
#98563=DIRECTION ( 'NONE',  ( 0.000000000000000000, 0.000000000000000000, 1.000000000000000000 ) ) ;
#98600=CARTESIAN_POINT ( 'NONE',  ( 66.00571552735603120, 6.975173280561618775E-15, 0.000000000000000000 ) ) ;
#98636=LINE ( 'NONE', #39373, #93489 ) ;
#98699=SHAPE_REPRESENTATION_RELATIONSHIP ( 'NONE' , 'NONE' ,  #77771, #48600 ) ;
#98734=VERTEX_POINT ( 'NONE', #94358 ) ;
#98735=VERTEX_POINT ( 'NONE', #69546 ) ;
#98738=EDGE_CURVE ( 'NONE', #7738, #50186, #44363, .T. ) ;
#98817=ORIENTED_EDGE ( 'NONE', *, *, #67494, .F. ) ;
#98848=FACE_OUTER_BOUND ( 'NONE', #78347, .T. ) ;
#98861=VERTEX_POINT ( 'NONE', #73086 ) ;
#98880=EDGE_LOOP ( 'NONE', ( #100048, #104264, #34499, #66802, #100960 ) ) ;
#98895=EDGE_CURVE ( 'NONE', #77883, #57259, #28482, .T. ) ;
#98920=AXIS2_PLACEMENT_3D ( 'NONE', #30374, #46015, #78894 ) ;
#98974=CARTESIAN_POINT ( 'NONE',  ( 4.699999999999999289, -3.752776749732578132, -6.500000000000000888 ) ) ;
#98992=VECTOR ( 'NONE', #35322, 1000.000000000000227 ) ;
#99023=ORIENTED_EDGE ( 'NONE', *, *, #10630, .T. ) ;
#99028=VERTEX_POINT ( 'NONE', #84404 ) ;
#99060=AXIS2_PLACEMENT_3D ( 'NONE', #74264, #339, #106632 ) ;
#99073=AXIS2_PLACEMENT_3D ( 'NONE', #71297, #95585, #22780 ) ;
#99075=CIRCLE ( 'NONE', #28523, 4.000000000000007105 ) ;
#99089=DIRECTION ( 'NONE',  ( -1.000000000000000000, -1.224606353822377258E-16, -0.000000000000000000 ) ) ;
#99128=VERTEX_POINT ( 'NONE', #12611 ) ;
#99146=CIRCLE ( 'NONE', #9602, 3.309500000000007880 ) ;
#99176=CARTESIAN_POINT ( 'NONE',  ( 69.18888888888888289, -3.309500000000000774, 0.000000000000000000 ) ) ;
#99202=DIRECTION ( 'NONE',  ( 0.000000000000000000, -1.000000000000000000, 0.000000000000000000 ) ) ;
#99223=ORIENTED_EDGE ( 'NONE', *, *, #61085, .F. ) ;
#99285=VECTOR ( 'NONE', #34387, 1000.000000000000000 ) ;
#99287=EDGE_LOOP ( 'NONE', ( #18274, #24166 ) ) ;
#99292=CIRCLE ( 'NONE', #75206, 4.000000000000007105 ) ;
#99293=DIRECTION ( 'NONE',  ( -1.000000000000000000, -1.224606353822377258E-16, -0.000000000000000000 ) ) ;
#99316=EDGE_LOOP ( 'NONE', ( #91618, #18744, #86952, #23410, #90668 ) ) ;
#99325=CIRCLE ( 'NONE', #83860, 4.000000000000007105 ) ;
#99332=EDGE_LOOP ( 'NONE', ( #96541, #9579, #75435, #58762, #95273 ) ) ;
#99377=LINE ( 'NONE', #97391, #80817 ) ;
#99421=AXIS2_PLACEMENT_3D ( 'NONE', #43260, #35193, #13529 ) ;
#99447=AXIS2_PLACEMENT_3D ( 'NONE', #72989, #97807, #32580 ) ;
#99463=VERTEX_POINT ( 'NONE', #103117 ) ;
#99484=VECTOR ( 'NONE', #19955, 1000.000000000000000 ) ;
#99487=EDGE_CURVE ( 'NONE', #32311, #80696, #61259, .T. ) ;
#99492=EDGE_CURVE ( 'NONE', #53571, #14336, #77245, .T. ) ;
#99493=ADVANCED_FACE ( 'NONE', ( #36822 ), #29788, .T. ) ;
#99504=CARTESIAN_POINT ( 'NONE',  ( 62.33904886068935980, 4.898587196589294500E-16, -4.000000000000007105 ) ) ;
#99547=CONICAL_SURFACE ( 'NONE', #61634, 4.000000000000007105, 0.9599310885968835860 ) ;
#99587=DIRECTION ( 'NONE',  ( 0.000000000000000000, 0.000000000000000000, -1.000000000000000000 ) ) ;
#99592=DIRECTION ( 'NONE',  ( -1.000000000000000000, -1.224606353822377258E-16, -0.000000000000000000 ) ) ;
#99595=EDGE_LOOP ( 'NONE', ( #71959, #22670, #72378, #22333, #18698 ) ) ;
#99616=AXIS2_PLACEMENT_3D ( 'NONE', #42731, #102021, #28181 ) ;
#99678=VECTOR ( 'NONE', #27392, 1000.000000000000000 ) ;
#99696=VERTEX_POINT ( 'NONE', #36169 ) ;
#99726=EDGE_CURVE ( 'NONE', #81361, #8468, #56046, .T. ) ;
#99732=VERTEX_POINT ( 'NONE', #40361 ) ;
#99750=DIRECTION ( 'NONE',  ( -1.000000000000000000, -1.224606353822377258E-16, -0.000000000000000000 ) ) ;
#99751=ORIENTED_EDGE ( 'NONE', *, *, #14823, .F. ) ;
#99806=DIRECTION ( 'NONE',  ( -1.000000000000000000, -1.224606353822377258E-16, -0.000000000000000000 ) ) ;
#99810=LINE ( 'NONE', #34056, #37461 ) ;
#99820=ORIENTED_EDGE ( 'NONE', *, *, #67494, .T. ) ;
#99821=CARTESIAN_POINT ( 'NONE',  ( 68.70539558375507738, 6.856755485862130937E-15, 0.000000000000000000 ) ) ;
#99834=ORIENTED_EDGE ( 'NONE', *, *, #60292, .T. ) ;
#99857=AXIS2_PLACEMENT_3D ( 'NONE', #17601, #68267, #42382 ) ;
#99931=CARTESIAN_POINT ( 'NONE',  ( 0.000000000000000000, 0.000000000000000000, 0.000000000000000000 ) ) ;
#99970=CARTESIAN_POINT ( 'NONE',  ( 72.11682663846713126, 6.975173280561618775E-15, 0.000000000000000000 ) ) ;
#100016=ORIENTED_EDGE ( 'NONE', *, *, #1973, .F. ) ;
#100034=VECTOR ( 'NONE', #80309, 1000.000000000000000 ) ;
#100042=DIRECTION ( 'NONE',  ( -1.000000000000000000, -1.224606353822377258E-16, -0.000000000000000000 ) ) ;
#100048=ORIENTED_EDGE ( 'NONE', *, *, #84299, .T. ) ;
#100082=DIRECTION ( 'NONE',  ( -1.000000000000000000, -1.224606353822377258E-16, -0.000000000000000000 ) ) ;
#100094=CIRCLE ( 'NONE', #53604, 4.000000000000007105 ) ;
#100109=VECTOR ( 'NONE', #26917, 1000.000000000000000 ) ;
#100125=ORIENTED_EDGE ( 'NONE', *, *, #71081, .T. ) ;
#100150=ORIENTED_EDGE ( 'NONE', *, *, #66454, .F. ) ;
#100161=EDGE_CURVE ( 'NONE', #31268, #38217, #26140, .T. ) ;
#100171=CARTESIAN_POINT ( 'NONE',  ( 53.29999999999999716, -3.309500000000000774, 0.000000000000000000 ) ) ;
#100205=CARTESIAN_POINT ( 'NONE',  ( 56.48317336153285595, 6.856755485862130937E-15, 0.000000000000000000 ) ) ;
#100208=DIRECTION ( 'NONE',  ( 0.000000000000000000, -1.000000000000000000, 0.000000000000000000 ) ) ;
#100223=DIRECTION ( 'NONE',  ( -1.000000000000000000, -1.224606353822377258E-16, -0.000000000000000000 ) ) ;
#100236=DIRECTION ( 'NONE',  ( -1.000000000000000000, -1.224606353822377258E-16, -0.000000000000000000 ) ) ;
#100243=EDGE_CURVE ( 'NONE', #31268, #66339, #87206, .T. ) ;
#100260=ORIENTED_EDGE ( 'NONE', *, *, #23770, .T. ) ;
#100264=DIRECTION ( 'NONE',  ( -1.000000000000000000, -1.224606353822377258E-16, -0.000000000000000000 ) ) ;
#100276=DIRECTION ( 'NONE',  ( -1.000000000000000000, -0.000000000000000000, -0.000000000000000000 ) ) ;
#100321=DIRECTION ( 'NONE',  ( 0.000000000000000000, -1.000000000000000000, 0.000000000000000000 ) ) ;
#100414=ORIENTED_EDGE ( 'NONE', *, *, #102318, .T. ) ;
#100420=EDGE_CURVE ( 'NONE', #57235, #6434, #61415, .T. ) ;
#100465=DIRECTION ( 'NONE',  ( -1.000000000000000000, -0.000000000000000000, -0.000000000000000000 ) ) ;
#100524=DIRECTION ( 'NONE',  ( 0.000000000000000000, -1.000000000000000000, 0.000000000000000000 ) ) ;
#100527=ORIENTED_EDGE ( 'NONE', *, *, #33459, .T. ) ;
#100628=CIRCLE ( 'NONE', #54113, 4.000000000000007105 ) ;
#100654=ORIENTED_EDGE ( 'NONE', *, *, #84286, .F. ) ;
#100677=DIRECTION ( 'NONE',  ( 0.000000000000000000, 0.000000000000000000, -1.000000000000000000 ) ) ;
#100685=CARTESIAN_POINT ( 'NONE',  ( 63.81650669486618455, 6.856755485862130937E-15, 0.000000000000000000 ) ) ;
#100705=DIRECTION ( 'NONE',  ( 0.000000000000000000, -1.000000000000000000, 0.000000000000000000 ) ) ;
#100720=CARTESIAN_POINT ( 'NONE',  ( 71.14984002819953446, -1.232595164407830946E-29, 4.000000000000007105 ) ) ;
#100722=CARTESIAN_POINT ( 'NONE',  ( 0.4037800551813753858, -7.199367570657607907, -0.5303295852573132185 ) ) ;
#100732=CYLINDRICAL_SURFACE ( 'NONE', #55126, 4.000000000000000000 ) ;
#100750=CARTESIAN_POINT ( 'NONE',  ( 62.33904886068935980, 4.000000000000014211, 0.000000000000000000 ) ) ;
#100752=EDGE_CURVE ( 'NONE', #18822, #40695, #9757, .T. ) ;
#100793=ORIENTED_EDGE ( 'NONE', *, *, #31588, .T. ) ;
#100813=CARTESIAN_POINT ( 'NONE',  ( 57.45015997180046696, 6.975173280561618775E-15, 0.000000000000000000 ) ) ;
#100836=EDGE_CURVE ( 'NONE', #92331, #98735, #81922, .T. ) ;
#100853=CARTESIAN_POINT ( 'NONE',  ( 0.000000000000000000, 0.000000000000000000, 0.000000000000000000 ) ) ;
#100955=ORIENTED_EDGE ( 'NONE', *, *, #48127, .F. ) ;
#100960=ORIENTED_EDGE ( 'NONE', *, *, #17500, .F. ) ;
#100989=CARTESIAN_POINT ( 'NONE',  ( 56.48317336153285595, 4.000000000000015099, 4.898587196589422689E-16 ) ) ;
#100994=CONICAL_SURFACE ( 'NONE', #7975, 6.499999999999999112, 1.047197551196600296 ) ;
#100999=DIRECTION ( 'NONE',  ( 0.000000000000000000, 0.000000000000000000, 1.000000000000000000 ) ) ;
#101014=AXIS2_PLACEMENT_3D ( 'NONE', #105844, #25508, #91286 ) ;
#101034=ORIENTED_EDGE ( 'NONE', *, *, #85776, .F. ) ;
#101036=DIRECTION ( 'NONE',  ( 0.000000000000000000, -1.000000000000000000, 0.000000000000000000 ) ) ;
#101041=CIRCLE ( 'NONE', #1151, 3.309500000000007880 ) ;
#101045=EDGE_CURVE ( 'NONE', #4517, #90738, #101041, .T. ) ;
#101053=ORIENTED_EDGE ( 'NONE', *, *, #72528, .F. ) ;
#101073=ORIENTED_EDGE ( 'NONE', *, *, #17234, .T. ) ;
#101111=DIRECTION ( 'NONE',  ( 0.000000000000000000, -1.000000000000000000, 0.000000000000000000 ) ) ;
#101205=DIRECTION ( 'NONE',  ( 0.000000000000000000, -1.000000000000000000, 0.000000000000000000 ) ) ;
#101224=EDGE_CURVE ( 'NONE', #40289, #84395, #47335, .T. ) ;
#101262=ADVANCED_FACE ( 'NONE', ( #6334 ), #13366, .T. ) ;
#101283=EDGE_CURVE ( 'NONE', #84625, #14056, #47751, .T. ) ;
#101318=VERTEX_POINT ( 'NONE', #14963 ) ;
#101339=DIRECTION ( 'NONE',  ( 0.000000000000000000, 0.000000000000000000, 1.000000000000000000 ) ) ;
#101359=VERTEX_POINT ( 'NONE', #57017 ) ;
#101404=ORIENTED_EDGE ( 'NONE', *, *, #62779, .T. ) ;
#101511=LINE ( 'NONE', #68635, #40582 ) ;
#101527=CARTESIAN_POINT ( 'NONE',  ( 72.85555555555556850, 3.309500000000014541, 0.000000000000000000 ) ) ;
#101605=ORIENTED_EDGE ( 'NONE', *, *, #30692, .T. ) ;
#101647=DIRECTION ( 'NONE',  ( 0.000000000000000000, -1.000000000000000000, 0.000000000000000000 ) ) ;
#101654=CARTESIAN_POINT ( 'NONE',  ( 56.22793774957824553, 4.898587196589294500E-16, -4.000000000000007105 ) ) ;
#101692=CONICAL_SURFACE ( 'NONE', #1809, 3.309500000000007880, 0.9599310885968770357 ) ;
#101705=ORIENTED_EDGE ( 'NONE', *, *, #68360, .T. ) ;
#101718=EDGE_LOOP ( 'NONE', ( #94163, #37007, #22700, #83291, #4870 ) ) ;
#101721=LINE ( 'NONE', #42416, #7827 ) ;
#101742=DIRECTION ( 'NONE',  ( -1.000000000000000000, -1.224606353822377258E-16, -0.000000000000000000 ) ) ;
#101794=ORIENTED_EDGE ( 'NONE', *, *, #36130, .F. ) ;
#101865=CARTESIAN_POINT ( 'NONE',  ( 0.5805565836007667846, -3.752776749732578132, -6.500000000000000888 ) ) ;
#101888=VECTOR ( 'NONE', #102839, 1000.000000000000227 ) ;
#101909=AXIS2_PLACEMENT_3D ( 'NONE', #76805, #85447, #69278 ) ;
#101942=EDGE_CURVE ( 'NONE', #45881, #106169, #27511, .T. ) ;
#101949=ORIENTED_EDGE ( 'NONE', *, *, #50056, .F. ) ;
#101954=VECTOR ( 'NONE', #66971, 1000.000000000000227 ) ;
#101959=ORIENTED_EDGE ( 'NONE', *, *, #60766, .F. ) ;
#101972=FACE_OUTER_BOUND ( 'NONE', #47366, .T. ) ;
#102021=DIRECTION ( 'NONE',  ( 1.000000000000000000, 1.224606353822377258E-16, 0.000000000000000000 ) ) ;
#102057=DIRECTION ( 'NONE',  ( -1.000000000000000000, -1.224606353822377258E-16, -0.000000000000000000 ) ) ;
#102083=VERTEX_POINT ( 'NONE', #29626 ) ;
#102102=CARTESIAN_POINT ( 'NONE',  ( 63.81650669486618455, 6.856755485862130937E-15, 0.000000000000000000 ) ) ;
#102113=EDGE_CURVE ( 'NONE', #7306, #76519, #75390, .T. ) ;
#102132=ORIENTED_EDGE ( 'NONE', *, *, #58479, .T. ) ;
#102157=ORIENTED_EDGE ( 'NONE', *, *, #20017, .F. ) ;
#102199=ORIENTED_EDGE ( 'NONE', *, *, #32651, .T. ) ;
#102245=ADVANCED_FACE ( 'NONE', ( #73945 ), #90890, .T. ) ;
#102291=CONICAL_SURFACE ( 'NONE', #16199, 4.000000000000007105, 0.9599310885968835860 ) ;
#102293=COLOUR_RGB ( '', 0.66274510, 0.83137255, 0.94901961) ;
#102318=EDGE_CURVE ( 'NONE', #54844, #2515, #11645, .T. ) ;
#102336=VERTEX_POINT ( 'NONE', #17334 ) ;
#102348=DIRECTION ( 'NONE',  ( 0.000000000000000000, -1.000000000000000000, 0.000000000000000000 ) ) ;
#102354=FACE_OUTER_BOUND ( 'NONE', #73141, .T. ) ;
#102370=ORIENTED_EDGE ( 'NONE', *, *, #50201, .T. ) ;
#102372=VERTEX_POINT ( 'NONE', #78745 ) ;
#102387=CARTESIAN_POINT ( 'NONE',  ( 57.45015997180046696, 4.898587196589294500E-16, -4.000000000000007105 ) ) ;
#102398=ORIENTED_EDGE ( 'NONE', *, *, #26452, .T. ) ;
#102436=CARTESIAN_POINT ( 'NONE',  ( 0.2573354458087823704, -6.889406814520509847, 1.067197363239225760 ) ) ;
#102461=CARTESIAN_POINT ( 'NONE',  ( 66.74444444444444002, 6.915964383211875250E-15, 0.000000000000000000 ) ) ;
#102517=DIRECTION ( 'NONE',  ( -1.000000000000000000, -1.224606353822377258E-16, -0.000000000000000000 ) ) ;
#102518=VECTOR ( 'NONE', #85890, 1000.000000000000227 ) ;
#102527=ORIENTED_EDGE ( 'NONE', *, *, #84159, .T. ) ;
#102564=AXIS2_PLACEMENT_3D ( 'NONE', #58647, #1978, #17657 ) ;
#102582=DIRECTION ( 'NONE',  ( 0.000000000000000000, 0.000000000000000000, 1.000000000000000000 ) ) ;
#102634=ORIENTED_EDGE ( 'NONE', *, *, #3266, .F. ) ;
#102641=DIRECTION ( 'NONE',  ( -1.000000000000000000, -1.224606353822377258E-16, -0.000000000000000000 ) ) ;
#102678=CARTESIAN_POINT ( 'NONE',  ( 58.18888888888888999, 6.915964383211875250E-15, 0.000000000000000000 ) ) ;
#102699=ORIENTED_EDGE ( 'NONE', *, *, #58880, .F. ) ;
#102709=CARTESIAN_POINT ( 'NONE',  ( 5.700000000000000178, 0.000000000000000000, -4.400000000000000355 ) ) ;
#102799=CARTESIAN_POINT ( 'NONE',  ( 62.59428447264396311, 6.856755485862130937E-15, 0.000000000000000000 ) ) ;
#102808=VERTEX_POINT ( 'NONE', #56610 ) ;
#102812=FACE_OUTER_BOUND ( 'NONE', #66585, .T. ) ;
#102820=ORIENTED_EDGE ( 'NONE', *, *, #89043, .T. ) ;
#102831=CARTESIAN_POINT ( 'NONE',  ( 73.59428447264397732, 6.856755485862130937E-15, 0.000000000000000000 ) ) ;
#102839=DIRECTION ( 'NONE',  ( 0.5735764363510442720, -0.8191520442889930198, 1.003171929053526349E-16 ) ) ;
#102866=VERTEX_POINT ( 'NONE', #66850 ) ;
#102890=VERTEX_POINT ( 'NONE', #17777 ) ;
#102935=EDGE_CURVE ( 'NONE', #84625, #42218, #45235, .T. ) ;
#102966=VECTOR ( 'NONE', #58480, 1000.000000000000000 ) ;
#102968=ORIENTED_EDGE ( 'NONE', *, *, #39854, .T. ) ;
#102976=CIRCLE ( 'NONE', #40993, 4.000000000000007105 ) ;
#102988=AXIS2_PLACEMENT_3D ( 'NONE', #95459, #94418, #21605 ) ;
#103009=ORIENTED_EDGE ( 'NONE', *, *, #23260, .T. ) ;
#103010=CARTESIAN_POINT ( 'NONE',  ( 66.26095113931063452, 4.000000000000015099, 4.898587196589422689E-16 ) ) ;
#103015=ADVANCED_FACE ( 'NONE', ( #44172 ), #101692, .T. ) ;
#103022=ORIENTED_EDGE ( 'NONE', *, *, #71220, .T. ) ;
#103097=DIRECTION ( 'NONE',  ( -0.5735764363510497121, 0.8191520442889892450, 1.003171929053521665E-16 ) ) ;
#103117=CARTESIAN_POINT ( 'NONE',  ( 61.11682663846713837, 4.898587196589294500E-16, -4.000000000000007105 ) ) ;
#103126=DIRECTION ( 'NONE',  ( 0.000000000000000000, -1.000000000000000000, 0.000000000000000000 ) ) ;
#103192=VECTOR ( 'NONE', #1061, 1000.000000000000000 ) ;
#103195=DIRECTION ( 'NONE',  ( -1.000000000000000000, -0.000000000000000000, -0.000000000000000000 ) ) ;
#103201=VERTEX_POINT ( 'NONE', #48399 ) ;
#103211=DIRECTION ( 'NONE',  ( 0.5735764363510442720, -0.8191520442889930198, 1.003171929053526349E-16 ) ) ;
#103238=DIRECTION ( 'NONE',  ( -1.000000000000000000, -1.224606353822377258E-16, -0.000000000000000000 ) ) ;
#103261=CARTESIAN_POINT ( 'NONE',  ( 72.37206225042174879, -1.232595164407830946E-29, 4.000000000000007105 ) ) ;
#103270=EDGE_LOOP ( 'NONE', ( #20751, #84604, #14067, #101949, #53490 ) ) ;
#103294=ORIENTED_EDGE ( 'NONE', *, *, #5611, .F. ) ;
#103296=DIRECTION ( 'NONE',  ( 0.000000000000000000, 1.000000000000000000, 0.000000000000000000 ) ) ;
#103310=DIRECTION ( 'NONE',  ( 0.000000000000000000, -1.000000000000000000, 2.311253228826402606E-16 ) ) ;
#103311=DIRECTION ( 'NONE',  ( -1.000000000000000000, -1.224606353822377258E-16, -0.000000000000000000 ) ) ;
#103365=EDGE_CURVE ( 'NONE', #39236, #63624, #38138, .T. ) ;
#103384=CIRCLE ( 'NONE', #17245, 0.4000000000000001887 ) ;
#103385=DIRECTION ( 'NONE',  ( 0.000000000000000000, -1.000000000000000000, 0.000000000000000000 ) ) ;
#103403=EDGE_CURVE ( 'NONE', #54829, #85509, #43258, .T. ) ;
#103405=CARTESIAN_POINT ( 'NONE',  ( 72.37206225042174879, 6.856755485862130937E-15, 0.000000000000000000 ) ) ;
#103415=EDGE_CURVE ( 'NONE', #98286, #2681, #5373, .T. ) ;
#103417=VERTEX_POINT ( 'NONE', #10602 ) ;
#103449=DIRECTION ( 'NONE',  ( 1.000000000000000000, 1.224606353822377258E-16, 0.000000000000000000 ) ) ;
#103487=ADVANCED_FACE ( 'NONE', ( #25789 ), #12217, .F. ) ;
#103488=DIRECTION ( 'NONE',  ( 0.000000000000000000, 0.000000000000000000, 1.000000000000000000 ) ) ;
#103497=CARTESIAN_POINT ( 'NONE',  ( 0.4033376246892493855, -7.198601258566898586, 0.5316568767328675449 ) ) ;
#103515=CARTESIAN_POINT ( 'NONE',  ( 56.22793774957824553, 6.975173280561618775E-15, 0.000000000000000000 ) ) ;
#103584=EDGE_CURVE ( 'NONE', #54844, #44950, #30012, .T. ) ;
#103631=DIRECTION ( 'NONE',  ( -1.000000000000000000, -0.000000000000000000, -0.000000000000000000 ) ) ;
#103691=CARTESIAN_POINT ( 'NONE',  ( 61.37206225042174879, -1.232595164407830946E-29, 4.000000000000007105 ) ) ;
#103696=CARTESIAN_POINT ( 'NONE',  ( 4.699999999999999289, 7.505553499465139389, 0.000000000000000000 ) ) ;
#103734=CARTESIAN_POINT ( 'NONE',  ( 59.89460441624491693, -4.000000000000000000, 4.898587196589421703E-16 ) ) ;
#103781=CARTESIAN_POINT ( 'NONE',  ( 66.74444444444444002, 3.309500000000014541, 0.000000000000000000 ) ) ;
#103799=FACE_OUTER_BOUND ( 'NONE', #7294, .T. ) ;
#103808=ORIENTED_EDGE ( 'NONE', *, *, #102113, .T. ) ;
#103843=ORIENTED_EDGE ( 'NONE', *, *, #91217, .F. ) ;
#103868=AXIS2_PLACEMENT_3D ( 'NONE', #92779, #67981, #50701 ) ;
#103877=LINE ( 'NONE', #62387, #95358 ) ;
#103880=AXIS2_PLACEMENT_3D ( 'NONE', #25362, #105706, #31848 ) ;
#103882=CARTESIAN_POINT ( 'NONE',  ( 60.63333333333333286, 3.309500000000014541, 4.052968581778174646E-16 ) ) ;
#103907=DIRECTION ( 'NONE',  ( 1.000000000000000000, 1.224606353822377258E-16, 0.000000000000000000 ) ) ;
#103935=CIRCLE ( 'NONE', #103868, 3.309500000000007880 ) ;
#103960=VERTEX_POINT ( 'NONE', #12071 ) ;
#103962=VERTEX_POINT ( 'NONE', #61178 ) ;
#103980=ORIENTED_EDGE ( 'NONE', *, *, #1973, .T. ) ;
#104004=ADVANCED_FACE ( 'NONE', ( #20764 ), #93299, .T. ) ;
#104028=VERTEX_POINT ( 'NONE', #28848 ) ;
#104061=ORIENTED_EDGE ( 'NONE', *, *, #69541, .T. ) ;
#104080=CIRCLE ( 'NONE', #71363, 0.4000000000000001887 ) ;
#104085=ORIENTED_EDGE ( 'NONE', *, *, #79841, .T. ) ;
#104150=( LENGTH_UNIT ( ) NAMED_UNIT ( * ) SI_UNIT ( .MILLI., .METRE. ) );
#104161=AXIS2_PLACEMENT_3D ( 'NONE', #3008, #20322, #94705 ) ;
#104162=CIRCLE ( 'NONE', #57646, 6.499999999999999112 ) ;
#104210=FACE_OUTER_BOUND ( 'NONE', #84147, .T. ) ;
#104237=CARTESIAN_POINT ( 'NONE',  ( 68.45015997180047407, 4.000000000000014211, 0.000000000000000000 ) ) ;
#104248=CARTESIAN_POINT ( 'NONE',  ( 0.000000000000000000, 0.000000000000000000, 0.000000000000000000 ) ) ;
#104261=CARTESIAN_POINT ( 'NONE',  ( 0.000000000000000000, 4.898587196589412829E-16, -4.000000000000000000 ) ) ;
#104264=ORIENTED_EDGE ( 'NONE', *, *, #67018, .T. ) ;
#104265=EDGE_CURVE ( 'NONE', #54829, #55601, #80819, .T. ) ;
#104299=EDGE_LOOP ( 'NONE', ( #41497, #80887, #51048 ) ) ;
#104333=CARTESIAN_POINT ( 'NONE',  ( 57.45015997180046696, 6.975173280561618775E-15, 0.000000000000000000 ) ) ;
#104347=CYLINDRICAL_SURFACE ( 'NONE', #22307, 4.000000000000000000 ) ;
#104363=DIRECTION ( 'NONE',  ( -1.000000000000000000, -1.224606353822377258E-16, -0.000000000000000000 ) ) ;
#104412=LINE ( 'NONE', #103882, #59891 ) ;
#104434=DIRECTION ( 'NONE',  ( 0.000000000000000000, 1.000000000000000000, 0.000000000000000000 ) ) ;
#104449=ORIENTED_EDGE ( 'NONE', *, *, #81453, .T. ) ;
#104457=ORIENTED_EDGE ( 'NONE', *, *, #100752, .T. ) ;
#104527=DIRECTION ( 'NONE',  ( -1.000000000000000000, -1.224606353822377258E-16, -0.000000000000000000 ) ) ;
#104543=AXIS2_PLACEMENT_3D ( 'NONE', #66550, #64051, #25607 ) ;
#104564=DIRECTION ( 'NONE',  ( 0.5735764363510442720, -0.8191520442889930198, 1.003171929053526349E-16 ) ) ;
#104568=ORIENTED_EDGE ( 'NONE', *, *, #17234, .F. ) ;
#104592=ORIENTED_EDGE ( 'NONE', *, *, #93469, .T. ) ;
#104594=EDGE_CURVE ( 'NONE', #65105, #42645, #105381, .T. ) ;
#104615=VERTEX_POINT ( 'NONE', #83881 ) ;
#104652=AXIS2_PLACEMENT_3D ( 'NONE', #83109, #59931, #75000 ) ;
#104678=DIRECTION ( 'NONE',  ( -1.000000000000000000, -0.000000000000000000, 0.000000000000000000 ) ) ;
#104700=DIRECTION ( 'NONE',  ( -1.000000000000000000, -0.000000000000000000, -0.000000000000000000 ) ) ;
#104704=ORIENTED_EDGE ( 'NONE', *, *, #38929, .T. ) ;
#104705=AXIS2_PLACEMENT_3D ( 'NONE', #27012, #1609, #100321 ) ;
#104714=DIRECTION ( 'NONE',  ( -1.000000000000000000, -0.000000000000000000, -0.000000000000000000 ) ) ;
#104717=AXIS2_PLACEMENT_3D ( 'NONE', #8059, #83025, #25904 ) ;
#104774=ORIENTED_EDGE ( 'NONE', *, *, #45010, .T. ) ;
#104786=CARTESIAN_POINT ( 'NONE',  ( 0.2565376335216109638, -2.516992571280020741, 6.499999999999999112 ) ) ;
#104807=ORIENTED_EDGE ( 'NONE', *, *, #99487, .T. ) ;
#104822=DIRECTION ( 'NONE',  ( 1.000000000000000000, 1.224606353822377258E-16, 0.000000000000000000 ) ) ;
#104827=ORIENTED_EDGE ( 'NONE', *, *, #30835, .F. ) ;
#104871=CARTESIAN_POINT ( 'NONE',  ( 0.5805565836007581249, -3.752776749732553263, 6.499999999999999112 ) ) ;
#104878=EDGE_CURVE ( 'NONE', #93427, #35284, #75117, .T. ) ;
#104882=ADVANCED_FACE ( 'NONE', ( #34179 ), #43304, .T. ) ;
#104904=DIRECTION ( 'NONE',  ( 1.000000000000000000, 1.224606353822377258E-16, 0.000000000000000000 ) ) ;
#104914=ORIENTED_EDGE ( 'NONE', *, *, #21720, .F. ) ;
#104925=CIRCLE ( 'NONE', #42931, 3.309500000000007880 ) ;
#104960=DIRECTION ( 'NONE',  ( -1.000000000000000000, -1.224606353822377258E-16, -0.000000000000000000 ) ) ;
#104978=CARTESIAN_POINT ( 'NONE',  ( 71.14984002819953446, 6.856755485862130937E-15, 0.000000000000000000 ) ) ;
#104979=DIRECTION ( 'NONE',  ( -1.000000000000000000, -1.224606353822377258E-16, -0.000000000000000000 ) ) ;
#104986=CIRCLE ( 'NONE', #24092, 4.000000000000007105 ) ;
#104993=ORIENTED_EDGE ( 'NONE', *, *, #67531, .T. ) ;
#105016=EDGE_CURVE ( 'NONE', #104028, #65683, #91686, .T. ) ;
#105018=CARTESIAN_POINT ( 'NONE',  ( 61.37206225042174879, -4.000000000000000000, 0.000000000000000000 ) ) ;
#105032=VECTOR ( 'NONE', #80272, 1000.000000000000000 ) ;
#105042=EDGE_LOOP ( 'NONE', ( #12186, #12584, #106044, #10897, #13184, #58026 ) ) ;
#105055=ORIENTED_EDGE ( 'NONE', *, *, #84286, .T. ) ;
#105087=AXIS2_PLACEMENT_3D ( 'NONE', #56790, #73503, #14207 ) ;
#105113=DIRECTION ( 'NONE',  ( -1.000000000000000000, -1.224606353822377258E-16, -0.000000000000000000 ) ) ;
#105179=EDGE_CURVE ( 'NONE', #65683, #65608, #67584, .T. ) ;
#105217=DIRECTION ( 'NONE',  ( 0.000000000000000000, 1.000000000000000000, 0.000000000000000000 ) ) ;
#105237=EDGE_CURVE ( 'NONE', #30745, #61384, #48588, .T. ) ;
#105286=CYLINDRICAL_SURFACE ( 'NONE', #10984, 4.000000000000000000 ) ;
#105312=CARTESIAN_POINT ( 'NONE',  ( 54.03872891708841308, 4.000000000000015099, 4.898587196589422689E-16 ) ) ;
#105321=CARTESIAN_POINT ( 'NONE',  ( 0.05458999538772688065, -1.264741368073328376, 6.499999999999999112 ) ) ;
#105323=ORIENTED_EDGE ( 'NONE', *, *, #90686, .T. ) ;
#105347=VECTOR ( 'NONE', #91166, 1000.000000000000000 ) ;
#105368=ORIENTED_EDGE ( 'NONE', *, *, #76977, .T. ) ;
#105381=CIRCLE ( 'NONE', #34819, 4.000000000000007105 ) ;
#105410=CARTESIAN_POINT ( 'NONE',  ( 68.45015997180047407, 6.975173280561618775E-15, 0.000000000000000000 ) ) ;
#105452=DIRECTION ( 'NONE',  ( -1.000000000000000000, -0.000000000000000000, -0.000000000000000000 ) ) ;
#105487=CIRCLE ( 'NONE', #46884, 4.000000000000007105 ) ;
#105492=CARTESIAN_POINT ( 'NONE',  ( 0.4037800551813687799, 4.058962678540087410, -5.969670414742687115 ) ) ;
#105514=ORIENTED_EDGE ( 'NONE', *, *, #19204, .T. ) ;
#105520=DIRECTION ( 'NONE',  ( 0.000000000000000000, -1.000000000000000000, 0.000000000000000000 ) ) ;
#105589=CIRCLE ( 'NONE', #9108, 3.309499999999999886 ) ;
#105671=FACE_OUTER_BOUND ( 'NONE', #12672, .T. ) ;
#105706=DIRECTION ( 'NONE',  ( -1.000000000000000000, -0.000000000000000000, 0.000000000000000000 ) ) ;
#105709=ADVANCED_FACE ( 'NONE', ( #50457 ), #17462, .T. ) ;
#105730=VERTEX_POINT ( 'NONE', #10011 ) ;
#105732=CIRCLE ( 'NONE', #81609, 4.000000000000007105 ) ;
#105823=ORIENTED_EDGE ( 'NONE', *, *, #67144, .T. ) ;
#105841=AXIS2_PLACEMENT_3D ( 'NONE', #44165, #2084, #75454 ) ;
#105844=CARTESIAN_POINT ( 'NONE',  ( 53.78349330513380266, 6.975173280561618775E-15, 0.000000000000000000 ) ) ;
#105857=VERTEX_POINT ( 'NONE', #7221 ) ;
#105865=CARTESIAN_POINT ( 'NONE',  ( 4.699999999999999289, 5.629165124598843661, -3.250000000000011990 ) ) ;
#105869=VERTEX_POINT ( 'NONE', #82714 ) ;
#105909=ORIENTED_EDGE ( 'NONE', *, *, #85776, .T. ) ;
#105940=DIRECTION ( 'NONE',  ( 0.000000000000000000, -0.5000000000000018874, -0.8660254037844374864 ) ) ;
#105955=VERTEX_POINT ( 'NONE', #73950 ) ;
#105994=VECTOR ( 'NONE', #95112, 1000.000000000000000 ) ;
#106004=CARTESIAN_POINT ( 'NONE',  ( 0.06682554136337624795, 4.993536075455413226, -4.350941807883113022 ) ) ;
#106025=DIRECTION ( 'NONE',  ( -1.000000000000000000, -0.000000000000000000, -0.000000000000000000 ) ) ;
#106044=ORIENTED_EDGE ( 'NONE', *, *, #61304, .F. ) ;
#106067=AXIS2_PLACEMENT_3D ( 'NONE', #31048, #32088, #80078 ) ;
#106069=AXIS2_PLACEMENT_3D ( 'NONE', #45474, #13601, #96139 ) ;
#106103=LINE ( 'NONE', #72687, #7965 ) ;
#106120=ORIENTED_EDGE ( 'NONE', *, *, #57156, .F. ) ;
#106148=DIRECTION ( 'NONE',  ( 0.000000000000000000, -1.000000000000000000, 0.000000000000000000 ) ) ;
#106156=ORIENTED_EDGE ( 'NONE', *, *, #74880, .F. ) ;
#106162=CARTESIAN_POINT ( 'NONE',  ( 68.70539558375507738, 6.856755485862130937E-15, 0.000000000000000000 ) ) ;
#106169=VERTEX_POINT ( 'NONE', #25455 ) ;
#106203=DIRECTION ( 'NONE',  ( 0.000000000000000000, -1.000000000000000000, 0.000000000000000000 ) ) ;
#106204=VERTEX_POINT ( 'NONE', #68001 ) ;
#106205=VERTEX_POINT ( 'NONE', #1649 ) ;
#106260=SURFACE_STYLE_FILL_AREA ( #48560 ) ;
#106270=ORIENTED_EDGE ( 'NONE', *, *, #60688, .T. ) ;
#106281=PLANE ( 'NONE',  #12323 ) ;
#106304=CARTESIAN_POINT ( 'NONE',  ( 53.29999999999999716, 3.309500000000014541, 0.000000000000000000 ) ) ;
#106319=ORIENTED_EDGE ( 'NONE', *, *, #36377, .T. ) ;
#106369=VECTOR ( 'NONE', #75957, 1000.000000000000000 ) ;
#106413=DIRECTION ( 'NONE',  ( -1.000000000000000000, -1.224606353822377258E-16, -0.000000000000000000 ) ) ;
#106426=AXIS2_PLACEMENT_3D ( 'NONE', #68547, #78726, #35669 ) ;
#106442=CIRCLE ( 'NONE', #41018, 4.000000000000007105 ) ;
#106450=ORIENTED_EDGE ( 'NONE', *, *, #102113, .F. ) ;
#106455=ORIENTED_EDGE ( 'NONE', *, *, #74003, .F. ) ;
#106459=DIRECTION ( 'NONE',  ( 0.000000000000000000, -1.000000000000000000, 0.000000000000000000 ) ) ;
#106460=CARTESIAN_POINT ( 'NONE',  ( 72.37206225042174879, 6.856755485862130937E-15, 0.000000000000000000 ) ) ;
#106466=EDGE_CURVE ( 'NONE', #32281, #8358, #93291, .T. ) ;
#106477=EDGE_LOOP ( 'NONE', ( #104827, #25638, #50761, #44904, #70820 ) ) ;
#106592=ORIENTED_EDGE ( 'NONE', *, *, #55462, .F. ) ;
#106618=ORIENTED_EDGE ( 'NONE', *, *, #52493, .T. ) ;
#106628=EDGE_CURVE ( 'NONE', #60384, #103201, #17615, .T. ) ;
#106632=DIRECTION ( 'NONE',  ( 0.000000000000000000, -1.000000000000000000, 0.000000000000000000 ) ) ;
#106666=ORIENTED_EDGE ( 'NONE', *, *, #48029, .F. ) ;
#106689=DIRECTION ( 'NONE',  ( -1.000000000000000000, -1.224606353822377258E-16, -0.000000000000000000 ) ) ;
#106758=ORIENTED_EDGE ( 'NONE', *, *, #73892, .F. ) ;
#106782=AXIS2_PLACEMENT_3D ( 'NONE', #64521, #104979, #38662 ) ;
ENDSEC;
END-ISO-10303-21;
